ISO-10303-21;
HEADER;
/* Generated by software containing ST-Developer
 * from STEP Tools, Inc. (www.steptools.com) 
 */

FILE_DESCRIPTION(
/* description */ (''),
/* implementation_level */ '2;1');

FILE_NAME(
/* name */ 'Socket head cap screw M3x16.step',
/* time_stamp */ '2026-11-10T09:14:46-08:00',
/* author */ (''),
/* organization */ (''),
/* preprocessor_version */ 'ST-DEVELOPER v20.2',
/* originating_system */ 'Autodesk Translation Framework v15.17.0.0',
/* authorisation */ '');

FILE_SCHEMA (('AUTOMOTIVE_DESIGN { 1 0 10303 214 3 1 1 }'));
ENDSEC;

DATA;
#10=MECHANICAL_DESIGN_GEOMETRIC_PRESENTATION_REPRESENTATION('',(#565),#19471);
#75=CONICAL_SURFACE('',#7749,0.1,0.785398163397448);
#168=B_SPLINE_SURFACE_WITH_KNOTS('',3,3,((#16719,#16720,#16721,#16722,#16723,
#16724,#16725,#16726,#16727,#16728,#16729,#16730,#16731,#16732,#16733,#16734,
#16735,#16736,#16737,#16738,#16739,#16740,#16741,#16742,#16743,#16744,#16745,
#16746,#16747,#16748,#16749,#16750,#16751,#16752,#16753,#16754,#16755,#16756,
#16757,#16758,#16759,#16760,#16761,#16762,#16763,#16764,#16765,#16766,#16767,
#16768,#16769,#16770,#16771,#16772,#16773,#16774,#16775,#16776,#16777,#16778,
#16779,#16780,#16781,#16782,#16783,#16784,#16785,#16786,#16787,#16788,#16789,
#16790,#16791,#16792,#16793,#16794,#16795,#16796,#16797,#16798,#16799,#16800,
#16801,#16802,#16803,#16804,#16805,#16806,#16807,#16808,#16809,#16810,#16811,
#16812,#16813,#16814,#16815,#16816,#16817,#16818,#16819,#16820,#16821,#16822,
#16823,#16824,#16825,#16826,#16827,#16828,#16829,#16830,#16831,#16832,#16833,
#16834,#16835,#16836,#16837,#16838,#16839,#16840,#16841,#16842,#16843,#16844,
#16845,#16846,#16847,#16848,#16849,#16850,#16851,#16852,#16853,#16854,#16855,
#16856,#16857,#16858,#16859,#16860,#16861,#16862,#16863,#16864,#16865,#16866,
#16867,#16868,#16869,#16870,#16871,#16872,#16873,#16874,#16875,#16876,#16877,
#16878,#16879,#16880,#16881,#16882,#16883,#16884,#16885,#16886,#16887,#16888,
#16889,#16890,#16891,#16892,#16893,#16894,#16895,#16896,#16897,#16898,#16899,
#16900,#16901,#16902,#16903,#16904,#16905,#16906,#16907,#16908,#16909,#16910,
#16911,#16912,#16913,#16914),(#16915,#16916,#16917,#16918,#16919,#16920,
#16921,#16922,#16923,#16924,#16925,#16926,#16927,#16928,#16929,#16930,#16931,
#16932,#16933,#16934,#16935,#16936,#16937,#16938,#16939,#16940,#16941,#16942,
#16943,#16944,#16945,#16946,#16947,#16948,#16949,#16950,#16951,#16952,#16953,
#16954,#16955,#16956,#16957,#16958,#16959,#16960,#16961,#16962,#16963,#16964,
#16965,#16966,#16967,#16968,#16969,#16970,#16971,#16972,#16973,#16974,#16975,
#16976,#16977,#16978,#16979,#16980,#16981,#16982,#16983,#16984,#16985,#16986,
#16987,#16988,#16989,#16990,#16991,#16992,#16993,#16994,#16995,#16996,#16997,
#16998,#16999,#17000,#17001,#17002,#17003,#17004,#17005,#17006,#17007,#17008,
#17009,#17010,#17011,#17012,#17013,#17014,#17015,#17016,#17017,#17018,#17019,
#17020,#17021,#17022,#17023,#17024,#17025,#17026,#17027,#17028,#17029,#17030,
#17031,#17032,#17033,#17034,#17035,#17036,#17037,#17038,#17039,#17040,#17041,
#17042,#17043,#17044,#17045,#17046,#17047,#17048,#17049,#17050,#17051,#17052,
#17053,#17054,#17055,#17056,#17057,#17058,#17059,#17060,#17061,#17062,#17063,
#17064,#17065,#17066,#17067,#17068,#17069,#17070,#17071,#17072,#17073,#17074,
#17075,#17076,#17077,#17078,#17079,#17080,#17081,#17082,#17083,#17084,#17085,
#17086,#17087,#17088,#17089,#17090,#17091,#17092,#17093,#17094,#17095,#17096,
#17097,#17098,#17099,#17100,#17101,#17102,#17103,#17104,#17105,#17106,#17107,
#17108,#17109,#17110),(#17111,#17112,#17113,#17114,#17115,#17116,#17117,
#17118,#17119,#17120,#17121,#17122,#17123,#17124,#17125,#17126,#17127,#17128,
#17129,#17130,#17131,#17132,#17133,#17134,#17135,#17136,#17137,#17138,#17139,
#17140,#17141,#17142,#17143,#17144,#17145,#17146,#17147,#17148,#17149,#17150,
#17151,#17152,#17153,#17154,#17155,#17156,#17157,#17158,#17159,#17160,#17161,
#17162,#17163,#17164,#17165,#17166,#17167,#17168,#17169,#17170,#17171,#17172,
#17173,#17174,#17175,#17176,#17177,#17178,#17179,#17180,#17181,#17182,#17183,
#17184,#17185,#17186,#17187,#17188,#17189,#17190,#17191,#17192,#17193,#17194,
#17195,#17196,#17197,#17198,#17199,#17200,#17201,#17202,#17203,#17204,#17205,
#17206,#17207,#17208,#17209,#17210,#17211,#17212,#17213,#17214,#17215,#17216,
#17217,#17218,#17219,#17220,#17221,#17222,#17223,#17224,#17225,#17226,#17227,
#17228,#17229,#17230,#17231,#17232,#17233,#17234,#17235,#17236,#17237,#17238,
#17239,#17240,#17241,#17242,#17243,#17244,#17245,#17246,#17247,#17248,#17249,
#17250,#17251,#17252,#17253,#17254,#17255,#17256,#17257,#17258,#17259,#17260,
#17261,#17262,#17263,#17264,#17265,#17266,#17267,#17268,#17269,#17270,#17271,
#17272,#17273,#17274,#17275,#17276,#17277,#17278,#17279,#17280,#17281,#17282,
#17283,#17284,#17285,#17286,#17287,#17288,#17289,#17290,#17291,#17292,#17293,
#17294,#17295,#17296,#17297,#17298,#17299,#17300,#17301,#17302,#17303,#17304,
#17305,#17306),(#17307,#17308,#17309,#17310,#17311,#17312,#17313,#17314,
#17315,#17316,#17317,#17318,#17319,#17320,#17321,#17322,#17323,#17324,#17325,
#17326,#17327,#17328,#17329,#17330,#17331,#17332,#17333,#17334,#17335,#17336,
#17337,#17338,#17339,#17340,#17341,#17342,#17343,#17344,#17345,#17346,#17347,
#17348,#17349,#17350,#17351,#17352,#17353,#17354,#17355,#17356,#17357,#17358,
#17359,#17360,#17361,#17362,#17363,#17364,#17365,#17366,#17367,#17368,#17369,
#17370,#17371,#17372,#17373,#17374,#17375,#17376,#17377,#17378,#17379,#17380,
#17381,#17382,#17383,#17384,#17385,#17386,#17387,#17388,#17389,#17390,#17391,
#17392,#17393,#17394,#17395,#17396,#17397,#17398,#17399,#17400,#17401,#17402,
#17403,#17404,#17405,#17406,#17407,#17408,#17409,#17410,#17411,#17412,#17413,
#17414,#17415,#17416,#17417,#17418,#17419,#17420,#17421,#17422,#17423,#17424,
#17425,#17426,#17427,#17428,#17429,#17430,#17431,#17432,#17433,#17434,#17435,
#17436,#17437,#17438,#17439,#17440,#17441,#17442,#17443,#17444,#17445,#17446,
#17447,#17448,#17449,#17450,#17451,#17452,#17453,#17454,#17455,#17456,#17457,
#17458,#17459,#17460,#17461,#17462,#17463,#17464,#17465,#17466,#17467,#17468,
#17469,#17470,#17471,#17472,#17473,#17474,#17475,#17476,#17477,#17478,#17479,
#17480,#17481,#17482,#17483,#17484,#17485,#17486,#17487,#17488,#17489,#17490,
#17491,#17492,#17493,#17494,#17495,#17496,#17497,#17498,#17499,#17500,#17501,
#17502)),.UNSPECIFIED.,.F.,.F.,.F.,(4,4),(4,1,1,1,1,1,1,1,1,1,1,1,1,1,1,
1,1,1,1,1,1,1,1,1,1,1,1,1,1,1,1,1,1,1,1,1,1,1,1,1,1,1,1,1,1,1,1,1,1,1,1,
1,1,1,1,1,1,1,1,1,1,1,1,1,1,1,1,1,1,1,1,1,1,1,1,1,1,1,1,1,1,1,1,1,1,1,1,
1,1,1,1,1,1,1,1,1,1,1,1,1,1,1,1,1,1,1,1,1,1,1,1,1,1,1,1,1,1,1,1,1,1,1,1,
1,1,1,1,1,1,1,1,1,1,1,1,1,1,1,1,1,1,1,1,1,1,1,1,1,1,1,1,1,1,1,1,1,1,1,1,
1,1,1,1,1,1,1,1,1,1,1,1,1,1,1,1,1,1,1,1,1,1,1,1,1,1,1,1,1,1,1,1,1,1,4),
(0.,0.0329955678841871),(11.6159397475006,12.61358260836,13.6112254692194,
14.6088683300789,15.6065111909383,16.6041540517977,17.6017969126571,18.5994397735165,
19.5970826343759,20.5947254952353,21.5923683560947,22.5900112169541,23.5876540778135,
24.5852969386729,25.5829397995323,26.5805826603917,27.5782255212511,28.5758683821105,
29.5735112429699,30.5711541038294,31.5687969646888,32.5664398255482,33.5640826864076,
34.561725547267,35.5593684081264,36.5570112689858,37.5546541298452,38.5522969907046,
39.549939851564,40.5475827124234,41.5452255732828,42.5428684341422,43.5405112950016,
44.538154155861,45.5357970167204,46.5334398775799,47.5310827384393,48.5287255992987,
49.5263684601581,50.5240113210175,51.5216541818769,52.5192970427363,53.5169399035957,
54.5145827644551,55.5122256253145,56.5098684861739,57.5075113470333,58.5051542078927,
59.5027970687521,60.5004399296115,61.4980827904709,62.4957256513303,63.4933685121897,
64.4910113730492,65.4886542339086,66.486297094768,67.4839399556274,68.4815828164868,
69.4792256773462,70.4768685382056,71.474511399065,72.4721542599244,73.4697971207838,
74.4674399816432,75.4650828425026,76.462725703362,77.4603685642214,78.4580114250808,
79.4556542859402,80.4532971467996,81.4509400076591,82.4485828685185,83.4462257293779,
84.4438685902373,85.4415114510967,86.4391543119561,87.4367971728155,88.4344400336749,
89.4320828945343,90.4297257553937,91.4273686162531,92.4250114771125,93.4226543379719,
94.4202971988313,95.4179400596907,96.4155829205502,97.4132257814096,98.410868642269,
99.4085115031284,100.406154363988,101.403797224847,102.401440085707,103.399082946566,
104.396725807425,105.394368668285,106.392011529144,107.389654390004,108.387297250863,
109.384940111722,110.382582972582,111.380225833441,112.377868694301,113.37551155516,
114.373154416019,115.370797276879,116.368440137738,117.366082998598,118.363725859457,
119.361368720316,120.359011581176,121.356654442035,122.354297302895,123.351940163754,
124.349583024614,125.347225885473,126.344868746332,127.342511607192,128.340154468051,
129.337797328911,130.33544018977,131.333083050629,132.330725911489,133.328368772348,
134.326011633208,135.323654494067,136.321297354926,137.318940215786,138.316583076645,
139.314225937505,140.311868798364,141.309511659223,142.307154520083,143.304797380942,
144.302440241802,145.300083102661,146.29772596352,147.29536882438,148.293011685239,
149.290654546099,150.288297406958,151.285940267817,152.283583128677,153.281225989536,
154.278868850396,155.276511711255,156.274154572115,157.271797432974,158.269440293833,
159.267083154693,160.264726015552,161.262368876412,162.260011737271,163.25765459813,
164.25529745899,165.252940319849,166.250583180709,167.248226041568,168.245868902427,
169.243511763287,170.241154624146,171.238797485006,172.236440345865,173.234083206724,
174.231726067584,175.229368928443,176.227011789303,177.224654650162,178.222297511021,
179.219940371881,180.21758323274,181.2152260936,182.212868954459,183.210511815318,
184.208154676178,185.205797537037,186.203440397897,187.201083258756,188.198726119616,
189.196368980475,190.194011841334,191.191654702194,192.189297563053,193.186940423913,
194.184583284772,195.182226145631,196.179869006491,197.17751186735,198.17515472821,
199.172797589069,200.170440449928,201.168083310788,202.165726171647,203.163369032507,
204.161011893366),.UNSPECIFIED.);
#169=B_SPLINE_SURFACE_WITH_KNOTS('',3,3,((#17592,#17593,#17594,#17595,#17596,
#17597,#17598,#17599,#17600,#17601,#17602,#17603,#17604,#17605,#17606,#17607,
#17608,#17609,#17610,#17611,#17612,#17613,#17614,#17615,#17616,#17617,#17618,
#17619,#17620,#17621,#17622,#17623,#17624,#17625,#17626,#17627,#17628,#17629,
#17630,#17631,#17632,#17633,#17634,#17635,#17636,#17637,#17638,#17639,#17640,
#17641,#17642,#17643,#17644,#17645,#17646,#17647,#17648,#17649,#17650,#17651,
#17652,#17653,#17654,#17655,#17656,#17657,#17658,#17659,#17660,#17661,#17662,
#17663,#17664,#17665,#17666,#17667,#17668,#17669,#17670,#17671,#17672,#17673,
#17674,#17675,#17676,#17677,#17678,#17679,#17680,#17681,#17682,#17683,#17684,
#17685,#17686,#17687,#17688,#17689,#17690,#17691,#17692,#17693,#17694,#17695,
#17696,#17697,#17698,#17699,#17700,#17701,#17702,#17703,#17704,#17705,#17706,
#17707,#17708,#17709,#17710,#17711,#17712,#17713,#17714,#17715,#17716,#17717,
#17718,#17719,#17720,#17721,#17722,#17723,#17724,#17725,#17726,#17727,#17728,
#17729,#17730,#17731,#17732,#17733,#17734,#17735,#17736,#17737,#17738,#17739,
#17740,#17741,#17742,#17743,#17744,#17745,#17746,#17747,#17748,#17749,#17750,
#17751,#17752,#17753,#17754,#17755,#17756,#17757,#17758,#17759,#17760,#17761,
#17762,#17763,#17764,#17765,#17766,#17767,#17768,#17769,#17770,#17771,#17772,
#17773,#17774,#17775,#17776,#17777,#17778,#17779,#17780,#17781,#17782,#17783,
#17784,#17785,#17786,#17787,#17788,#17789),(#17790,#17791,#17792,#17793,
#17794,#17795,#17796,#17797,#17798,#17799,#17800,#17801,#17802,#17803,#17804,
#17805,#17806,#17807,#17808,#17809,#17810,#17811,#17812,#17813,#17814,#17815,
#17816,#17817,#17818,#17819,#17820,#17821,#17822,#17823,#17824,#17825,#17826,
#17827,#17828,#17829,#17830,#17831,#17832,#17833,#17834,#17835,#17836,#17837,
#17838,#17839,#17840,#17841,#17842,#17843,#17844,#17845,#17846,#17847,#17848,
#17849,#17850,#17851,#17852,#17853,#17854,#17855,#17856,#17857,#17858,#17859,
#17860,#17861,#17862,#17863,#17864,#17865,#17866,#17867,#17868,#17869,#17870,
#17871,#17872,#17873,#17874,#17875,#17876,#17877,#17878,#17879,#17880,#17881,
#17882,#17883,#17884,#17885,#17886,#17887,#17888,#17889,#17890,#17891,#17892,
#17893,#17894,#17895,#17896,#17897,#17898,#17899,#17900,#17901,#17902,#17903,
#17904,#17905,#17906,#17907,#17908,#17909,#17910,#17911,#17912,#17913,#17914,
#17915,#17916,#17917,#17918,#17919,#17920,#17921,#17922,#17923,#17924,#17925,
#17926,#17927,#17928,#17929,#17930,#17931,#17932,#17933,#17934,#17935,#17936,
#17937,#17938,#17939,#17940,#17941,#17942,#17943,#17944,#17945,#17946,#17947,
#17948,#17949,#17950,#17951,#17952,#17953,#17954,#17955,#17956,#17957,#17958,
#17959,#17960,#17961,#17962,#17963,#17964,#17965,#17966,#17967,#17968,#17969,
#17970,#17971,#17972,#17973,#17974,#17975,#17976,#17977,#17978,#17979,#17980,
#17981,#17982,#17983,#17984,#17985,#17986,#17987),(#17988,#17989,#17990,
#17991,#17992,#17993,#17994,#17995,#17996,#17997,#17998,#17999,#18000,#18001,
#18002,#18003,#18004,#18005,#18006,#18007,#18008,#18009,#18010,#18011,#18012,
#18013,#18014,#18015,#18016,#18017,#18018,#18019,#18020,#18021,#18022,#18023,
#18024,#18025,#18026,#18027,#18028,#18029,#18030,#18031,#18032,#18033,#18034,
#18035,#18036,#18037,#18038,#18039,#18040,#18041,#18042,#18043,#18044,#18045,
#18046,#18047,#18048,#18049,#18050,#18051,#18052,#18053,#18054,#18055,#18056,
#18057,#18058,#18059,#18060,#18061,#18062,#18063,#18064,#18065,#18066,#18067,
#18068,#18069,#18070,#18071,#18072,#18073,#18074,#18075,#18076,#18077,#18078,
#18079,#18080,#18081,#18082,#18083,#18084,#18085,#18086,#18087,#18088,#18089,
#18090,#18091,#18092,#18093,#18094,#18095,#18096,#18097,#18098,#18099,#18100,
#18101,#18102,#18103,#18104,#18105,#18106,#18107,#18108,#18109,#18110,#18111,
#18112,#18113,#18114,#18115,#18116,#18117,#18118,#18119,#18120,#18121,#18122,
#18123,#18124,#18125,#18126,#18127,#18128,#18129,#18130,#18131,#18132,#18133,
#18134,#18135,#18136,#18137,#18138,#18139,#18140,#18141,#18142,#18143,#18144,
#18145,#18146,#18147,#18148,#18149,#18150,#18151,#18152,#18153,#18154,#18155,
#18156,#18157,#18158,#18159,#18160,#18161,#18162,#18163,#18164,#18165,#18166,
#18167,#18168,#18169,#18170,#18171,#18172,#18173,#18174,#18175,#18176,#18177,
#18178,#18179,#18180,#18181,#18182,#18183,#18184,#18185),(#18186,#18187,
#18188,#18189,#18190,#18191,#18192,#18193,#18194,#18195,#18196,#18197,#18198,
#18199,#18200,#18201,#18202,#18203,#18204,#18205,#18206,#18207,#18208,#18209,
#18210,#18211,#18212,#18213,#18214,#18215,#18216,#18217,#18218,#18219,#18220,
#18221,#18222,#18223,#18224,#18225,#18226,#18227,#18228,#18229,#18230,#18231,
#18232,#18233,#18234,#18235,#18236,#18237,#18238,#18239,#18240,#18241,#18242,
#18243,#18244,#18245,#18246,#18247,#18248,#18249,#18250,#18251,#18252,#18253,
#18254,#18255,#18256,#18257,#18258,#18259,#18260,#18261,#18262,#18263,#18264,
#18265,#18266,#18267,#18268,#18269,#18270,#18271,#18272,#18273,#18274,#18275,
#18276,#18277,#18278,#18279,#18280,#18281,#18282,#18283,#18284,#18285,#18286,
#18287,#18288,#18289,#18290,#18291,#18292,#18293,#18294,#18295,#18296,#18297,
#18298,#18299,#18300,#18301,#18302,#18303,#18304,#18305,#18306,#18307,#18308,
#18309,#18310,#18311,#18312,#18313,#18314,#18315,#18316,#18317,#18318,#18319,
#18320,#18321,#18322,#18323,#18324,#18325,#18326,#18327,#18328,#18329,#18330,
#18331,#18332,#18333,#18334,#18335,#18336,#18337,#18338,#18339,#18340,#18341,
#18342,#18343,#18344,#18345,#18346,#18347,#18348,#18349,#18350,#18351,#18352,
#18353,#18354,#18355,#18356,#18357,#18358,#18359,#18360,#18361,#18362,#18363,
#18364,#18365,#18366,#18367,#18368,#18369,#18370,#18371,#18372,#18373,#18374,
#18375,#18376,#18377,#18378,#18379,#18380,#18381,#18382,#18383)),
 .UNSPECIFIED.,.F.,.F.,.F.,(4,4),(4,1,1,1,1,1,1,1,1,1,1,1,1,1,1,1,1,1,1,
1,1,1,1,1,1,1,1,1,1,1,1,1,1,1,1,1,1,1,1,1,1,1,1,1,1,1,1,1,1,1,1,1,1,1,1,
1,1,1,1,1,1,1,1,1,1,1,1,1,1,1,1,1,1,1,1,1,1,1,1,1,1,1,1,1,1,1,1,1,1,1,1,
1,1,1,1,1,1,1,1,1,1,1,1,1,1,1,1,1,1,1,1,1,1,1,1,1,1,1,1,1,1,1,1,1,1,1,1,
1,1,1,1,1,1,1,1,1,1,1,1,1,1,1,1,1,1,1,1,1,1,1,1,1,1,1,1,1,1,1,1,1,1,1,1,
1,1,1,1,1,1,1,1,1,1,1,1,1,1,1,1,1,1,1,1,1,1,1,1,1,1,1,1,1,1,1,1,4),(0.,
0.0329955678841871),(8.30203615430855,9.30007843543257,10.2981207165566,
11.2961629976806,12.2942052788047,13.2922475599287,14.2902898410527,15.2883321221767,
16.2863744033008,17.2844166844248,18.2824589655488,19.2805012466728,20.2785435277969,
21.2765858089209,22.2746280900449,23.272670371169,24.270712652293,25.268754933417,
26.266797214541,27.2648394956651,28.2628817767891,29.2609240579131,30.2589663390371,
31.2570086201612,32.2550509012852,33.2530931824092,34.2511354635333,35.2491777446573,
36.2472200257813,37.2452623069053,38.2433045880294,39.2413468691534,40.2393891502774,
41.2374314314014,42.2354737125255,43.2335159936495,44.2315582747735,45.2296005558975,
46.2276428370216,47.2256851181456,48.2237273992696,49.2217696803937,50.2198119615177,
51.2178542426417,52.2158965237657,53.2139388048898,54.2119810860138,55.2100233671378,
56.2080656482619,57.2061079293859,58.2041502105099,59.2021924916339,60.200234772758,
61.198277053882,62.196319335006,63.19436161613,64.1924038972541,65.1904461783781,
66.1884884595021,67.1865307406262,68.1845730217502,69.1826153028742,70.1806575839982,
71.1786998651223,72.1767421462463,73.1747844273703,74.1728267084943,75.1708689896184,
76.1689112707424,77.1669535518664,78.1649958329905,79.1630381141145,80.1610803952385,
81.1591226763625,82.1571649574865,83.1552072386106,84.1532495197346,85.1512918008586,
86.1493340819827,87.1473763631067,88.1454186442307,89.1434609253548,90.1415032064788,
91.1395454876028,92.1375877687268,93.1356300498508,94.1336723309749,95.1317146120989,
96.1297568932229,97.127799174347,98.125841455471,99.123883736595,100.121926017719,
101.119968298843,102.118010579967,103.116052861091,104.114095142215,105.112137423339,
106.110179704463,107.108221985587,108.106264266711,109.104306547835,110.102348828959,
111.100391110083,112.098433391207,113.096475672331,114.094517953455,115.092560234579,
116.090602515703,117.088644796828,118.086687077952,119.084729359076,120.0827716402,
121.080813921324,122.078856202448,123.076898483572,124.074940764696,125.07298304582,
126.071025326944,127.069067608068,128.067109889192,129.065152170316,130.06319445144,
131.061236732564,132.059279013688,133.057321294812,134.055363575936,135.05340585706,
136.051448138184,137.049490419308,138.047532700432,139.045574981556,140.04361726268,
141.041659543804,142.039701824928,143.037744106052,144.035786387176,145.0338286683,
146.031870949424,147.029913230548,148.027955511672,149.025997792796,150.02404007392,
151.022082355044,152.020124636168,153.018166917292,154.016209198417,155.014251479541,
156.012293760665,157.010336041789,158.008378322913,159.006420604037,160.004462885161,
161.002505166285,162.000547447409,162.998589728533,163.996632009657,164.994674290781,
165.992716571905,166.990758853029,167.988801134153,168.986843415277,169.984885696401,
170.982927977525,171.980970258649,172.979012539773,173.977054820897,174.975097102021,
175.973139383145,176.971181664269,177.969223945393,178.967266226517,179.965308507641,
180.963350788765,181.961393069889,182.959435351013,183.957477632137,184.955519913261,
185.953562194385,186.951604475509,187.949646756633,188.947689037757,189.945731318881,
190.943773600006,191.94181588113,192.939858162254,193.937900443378,194.935942724502,
195.933985005626,196.93202728675,197.930069567874,198.928111848998,199.926154130122,
200.924196411246,201.92223869237,202.920280973494),.UNSPECIFIED.);
#382=B_SPLINE_CURVE_WITH_KNOTS('',3,(#14343,#14344,#14345,#14346,#14347,
#14348,#14349,#14350,#14351,#14352),.UNSPECIFIED.,.F.,.F.,(4,3,3,4),(-4.09202352044852,
-3.99057144343763,-2.99292858257822,-2.07317267331971),.UNSPECIFIED.);
#383=B_SPLINE_CURVE_WITH_KNOTS('',3,(#14355,#14356,#14357,#14358,#14359,
#14360,#14361),.UNSPECIFIED.,.F.,.F.,(4,3,4),(0.,0.998042281124014,1.12274180646116),
 .UNSPECIFIED.);
#384=B_SPLINE_CURVE_WITH_KNOTS('',3,(#14366,#14367,#14368,#14369,#14370,
#14371,#14372,#14373,#14374,#14375,#14376,#14377,#14378,#14379,#14380,#14381,
#14382,#14383,#14384,#14385,#14386,#14387),.UNSPECIFIED.,.F.,.F.,(4,3,3,
3,3,3,3,4),(-10.3752088276281,-9.97642860859406,-8.97878574773466,-7.98114288687525,
-6.98350002601584,-5.98585716515644,-4.98821430429703,-4.09202352044852),
 .UNSPECIFIED.);
#385=B_SPLINE_CURVE_WITH_KNOTS('',3,(#14388,#14389,#14390,#14391,#14392,
#14393,#14394,#14395,#14396,#14397,#14398,#14399,#14400,#14401,#14402,#14403,
#14404,#14405,#14406,#14407,#14408,#14409),.UNSPECIFIED.,.F.,.F.,(4,3,3,
3,3,3,3,4),(1.12274180646116,1.99608456224804,2.99412684337208,3.99216912449611,
4.99021140562014,5.98825368674417,6.98629596786821,7.40592711364074),
 .UNSPECIFIED.);
#386=B_SPLINE_CURVE_WITH_KNOTS('',3,(#14414,#14415,#14416,#14417,#14418,
#14419,#14420,#14421,#14422,#14423,#14424,#14425,#14426,#14427,#14428,#14429,
#14430,#14431,#14432,#14433,#14434,#14435),.UNSPECIFIED.,.F.,.F.,(4,3,3,
3,3,3,3,4),(-16.6583941348077,-15.9622857737505,-14.9646429128911,-13.9670000520317,
-12.9693571911723,-11.9717143303129,-10.9740714694535,-10.3752088276281),
 .UNSPECIFIED.);
#387=B_SPLINE_CURVE_WITH_KNOTS('',3,(#14436,#14437,#14438,#14439,#14440,
#14441,#14442,#14443,#14444,#14445,#14446,#14447,#14448,#14449,#14450,#14451,
#14452,#14453,#14454,#14455,#14456,#14457),.UNSPECIFIED.,.F.,.F.,(4,3,3,
3,3,3,3,4),(7.40592711364074,7.98433824899223,8.98238053011626,9.98042281124028,
10.9784650923643,11.9765073734883,12.9745496546124,13.6891124208203),
 .UNSPECIFIED.);
#388=B_SPLINE_CURVE_WITH_KNOTS('',3,(#14462,#14463,#14464,#14465,#14466,
#14467,#14468,#14469,#14470,#14471,#14472,#14473,#14474,#14475,#14476,#14477,
#14478,#14479,#14480,#14481,#14482,#14483),.UNSPECIFIED.,.F.,.F.,(4,3,3,
3,3,3,3,4),(-22.9415794419873,-21.9481429389069,-20.9505000780475,-19.9528572171881,
-18.9552143563287,-17.9575714954693,-16.9599286346099,-16.6583941348077),
 .UNSPECIFIED.);
#389=B_SPLINE_CURVE_WITH_KNOTS('',3,(#14484,#14485,#14486,#14487,#14488,
#14489,#14490,#14491,#14492,#14493,#14494,#14495,#14496,#14497,#14498,#14499,
#14500,#14501,#14502,#14503,#14504,#14505,#14506,#14507,#14508),
 .UNSPECIFIED.,.F.,.F.,(4,3,3,3,3,3,3,3,4),(13.6891124208203,13.9725919357364,
14.9706342168604,15.9686764979844,16.9667187791085,17.9647610602325,18.9628033413565,
19.9608456224805,19.9722977279999),.UNSPECIFIED.);
#390=B_SPLINE_CURVE_WITH_KNOTS('',3,(#14513,#14514,#14515,#14516,#14517,
#14518,#14519,#14520,#14521,#14522,#14523,#14524,#14525,#14526,#14527,#14528,
#14529,#14530,#14531,#14532,#14533,#14534),.UNSPECIFIED.,.F.,.F.,(4,3,3,
3,3,3,3,4),(-29.2247647491669,-28.9316429649228,-27.9340001040634,-26.936357243204,
-25.9387143823446,-24.9410715214852,-23.9434286606257,-22.9415794419873),
 .UNSPECIFIED.);
#391=B_SPLINE_CURVE_WITH_KNOTS('',3,(#14535,#14536,#14537,#14538,#14539,
#14540,#14541,#14542,#14543,#14544,#14545,#14546,#14547,#14548,#14549,#14550,
#14551,#14552,#14553,#14554,#14555,#14556),.UNSPECIFIED.,.F.,.F.,(4,3,3,
3,3,3,3,4),(19.9722977279999,20.9588879036046,21.9569301847286,22.9549724658526,
23.9530147469767,24.9510570281007,25.9490993092247,26.2554830351795),
 .UNSPECIFIED.);
#392=B_SPLINE_CURVE_WITH_KNOTS('',3,(#14561,#14562,#14563,#14564,#14565,
#14566,#14567,#14568,#14569,#14570,#14571,#14572,#14573,#14574,#14575,#14576,
#14577,#14578,#14579,#14580,#14581,#14582),.UNSPECIFIED.,.F.,.F.,(4,3,3,
3,3,3,3,4),(-35.5079500563465,-34.9175001300792,-33.9198572692198,-32.9222144083604,
-31.924571547501,-30.9269286866416,-29.9292858257822,-29.2247647491669),
 .UNSPECIFIED.);
#393=B_SPLINE_CURVE_WITH_KNOTS('',3,(#14583,#14584,#14585,#14586,#14587,
#14588,#14589,#14590,#14591,#14592,#14593,#14594,#14595,#14596,#14597,#14598,
#14599,#14600,#14601,#14602,#14603,#14604),.UNSPECIFIED.,.F.,.F.,(4,3,3,
3,3,3,3,4),(26.2554830351795,26.9471415903487,27.9451838714728,28.9432261525968,
29.9412684337208,30.9393107148448,31.9373529959689,32.5386683423591),
 .UNSPECIFIED.);
#394=B_SPLINE_CURVE_WITH_KNOTS('',3,(#14609,#14610,#14611,#14612,#14613,
#14614,#14615,#14616,#14617,#14618,#14619,#14620,#14621,#14622,#14623,#14624,
#14625,#14626,#14627,#14628,#14629,#14630),.UNSPECIFIED.,.F.,.F.,(4,3,3,
3,3,3,3,4),(-41.791135363526,-40.9033572952357,-39.9057144343762,-38.9080715735168,
-37.9104287126574,-36.912785851798,-35.9151429909386,-35.5079500563465),
 .UNSPECIFIED.);
#395=B_SPLINE_CURVE_WITH_KNOTS('',3,(#14631,#14632,#14633,#14634,#14635,
#14636,#14637,#14638,#14639,#14640,#14641,#14642,#14643,#14644,#14645,#14646,
#14647,#14648,#14649,#14650,#14651,#14652),.UNSPECIFIED.,.F.,.F.,(4,3,3,
3,3,3,3,4),(32.5386683423591,32.9353952770929,33.9334375582169,34.931479839341,
35.929522120465,36.927564401589,37.9256066827131,38.8218536495387),
 .UNSPECIFIED.);
#396=B_SPLINE_CURVE_WITH_KNOTS('',3,(#14657,#14658,#14659,#14660,#14661,
#14662,#14663,#14664,#14665,#14666,#14667,#14668,#14669,#14670,#14671,#14672,
#14673,#14674,#14675,#14676,#14677,#14678,#14679,#14680,#14681),
 .UNSPECIFIED.,.F.,.F.,(4,3,3,3,3,3,3,3,4),(-48.0743206707056,-47.8868573212515,
-46.8892144603921,-45.8915715995327,-44.8939287386733,-43.8962858778139,
-42.8986430169545,-41.9010001560951,-41.791135363526),.UNSPECIFIED.);
#397=B_SPLINE_CURVE_WITH_KNOTS('',3,(#14682,#14683,#14684,#14685,#14686,
#14687,#14688,#14689,#14690,#14691,#14692,#14693,#14694,#14695,#14696,#14697,
#14698,#14699,#14700,#14701,#14702,#14703,#14704,#14705,#14706),
 .UNSPECIFIED.,.F.,.F.,(4,3,3,3,3,3,3,3,4),(38.8218536495387,38.9236489638371,
39.9216912449611,40.9197335260851,41.9177758072091,42.9158180883332,43.9138603694572,
44.9119026505812,45.1050389567183),.UNSPECIFIED.);
#398=B_SPLINE_CURVE_WITH_KNOTS('',3,(#14711,#14712,#14713,#14714,#14715,
#14716,#14717,#14718,#14719,#14720,#14721,#14722,#14723,#14724,#14725,#14726,
#14727,#14728,#14729,#14730,#14731,#14732),.UNSPECIFIED.,.F.,.F.,(4,3,3,
3,3,3,3,4),(-54.3575059778852,-53.8727144864079,-52.8750716255485,-51.8774287646891,
-50.8797859038297,-49.8821430429703,-48.8845001821109,-48.0743206707056),
 .UNSPECIFIED.);
#399=B_SPLINE_CURVE_WITH_KNOTS('',3,(#14733,#14734,#14735,#14736,#14737,
#14738,#14739,#14740,#14741,#14742,#14743,#14744,#14745,#14746,#14747,#14748,
#14749,#14750,#14751,#14752,#14753,#14754),.UNSPECIFIED.,.F.,.F.,(4,3,3,
3,3,3,3,4),(45.1050389567183,45.9099449317052,46.9079872128293,47.9060294939533,
48.9040717750773,49.9021140562014,50.9001563373254,51.3882242638979),
 .UNSPECIFIED.);
#400=B_SPLINE_CURVE_WITH_KNOTS('',3,(#14759,#14760,#14761,#14762,#14763,
#14764,#14765,#14766,#14767,#14768,#14769,#14770,#14771,#14772,#14773,#14774,
#14775,#14776,#14777,#14778,#14779,#14780),.UNSPECIFIED.,.F.,.F.,(4,3,3,
3,3,3,3,4),(-60.6406912850648,-59.8585716515644,-58.860928790705,-57.8632859298455,
-56.8656430689861,-55.8680002081267,-54.8703573472673,-54.3575059778852),
 .UNSPECIFIED.);
#401=B_SPLINE_CURVE_WITH_KNOTS('',3,(#14781,#14782,#14783,#14784,#14785,
#14786,#14787,#14788,#14789,#14790,#14791,#14792,#14793,#14794,#14795,#14796,
#14797,#14798,#14799,#14800,#14801,#14802),.UNSPECIFIED.,.F.,.F.,(4,3,3,
3,3,3,3,4),(51.3882242638979,51.8981986184494,52.8962408995734,53.8942831806975,
54.8923254618215,55.8903677429455,56.8884100240695,57.6714095710775),
 .UNSPECIFIED.);
#402=B_SPLINE_CURVE_WITH_KNOTS('',3,(#14807,#14808,#14809,#14810,#14811,
#14812,#14813,#14814,#14815,#14816,#14817,#14818,#14819,#14820,#14821,#14822,
#14823,#14824,#14825,#14826,#14827,#14828,#14829,#14830,#14831),
 .UNSPECIFIED.,.F.,.F.,(4,3,3,3,3,3,3,3,4),(-66.9238765922444,-66.8420716775802,
-65.8444288167208,-64.8467859558614,-63.849143095002,-62.8515002341426,
-61.8538573732832,-60.8562145124238,-60.6406912850648),.UNSPECIFIED.);
#403=B_SPLINE_CURVE_WITH_KNOTS('',3,(#14832,#14833,#14834,#14835,#14836,
#14837,#14838,#14839,#14840,#14841,#14842,#14843,#14844,#14845,#14846,#14847,
#14848,#14849,#14850,#14851,#14852,#14853,#14854,#14855,#14856),
 .UNSPECIFIED.,.F.,.F.,(4,3,3,3,3,3,3,3,4),(57.6714095710775,57.8864523051936,
58.8844945863176,59.8825368674416,60.8805791485657,61.8786214296897,62.8766637108137,
63.8747059919378,63.9545948782571),.UNSPECIFIED.);
#404=B_SPLINE_CURVE_WITH_KNOTS('',3,(#14861,#14862,#14863,#14864,#14865,
#14866,#14867,#14868,#14869,#14870,#14871,#14872,#14873,#14874,#14875,#14876,
#14877,#14878,#14879,#14880,#14881,#14882),.UNSPECIFIED.,.F.,.F.,(4,3,3,
3,3,3,3,4),(-73.207061899424,-72.8279288427366,-71.8302859818773,-70.8326431210178,
-69.8350002601584,-68.837357399299,-67.8397145384396,-66.9238765922444),
 .UNSPECIFIED.);
#405=B_SPLINE_CURVE_WITH_KNOTS('',3,(#14883,#14884,#14885,#14886,#14887,
#14888,#14889,#14890,#14891,#14892,#14893,#14894,#14895,#14896,#14897,#14898,
#14899,#14900,#14901,#14902,#14903,#14904),.UNSPECIFIED.,.F.,.F.,(4,3,3,
3,3,3,3,4),(63.9545948782571,64.8727482730618,65.8707905541858,66.8688328353098,
67.8668751164338,68.8649173975579,69.8629596786819,70.2377801854366),
 .UNSPECIFIED.);
#406=B_SPLINE_CURVE_WITH_KNOTS('',3,(#14909,#14910,#14911,#14912,#14913,
#14914,#14915,#14916,#14917,#14918,#14919,#14920,#14921,#14922,#14923,#14924,
#14925,#14926,#14927,#14928,#14929,#14930),.UNSPECIFIED.,.F.,.F.,(4,3,3,
3,3,3,3,4),(-79.4902472066036,-78.8137860078931,-77.8161431470337,-76.8185002861743,
-75.8208574253149,-74.8232145644555,-73.825571703596,-73.207061899424),
 .UNSPECIFIED.);
#407=B_SPLINE_CURVE_WITH_KNOTS('',3,(#14931,#14932,#14933,#14934,#14935,
#14936,#14937,#14938,#14939,#14940,#14941,#14942,#14943,#14944,#14945,#14946,
#14947,#14948,#14949,#14950,#14951,#14952),.UNSPECIFIED.,.F.,.F.,(4,3,3,
3,3,3,3,4),(70.2377801854366,70.8610019598059,71.85904424093,72.857086522054,
73.855128803178,74.853171084302,75.8512133654261,76.5209654926162),
 .UNSPECIFIED.);
#408=B_SPLINE_CURVE_WITH_KNOTS('',3,(#14957,#14958,#14959,#14960,#14961,
#14962,#14963,#14964,#14965,#14966,#14967,#14968,#14969,#14970,#14971,#14972,
#14973,#14974,#14975,#14976,#14977,#14978),.UNSPECIFIED.,.F.,.F.,(4,3,3,
3,3,3,3,4),(-85.7734325137832,-84.7996431730495,-83.8020003121901,-82.8043574513307,
-81.8067145904713,-80.8090717296119,-79.8114288687525,-79.4902472066036),
 .UNSPECIFIED.);
#409=B_SPLINE_CURVE_WITH_KNOTS('',3,(#14979,#14980,#14981,#14982,#14983,
#14984,#14985,#14986,#14987,#14988,#14989,#14990,#14991,#14992,#14993,#14994,
#14995,#14996,#14997,#14998,#14999,#15000),.UNSPECIFIED.,.F.,.F.,(4,3,3,
3,3,3,3,4),(76.5209654926162,76.8492556465501,77.8472979276741,78.8453402087982,
79.8433824899222,80.8414247710462,81.8394670521702,82.8041507997958),
 .UNSPECIFIED.);
#410=B_SPLINE_CURVE_WITH_KNOTS('',3,(#15005,#15006,#15007,#15008,#15009,
#15010,#15011,#15012,#15013,#15014,#15015,#15016,#15017,#15018,#15019,#15020,
#15021,#15022,#15023,#15024,#15025,#15026,#15027,#15028,#15029),
 .UNSPECIFIED.,.F.,.F.,(4,3,3,3,3,3,3,3,4),(-92.0566178209628,-91.7831431990654,
-90.7855003382059,-89.7878574773465,-88.7902146164871,-87.7925717556277,
-86.7949288947683,-85.7972860339089,-85.7734325137832),.UNSPECIFIED.);
#411=B_SPLINE_CURVE_WITH_KNOTS('',3,(#15030,#15031,#15032,#15033,#15034,
#15035,#15036,#15037,#15038,#15039,#15040,#15041,#15042,#15043,#15044,#15045,
#15046,#15047,#15048,#15049,#15050,#15051,#15052,#15053,#15054),
 .UNSPECIFIED.,.F.,.F.,(4,3,3,3,3,3,3,3,4),(82.8041507997958,82.8375093332942,
83.8355516144183,84.8335938955423,85.8316361766664,86.8296784577904,87.8277207389144,
88.8257630200384,89.0873361069754),.UNSPECIFIED.);
#412=B_SPLINE_CURVE_WITH_KNOTS('',3,(#15059,#15060,#15061,#15062,#15063,
#15064,#15065,#15066,#15067,#15068,#15069,#15070,#15071,#15072,#15073,#15074,
#15075,#15076,#15077,#15078,#15079,#15080),.UNSPECIFIED.,.F.,.F.,(4,3,3,
3,3,3,3,4),(-98.3398031281424,-97.7690003642218,-96.7713575033624,-95.773714642503,
-94.7760717816436,-93.7784289207842,-92.7807860599248,-92.0566178209628),
 .UNSPECIFIED.);
#413=B_SPLINE_CURVE_WITH_KNOTS('',3,(#15081,#15082,#15083,#15084,#15085,
#15086,#15087,#15088,#15089,#15090,#15091,#15092,#15093,#15094,#15095,#15096,
#15097,#15098,#15099,#15100,#15101,#15102),.UNSPECIFIED.,.F.,.F.,(4,3,3,
3,3,3,3,4),(89.0873361069754,89.8238053011624,90.8218475822865,91.8198898634105,
92.8179321445345,93.8159744256585,94.8140167067826,95.370521414155),
 .UNSPECIFIED.);
#414=B_SPLINE_CURVE_WITH_KNOTS('',3,(#15107,#15108,#15109,#15110,#15111,
#15112,#15113,#15114,#15115,#15116,#15117,#15118,#15119,#15120,#15121,#15122,
#15123,#15124,#15125,#15126,#15127,#15128),.UNSPECIFIED.,.F.,.F.,(4,3,3,
3,3,3,3,4),(-104.622988435322,-103.754857529378,-102.757214668519,-101.759571807659,
-100.7619289468,-99.7642860859406,-98.7666432250812,-98.3398031281424),
 .UNSPECIFIED.);
#415=B_SPLINE_CURVE_WITH_KNOTS('',3,(#15129,#15130,#15131,#15132,#15133,
#15134,#15135,#15136,#15137,#15138,#15139,#15140,#15141,#15142,#15143,#15144,
#15145,#15146,#15147,#15148,#15149,#15150),.UNSPECIFIED.,.F.,.F.,(4,3,3,
3,3,3,3,4),(95.370521414155,95.8120589879066,96.8101012690306,97.8081435501546,
98.8061858312787,99.8042281124027,100.802270393527,101.653706721335),
 .UNSPECIFIED.);
#416=B_SPLINE_CURVE_WITH_KNOTS('',3,(#15155,#15156,#15157,#15158,#15159,
#15160,#15161,#15162,#15163,#15164,#15165,#15166,#15167,#15168,#15169,#15170,
#15171,#15172,#15173,#15174,#15175,#15176,#15177,#15178,#15179),
 .UNSPECIFIED.,.F.,.F.,(4,3,3,3,3,3,3,3,4),(-110.906173742502,-110.738357555394,
-109.740714694535,-108.743071833675,-107.745428972816,-106.747786111956,
-105.750143251097,-104.752500390238,-104.622988435322),.UNSPECIFIED.);
#417=B_SPLINE_CURVE_WITH_KNOTS('',3,(#15180,#15181,#15182,#15183,#15184,
#15185,#15186,#15187,#15188,#15189,#15190,#15191,#15192,#15193,#15194,#15195,
#15196,#15197,#15198,#15199,#15200,#15201,#15202,#15203,#15204),
 .UNSPECIFIED.,.F.,.F.,(4,3,3,3,3,3,3,3,4),(101.653706721335,101.800312674651,
102.798354955775,103.796397236899,104.794439518023,105.792481799147,106.790524080271,
107.788566361395,107.936892028514),.UNSPECIFIED.);
#418=B_SPLINE_CURVE_WITH_KNOTS('',3,(#15209,#15210,#15211,#15212,#15213,
#15214,#15215,#15216,#15217,#15218,#15219,#15220,#15221,#15222,#15223,#15224,
#15225,#15226,#15227,#15228,#15229,#15230),.UNSPECIFIED.,.F.,.F.,(4,3,3,
3,3,3,3,4),(-117.189359049681,-116.724214720551,-115.726571859691,-114.728928998832,
-113.731286137972,-112.733643277113,-111.736000416253,-110.906173742502),
 .UNSPECIFIED.);
#419=B_SPLINE_CURVE_WITH_KNOTS('',3,(#15231,#15232,#15233,#15234,#15235,
#15236,#15237,#15238,#15239,#15240,#15241,#15242,#15243,#15244,#15245,#15246,
#15247,#15248,#15249,#15250,#15251,#15252),.UNSPECIFIED.,.F.,.F.,(4,3,3,
3,3,3,3,4),(107.936892028514,108.786608642519,109.784650923643,110.782693204767,
111.780735485891,112.778777767015,113.776820048139,114.220077335694),
 .UNSPECIFIED.);
#420=B_SPLINE_CURVE_WITH_KNOTS('',3,(#15257,#15258,#15259,#15260,#15261,
#15262,#15263,#15264,#15265,#15266,#15267,#15268,#15269,#15270,#15271,#15272,
#15273,#15274,#15275,#15276,#15277,#15278),.UNSPECIFIED.,.F.,.F.,(4,3,3,
3,3,3,3,4),(-123.472544356861,-122.710071885707,-121.712429024848,-120.714786163988,
-119.717143303129,-118.719500442269,-117.72185758141,-117.189359049681),
 .UNSPECIFIED.);
#421=B_SPLINE_CURVE_WITH_KNOTS('',3,(#15279,#15280,#15281,#15282,#15283,
#15284,#15285,#15286,#15287,#15288,#15289,#15290,#15291,#15292,#15293,#15294,
#15295,#15296,#15297,#15298,#15299,#15300),.UNSPECIFIED.,.F.,.F.,(4,3,3,
3,3,3,3,4),(114.220077335694,114.774862329263,115.772904610387,116.770946891511,
117.768989172635,118.767031453759,119.765073734883,120.503262642873),
 .UNSPECIFIED.);
#422=B_SPLINE_CURVE_WITH_KNOTS('',3,(#15305,#15306,#15307,#15308,#15309,
#15310,#15311,#15312,#15313,#15314,#15315,#15316,#15317,#15318,#15319,#15320,
#15321,#15322,#15323,#15324,#15325,#15326,#15327,#15328,#15329),
 .UNSPECIFIED.,.F.,.F.,(4,3,3,3,3,3,3,3,4),(-129.75572966404,-129.693571911723,
-128.695929050863,-127.698286190004,-126.700643329145,-125.703000468285,
-124.705357607426,-123.707714746566,-123.472544356861),.UNSPECIFIED.);
#423=B_SPLINE_CURVE_WITH_KNOTS('',3,(#15330,#15331,#15332,#15333,#15334,
#15335,#15336,#15337,#15338,#15339,#15340,#15341,#15342,#15343,#15344,#15345,
#15346,#15347,#15348,#15349,#15350,#15351,#15352,#15353,#15354),
 .UNSPECIFIED.,.F.,.F.,(4,3,3,3,3,3,3,3,4),(120.503262642873,120.763116016007,
121.761158297131,122.759200578255,123.757242859379,124.755285140503,125.753327421627,
126.751369702751,126.786447950053),.UNSPECIFIED.);
#424=B_SPLINE_CURVE_WITH_KNOTS('',3,(#15359,#15360,#15361,#15362,#15363,
#15364,#15365,#15366,#15367,#15368,#15369,#15370,#15371,#15372,#15373,#15374,
#15375,#15376,#15377,#15378,#15379,#15380),.UNSPECIFIED.,.F.,.F.,(4,3,3,
3,3,3,3,4),(-136.03891497122,-135.679429076879,-134.68178621602,-133.68414335516,
-132.686500494301,-131.688857633442,-130.691214772582,-129.75572966404),
 .UNSPECIFIED.);
#425=B_SPLINE_CURVE_WITH_KNOTS('',3,(#15381,#15382,#15383,#15384,#15385,
#15386,#15387,#15388,#15389,#15390,#15391,#15392,#15393,#15394,#15395,#15396,
#15397,#15398,#15399,#15400,#15401,#15402),.UNSPECIFIED.,.F.,.F.,(4,3,3,
3,3,3,3,4),(126.786447950053,127.749411983875,128.747454265,129.745496546124,
130.743538827248,131.741581108372,132.739623389496,133.069633257233),
 .UNSPECIFIED.);
#426=B_SPLINE_CURVE_WITH_KNOTS('',3,(#15407,#15408,#15409,#15410,#15411,
#15412,#15413,#15414,#15415,#15416,#15417,#15418,#15419,#15420,#15421,#15422,
#15423,#15424,#15425,#15426,#15427,#15428),.UNSPECIFIED.,.F.,.F.,(4,3,3,
3,3,3,3,4),(-142.322100278399,-141.665286242036,-140.667643381176,-139.670000520317,
-138.672357659457,-137.674714798598,-136.677071937739,-136.03891497122),
 .UNSPECIFIED.);
#427=B_SPLINE_CURVE_WITH_KNOTS('',3,(#15429,#15430,#15431,#15432,#15433,
#15434,#15435,#15436,#15437,#15438,#15439,#15440,#15441,#15442,#15443,#15444,
#15445,#15446,#15447,#15448,#15449,#15450),.UNSPECIFIED.,.F.,.F.,(4,3,3,
3,3,3,3,4),(133.069633257233,133.73766567062,134.735707951744,135.733750232868,
136.731792513992,137.729834795116,138.72787707624,139.352818564412),
 .UNSPECIFIED.);
#428=B_SPLINE_CURVE_WITH_KNOTS('',3,(#15455,#15456,#15457,#15458,#15459,
#15460,#15461,#15462,#15463,#15464,#15465,#15466,#15467,#15468,#15469,#15470,
#15471,#15472,#15473,#15474,#15475,#15476),.UNSPECIFIED.,.F.,.F.,(4,3,3,
3,3,3,3,4),(-148.605285585579,-147.651143407192,-146.653500546333,-145.655857685473,
-144.658214824614,-143.660571963754,-142.662929102895,-142.322100278399),
 .UNSPECIFIED.);
#429=B_SPLINE_CURVE_WITH_KNOTS('',3,(#15477,#15478,#15479,#15480,#15481,
#15482,#15483,#15484,#15485,#15486,#15487,#15488,#15489,#15490,#15491,#15492,
#15493,#15494,#15495,#15496,#15497,#15498),.UNSPECIFIED.,.F.,.F.,(4,3,3,
3,3,3,3,4),(139.352818564412,139.725919357364,140.723961638488,141.722003919612,
142.720046200736,143.71808848186,144.716130762984,145.636003871592),
 .UNSPECIFIED.);
#430=B_SPLINE_CURVE_WITH_KNOTS('',3,(#15503,#15504,#15505,#15506,#15507,
#15508,#15509,#15510,#15511,#15512,#15513,#15514,#15515,#15516,#15517,#15518,
#15519,#15520,#15521,#15522,#15523,#15524,#15525,#15526,#15527),
 .UNSPECIFIED.,.F.,.F.,(4,3,3,3,3,3,3,3,4),(-154.888470892759,-154.634643433208,
-153.637000572349,-152.639357711489,-151.64171485063,-150.64407198977,-149.646429128911,
-148.648786268052,-148.605285585579),.UNSPECIFIED.);
#431=B_SPLINE_CURVE_WITH_KNOTS('',3,(#15528,#15529,#15530,#15531,#15532,
#15533,#15534,#15535,#15536,#15537,#15538,#15539,#15540,#15541,#15542,#15543,
#15544,#15545,#15546,#15547,#15548,#15549,#15550,#15551,#15552),
 .UNSPECIFIED.,.F.,.F.,(4,3,3,3,3,3,3,3,4),(145.636003871592,145.714173044108,
146.712215325232,147.710257606356,148.70829988748,149.706342168604,150.704384449728,
151.702426730852,151.919189178771),.UNSPECIFIED.);
#432=B_SPLINE_CURVE_WITH_KNOTS('',3,(#15557,#15558,#15559,#15560,#15561,
#15562,#15563,#15564,#15565,#15566,#15567,#15568,#15569,#15570,#15571,#15572,
#15573,#15574,#15575,#15576,#15577,#15578),.UNSPECIFIED.,.F.,.F.,(4,3,3,
3,3,3,3,4),(-161.171656199938,-160.620500598364,-159.622857737505,-158.625214876646,
-157.627572015786,-156.629929154927,-155.632286294067,-154.888470892759),
 .UNSPECIFIED.);
#433=B_SPLINE_CURVE_WITH_KNOTS('',3,(#15579,#15580,#15581,#15582,#15583,
#15584,#15585,#15586,#15587,#15588,#15589,#15590,#15591,#15592,#15593,#15594,
#15595,#15596,#15597,#15598,#15599,#15600),.UNSPECIFIED.,.F.,.F.,(4,3,3,
3,3,3,3,4),(151.919189178771,152.700469011976,153.6985112931,154.696553574224,
155.694595855348,156.692638136472,157.690680417596,158.202374485951),
 .UNSPECIFIED.);
#434=B_SPLINE_CURVE_WITH_KNOTS('',3,(#15605,#15606,#15607,#15608,#15609,
#15610,#15611,#15612,#15613,#15614,#15615,#15616,#15617,#15618,#15619,#15620,
#15621,#15622,#15623,#15624,#15625,#15626),.UNSPECIFIED.,.F.,.F.,(4,3,3,
3,3,3,3,4),(-167.454841507118,-166.606357763521,-165.608714902661,-164.611072041802,
-163.613429180943,-162.615786320083,-161.618143459224,-161.171656199938),
 .UNSPECIFIED.);
#435=B_SPLINE_CURVE_WITH_KNOTS('',3,(#15627,#15628,#15629,#15630,#15631,
#15632,#15633,#15634,#15635,#15636,#15637,#15638,#15639,#15640,#15641,#15642,
#15643,#15644,#15645,#15646,#15647,#15648),.UNSPECIFIED.,.F.,.F.,(4,3,3,
3,3,3,3,4),(158.202374485951,158.68872269872,159.686764979844,160.684807260968,
161.682849542092,162.680891823216,163.67893410434,164.48555979313),
 .UNSPECIFIED.);
#436=B_SPLINE_CURVE_WITH_KNOTS('',3,(#15653,#15654,#15655,#15656,#15657,
#15658,#15659,#15660,#15661,#15662,#15663,#15664,#15665,#15666,#15667,#15668,
#15669,#15670,#15671,#15672,#15673,#15674,#15675,#15676,#15677),
 .UNSPECIFIED.,.F.,.F.,(4,3,3,3,3,3,3,3,4),(-173.738026814297,-173.589857789537,
-172.592214928677,-171.594572067818,-170.596929206958,-169.599286346099,
-168.60164348524,-167.60400062438,-167.454841507118),.UNSPECIFIED.);
#437=B_SPLINE_CURVE_WITH_KNOTS('',3,(#15678,#15679,#15680,#15681,#15682,
#15683,#15684,#15685,#15686,#15687,#15688,#15689,#15690,#15691,#15692,#15693,
#15694,#15695,#15696,#15697,#15698,#15699,#15700,#15701,#15702),
 .UNSPECIFIED.,.F.,.F.,(4,3,3,3,3,3,3,3,4),(164.48555979313,164.676976385465,
165.675018666588,166.673060947713,167.671103228837,168.669145509961,169.667187791085,
170.665230072209,170.76874510031),.UNSPECIFIED.);
#438=B_SPLINE_CURVE_WITH_KNOTS('',3,(#15707,#15708,#15709,#15710,#15711,
#15712,#15713,#15714,#15715,#15716,#15717,#15718,#15719,#15720,#15721,#15722,
#15723,#15724,#15725,#15726,#15727,#15728),.UNSPECIFIED.,.F.,.F.,(4,3,3,
3,3,3,3,4),(-180.021212121477,-179.575714954693,-178.578072093834,-177.580429232974,
-176.582786372115,-175.585143511255,-174.587500650396,-173.738026814297),
 .UNSPECIFIED.);
#439=B_SPLINE_CURVE_WITH_KNOTS('',3,(#15729,#15730,#15731,#15732,#15733,
#15734,#15735,#15736,#15737,#15738,#15739,#15740,#15741,#15742,#15743,#15744,
#15745,#15746,#15747,#15748,#15749,#15750),.UNSPECIFIED.,.F.,.F.,(4,3,3,
3,3,3,3,4),(170.76874510031,171.663272353333,172.661314634457,173.659356915581,
174.657399196705,175.655441477829,176.653483758953,177.051930407489),
 .UNSPECIFIED.);
#440=B_SPLINE_CURVE_WITH_KNOTS('',3,(#15755,#15756,#15757,#15758,#15759,
#15760,#15761,#15762,#15763,#15764,#15765,#15766,#15767,#15768,#15769,#15770,
#15771,#15772,#15773,#15774,#15775,#15776),.UNSPECIFIED.,.F.,.F.,(4,3,3,
3,3,3,3,4),(-186.304397428656,-185.56157211985,-184.56392925899,-183.566286398131,
-182.568643537271,-181.571000676412,-180.573357815553,-180.021212121477),
 .UNSPECIFIED.);
#441=B_SPLINE_CURVE_WITH_KNOTS('',3,(#15777,#15778,#15779,#15780,#15781,
#15782,#15783,#15784,#15785,#15786,#15787,#15788,#15789,#15790,#15791,#15792,
#15793,#15794,#15795,#15796,#15797,#15798),.UNSPECIFIED.,.F.,.F.,(4,3,3,
3,3,3,3,4),(177.051930407489,177.651526040077,178.649568321201,179.647610602325,
180.645652883449,181.643695164573,182.641737445697,183.335115714669),
 .UNSPECIFIED.);
#442=B_SPLINE_CURVE_WITH_KNOTS('',3,(#15804,#15805,#15806,#15807,#15808,
#15809,#15810,#15811,#15812,#15813),.UNSPECIFIED.,.F.,.F.,(4,1,1,1,1,1,
1,4),(197.920337176157,198.17515472821,199.172797589069,200.170440449928,
201.168083310788,202.165726171647,203.163369032507,204.161011893366),
 .UNSPECIFIED.);
#443=B_SPLINE_CURVE_WITH_KNOTS('',3,(#15816,#15817,#15818,#15819,#15820,
#15821,#15822,#15823,#15824),.UNSPECIFIED.,.F.,.F.,(4,1,1,1,1,1,4),(197.920337176157,
197.930069567874,198.928111848998,199.926154130122,200.924196411246,201.92223869237,
202.920280973494),.UNSPECIFIED.);
#444=B_SPLINE_CURVE_WITH_KNOTS('',3,(#15829,#15830,#15831,#15832,#15833,
#15834,#15835,#15836,#15837,#15838),.UNSPECIFIED.,.F.,.F.,(4,1,1,1,1,1,
1,4),(191.637151868977,192.189297563053,193.186940423913,194.184583284772,
195.182226145631,196.179869006491,197.17751186735,197.920337176157),
 .UNSPECIFIED.);
#445=B_SPLINE_CURVE_WITH_KNOTS('',3,(#15839,#15840,#15841,#15842,#15843,
#15844,#15845,#15846,#15847,#15848),.UNSPECIFIED.,.F.,.F.,(4,1,1,1,1,1,
1,4),(191.637151868977,191.94181588113,192.939858162254,193.937900443378,
194.935942724502,195.933985005626,196.93202728675,197.920337176157),
 .UNSPECIFIED.);
#446=B_SPLINE_CURVE_WITH_KNOTS('',3,(#15853,#15854,#15855,#15856,#15857,
#15858,#15859,#15860,#15861,#15862),.UNSPECIFIED.,.F.,.F.,(4,1,1,1,1,1,
1,4),(185.353966561798,186.203440397897,187.201083258756,188.198726119616,
189.196368980475,190.194011841334,191.191654702194,191.637151868977),
 .UNSPECIFIED.);
#447=B_SPLINE_CURVE_WITH_KNOTS('',3,(#15863,#15864,#15865,#15866,#15867,
#15868,#15869,#15870,#15871,#15872),.UNSPECIFIED.,.F.,.F.,(4,1,1,1,1,1,
1,4),(185.353966561798,185.953562194385,186.951604475509,187.949646756633,
188.947689037757,189.945731318881,190.943773600006,191.637151868977),
 .UNSPECIFIED.);
#448=B_SPLINE_CURVE_WITH_KNOTS('',3,(#15877,#15878,#15879,#15880,#15881,
#15882,#15883,#15884,#15885,#15886,#15887),.UNSPECIFIED.,.F.,.F.,(4,1,1,
1,1,1,1,1,4),(179.070781254618,179.219940371881,180.21758323274,181.2152260936,
182.212868954459,183.210511815318,184.208154676178,185.205797537037,185.353966561798),
 .UNSPECIFIED.);
#449=B_SPLINE_CURVE_WITH_KNOTS('',3,(#15888,#15889,#15890,#15891,#15892,
#15893,#15894,#15895,#15896,#15897),.UNSPECIFIED.,.F.,.F.,(4,1,1,1,1,1,
1,4),(179.070781254618,179.965308507641,180.963350788765,181.961393069889,
182.959435351013,183.957477632137,184.955519913261,185.353966561798),
 .UNSPECIFIED.);
#450=B_SPLINE_CURVE_WITH_KNOTS('',3,(#15902,#15903,#15904,#15905,#15906,
#15907,#15908,#15909,#15910,#15911),.UNSPECIFIED.,.F.,.F.,(4,1,1,1,1,1,
1,4),(172.787595947439,173.234083206724,174.231726067584,175.229368928443,
176.227011789303,177.224654650162,178.222297511021,179.070781254618),
 .UNSPECIFIED.);
#451=B_SPLINE_CURVE_WITH_KNOTS('',3,(#15912,#15913,#15914,#15915,#15916,
#15917,#15918,#15919,#15920,#15921,#15922),.UNSPECIFIED.,.F.,.F.,(4,1,1,
1,1,1,1,1,4),(172.787595947439,172.979012539773,173.977054820897,174.975097102021,
175.973139383145,176.971181664269,177.969223945393,178.967266226517,179.070781254618),
 .UNSPECIFIED.);
#452=B_SPLINE_CURVE_WITH_KNOTS('',3,(#15927,#15928,#15929,#15930,#15931,
#15932,#15933,#15934,#15935,#15936),.UNSPECIFIED.,.F.,.F.,(4,1,1,1,1,1,
1,4),(166.504410640259,167.248226041568,168.245868902427,169.243511763287,
170.241154624146,171.238797485006,172.236440345865,172.787595947439),
 .UNSPECIFIED.);
#453=B_SPLINE_CURVE_WITH_KNOTS('',3,(#15937,#15938,#15939,#15940,#15941,
#15942,#15943,#15944,#15945,#15946),.UNSPECIFIED.,.F.,.F.,(4,1,1,1,1,1,
1,4),(166.504410640259,166.990758853029,167.988801134153,168.986843415277,
169.984885696401,170.982927977525,171.980970258649,172.787595947439),
 .UNSPECIFIED.);
#454=B_SPLINE_CURVE_WITH_KNOTS('',3,(#15951,#15952,#15953,#15954,#15955,
#15956,#15957,#15958,#15959,#15960,#15961),.UNSPECIFIED.,.F.,.F.,(4,1,1,
1,1,1,1,1,4),(160.22122533308,160.264726015552,161.262368876412,162.260011737271,
163.25765459813,164.25529745899,165.252940319849,166.250583180709,166.504410640259),
 .UNSPECIFIED.);
#455=B_SPLINE_CURVE_WITH_KNOTS('',3,(#15962,#15963,#15964,#15965,#15966,
#15967,#15968,#15969,#15970,#15971),.UNSPECIFIED.,.F.,.F.,(4,1,1,1,1,1,
1,4),(160.22122533308,161.002505166285,162.000547447409,162.998589728533,
163.996632009657,164.994674290781,165.992716571905,166.504410640259),
 .UNSPECIFIED.);
#456=B_SPLINE_CURVE_WITH_KNOTS('',3,(#15976,#15977,#15978,#15979,#15980,
#15981,#15982,#15983,#15984,#15985),.UNSPECIFIED.,.F.,.F.,(4,1,1,1,1,1,
1,4),(153.9380400259,154.278868850396,155.276511711255,156.274154572115,
157.271797432974,158.269440293833,159.267083154693,160.22122533308),
 .UNSPECIFIED.);
#457=B_SPLINE_CURVE_WITH_KNOTS('',3,(#15986,#15987,#15988,#15989,#15990,
#15991,#15992,#15993,#15994,#15995,#15996),.UNSPECIFIED.,.F.,.F.,(4,1,1,
1,1,1,1,1,4),(153.9380400259,154.016209198417,155.014251479541,156.012293760665,
157.010336041789,158.008378322913,159.006420604037,160.004462885161,160.22122533308),
 .UNSPECIFIED.);
#458=B_SPLINE_CURVE_WITH_KNOTS('',3,(#16001,#16002,#16003,#16004,#16005,
#16006,#16007,#16008,#16009,#16010),.UNSPECIFIED.,.F.,.F.,(4,1,1,1,1,1,
1,4),(147.65485471872,148.293011685239,149.290654546099,150.288297406958,
151.285940267817,152.283583128677,153.281225989536,153.9380400259),
 .UNSPECIFIED.);
#459=B_SPLINE_CURVE_WITH_KNOTS('',3,(#16011,#16012,#16013,#16014,#16015,
#16016,#16017,#16018,#16019,#16020),.UNSPECIFIED.,.F.,.F.,(4,1,1,1,1,1,
1,4),(147.65485471872,148.027955511672,149.025997792796,150.02404007392,
151.022082355044,152.020124636168,153.018166917292,153.9380400259),
 .UNSPECIFIED.);
#460=B_SPLINE_CURVE_WITH_KNOTS('',3,(#16025,#16026,#16027,#16028,#16029,
#16030,#16031,#16032,#16033,#16034),.UNSPECIFIED.,.F.,.F.,(4,1,1,1,1,1,
1,4),(141.371669411541,142.307154520083,143.304797380942,144.302440241802,
145.300083102661,146.29772596352,147.29536882438,147.65485471872),
 .UNSPECIFIED.);
#461=B_SPLINE_CURVE_WITH_KNOTS('',3,(#16035,#16036,#16037,#16038,#16039,
#16040,#16041,#16042,#16043,#16044),.UNSPECIFIED.,.F.,.F.,(4,1,1,1,1,1,
1,4),(141.371669411541,142.039701824928,143.037744106052,144.035786387176,
145.0338286683,146.031870949424,147.029913230548,147.65485471872),
 .UNSPECIFIED.);
#462=B_SPLINE_CURVE_WITH_KNOTS('',3,(#16049,#16050,#16051,#16052,#16053,
#16054,#16055,#16056,#16057,#16058,#16059),.UNSPECIFIED.,.F.,.F.,(4,1,1,
1,1,1,1,1,4),(135.088484104361,135.323654494067,136.321297354926,137.318940215786,
138.316583076645,139.314225937505,140.311868798364,141.309511659223,141.371669411541),
 .UNSPECIFIED.);
#463=B_SPLINE_CURVE_WITH_KNOTS('',3,(#16060,#16061,#16062,#16063,#16064,
#16065,#16066,#16067,#16068,#16069),.UNSPECIFIED.,.F.,.F.,(4,1,1,1,1,1,
1,4),(135.088484104361,136.051448138184,137.049490419308,138.047532700432,
139.045574981556,140.04361726268,141.041659543804,141.371669411541),
 .UNSPECIFIED.);
#464=B_SPLINE_CURVE_WITH_KNOTS('',3,(#16074,#16075,#16076,#16077,#16078,
#16079,#16080,#16081,#16082,#16083),.UNSPECIFIED.,.F.,.F.,(4,1,1,1,1,1,
1,4),(128.805298797182,129.337797328911,130.33544018977,131.333083050629,
132.330725911489,133.328368772348,134.326011633208,135.088484104361),
 .UNSPECIFIED.);
#465=B_SPLINE_CURVE_WITH_KNOTS('',3,(#16084,#16085,#16086,#16087,#16088,
#16089,#16090,#16091,#16092,#16093,#16094),.UNSPECIFIED.,.F.,.F.,(4,1,1,
1,1,1,1,1,4),(128.805298797182,129.065152170316,130.06319445144,131.061236732564,
132.059279013688,133.057321294812,134.055363575936,135.05340585706,135.088484104361),
 .UNSPECIFIED.);
#466=B_SPLINE_CURVE_WITH_KNOTS('',3,(#16099,#16100,#16101,#16102,#16103,
#16104,#16105,#16106,#16107,#16108),.UNSPECIFIED.,.F.,.F.,(4,1,1,1,1,1,
1,4),(122.522113490002,123.351940163754,124.349583024614,125.347225885473,
126.344868746332,127.342511607192,128.340154468051,128.805298797182),
 .UNSPECIFIED.);
#467=B_SPLINE_CURVE_WITH_KNOTS('',3,(#16109,#16110,#16111,#16112,#16113,
#16114,#16115,#16116,#16117,#16118),.UNSPECIFIED.,.F.,.F.,(4,1,1,1,1,1,
1,4),(122.522113490002,123.076898483572,124.074940764696,125.07298304582,
126.071025326944,127.069067608068,128.067109889192,128.805298797182),
 .UNSPECIFIED.);
#468=B_SPLINE_CURVE_WITH_KNOTS('',3,(#16123,#16124,#16125,#16126,#16127,
#16128,#16129,#16130,#16131,#16132,#16133),.UNSPECIFIED.,.F.,.F.,(4,1,1,
1,1,1,1,1,4),(116.238928182823,116.368440137738,117.366082998598,118.363725859457,
119.361368720316,120.359011581176,121.356654442035,122.354297302895,122.522113490002),
 .UNSPECIFIED.);
#469=B_SPLINE_CURVE_WITH_KNOTS('',3,(#16134,#16135,#16136,#16137,#16138,
#16139,#16140,#16141,#16142,#16143),.UNSPECIFIED.,.F.,.F.,(4,1,1,1,1,1,
1,4),(116.238928182823,117.088644796828,118.086687077952,119.084729359076,
120.0827716402,121.080813921324,122.078856202448,122.522113490002),
 .UNSPECIFIED.);
#470=B_SPLINE_CURVE_WITH_KNOTS('',3,(#16148,#16149,#16150,#16151,#16152,
#16153,#16154,#16155,#16156,#16157),.UNSPECIFIED.,.F.,.F.,(4,1,1,1,1,1,
1,4),(109.955742875643,110.382582972582,111.380225833441,112.377868694301,
113.37551155516,114.373154416019,115.370797276879,116.238928182823),
 .UNSPECIFIED.);
#471=B_SPLINE_CURVE_WITH_KNOTS('',3,(#16158,#16159,#16160,#16161,#16162,
#16163,#16164,#16165,#16166,#16167,#16168),.UNSPECIFIED.,.F.,.F.,(4,1,1,
1,1,1,1,1,4),(109.955742875643,110.102348828959,111.100391110083,112.098433391207,
113.096475672331,114.094517953455,115.092560234579,116.090602515703,116.238928182823),
 .UNSPECIFIED.);
#472=B_SPLINE_CURVE_WITH_KNOTS('',3,(#16173,#16174,#16175,#16176,#16177,
#16178,#16179,#16180,#16181,#16182),.UNSPECIFIED.,.F.,.F.,(4,1,1,1,1,1,
1,4),(103.672557568463,104.396725807425,105.394368668285,106.392011529144,
107.389654390004,108.387297250863,109.384940111722,109.955742875643),
 .UNSPECIFIED.);
#473=B_SPLINE_CURVE_WITH_KNOTS('',3,(#16183,#16184,#16185,#16186,#16187,
#16188,#16189,#16190,#16191,#16192),.UNSPECIFIED.,.F.,.F.,(4,1,1,1,1,1,
1,4),(103.672557568463,104.114095142215,105.112137423339,106.110179704463,
107.108221985587,108.106264266711,109.104306547835,109.955742875643),
 .UNSPECIFIED.);
#474=B_SPLINE_CURVE_WITH_KNOTS('',3,(#16197,#16198,#16199,#16200,#16201,
#16202,#16203,#16204,#16205,#16206,#16207),.UNSPECIFIED.,.F.,.F.,(4,1,1,
1,1,1,1,1,4),(97.3893722612837,97.4132257814096,98.410868642269,99.4085115031284,
100.406154363988,101.403797224847,102.401440085707,103.399082946566,103.672557568463),
 .UNSPECIFIED.);
#475=B_SPLINE_CURVE_WITH_KNOTS('',3,(#16208,#16209,#16210,#16211,#16212,
#16213,#16214,#16215,#16216,#16217),.UNSPECIFIED.,.F.,.F.,(4,1,1,1,1,1,
1,4),(97.3893722612838,98.125841455471,99.123883736595,100.121926017719,
101.119968298843,102.118010579967,103.116052861091,103.672557568463),
 .UNSPECIFIED.);
#476=B_SPLINE_CURVE_WITH_KNOTS('',3,(#16222,#16223,#16224,#16225,#16226,
#16227,#16228,#16229,#16230,#16231),.UNSPECIFIED.,.F.,.F.,(4,1,1,1,1,1,
1,4),(91.1061869541041,91.4273686162531,92.4250114771125,93.4226543379719,
94.4202971988313,95.4179400596907,96.4155829205502,97.3893722612837),
 .UNSPECIFIED.);
#477=B_SPLINE_CURVE_WITH_KNOTS('',3,(#16232,#16233,#16234,#16235,#16236,
#16237,#16238,#16239,#16240,#16241,#16242),.UNSPECIFIED.,.F.,.F.,(4,1,1,
1,1,1,1,1,4),(91.1061869541042,91.1395454876028,92.1375877687268,93.1356300498508,
94.1336723309749,95.1317146120989,96.1297568932229,97.127799174347,97.3893722612838),
 .UNSPECIFIED.);
#478=B_SPLINE_CURVE_WITH_KNOTS('',3,(#16247,#16248,#16249,#16250,#16251,
#16252,#16253,#16254,#16255,#16256),.UNSPECIFIED.,.F.,.F.,(4,1,1,1,1,1,
1,4),(84.8230016469245,85.4415114510967,86.4391543119561,87.4367971728155,
88.4344400336749,89.4320828945343,90.4297257553937,91.1061869541041),
 .UNSPECIFIED.);
#479=B_SPLINE_CURVE_WITH_KNOTS('',3,(#16257,#16258,#16259,#16260,#16261,
#16262,#16263,#16264,#16265,#16266),.UNSPECIFIED.,.F.,.F.,(4,1,1,1,1,1,
1,4),(84.8230016469246,85.1512918008586,86.1493340819827,87.1473763631067,
88.1454186442307,89.1434609253548,90.1415032064788,91.1061869541042),
 .UNSPECIFIED.);
#480=B_SPLINE_CURVE_WITH_KNOTS('',3,(#16271,#16272,#16273,#16274,#16275,
#16276,#16277,#16278,#16279,#16280),.UNSPECIFIED.,.F.,.F.,(4,1,1,1,1,1,
1,4),(78.539816339745,79.4556542859402,80.4532971467996,81.4509400076591,
82.4485828685185,83.4462257293779,84.4438685902373,84.8230016469245),
 .UNSPECIFIED.);
#481=B_SPLINE_CURVE_WITH_KNOTS('',3,(#16281,#16282,#16283,#16284,#16285,
#16286,#16287,#16288,#16289,#16290),.UNSPECIFIED.,.F.,.F.,(4,1,1,1,1,1,
1,4),(78.539816339745,79.1630381141145,80.1610803952385,81.1591226763625,
82.1571649574865,83.1552072386106,84.1532495197346,84.8230016469246),
 .UNSPECIFIED.);
#482=B_SPLINE_CURVE_WITH_KNOTS('',3,(#16295,#16296,#16297,#16298,#16299,
#16300,#16301,#16302,#16303,#16304,#16305),.UNSPECIFIED.,.F.,.F.,(4,1,1,
1,1,1,1,1,4),(72.2566310325654,72.4721542599244,73.4697971207838,74.4674399816432,
75.4650828425026,76.462725703362,77.4603685642214,78.4580114250808,78.539816339745),
 .UNSPECIFIED.);
#483=B_SPLINE_CURVE_WITH_KNOTS('',3,(#16306,#16307,#16308,#16309,#16310,
#16311,#16312,#16313,#16314,#16315),.UNSPECIFIED.,.F.,.F.,(4,1,1,1,1,1,
1,4),(72.2566310325654,73.1747844273703,74.1728267084943,75.1708689896184,
76.1689112707424,77.1669535518664,78.1649958329905,78.539816339745),
 .UNSPECIFIED.);
#484=B_SPLINE_CURVE_WITH_KNOTS('',3,(#16320,#16321,#16322,#16323,#16324,
#16325,#16326,#16327,#16328,#16329),.UNSPECIFIED.,.F.,.F.,(4,1,1,1,1,1,
1,4),(65.9734457253858,66.486297094768,67.4839399556274,68.4815828164868,
69.4792256773462,70.4768685382056,71.474511399065,72.2566310325654),
 .UNSPECIFIED.);
#485=B_SPLINE_CURVE_WITH_KNOTS('',3,(#16330,#16331,#16332,#16333,#16334,
#16335,#16336,#16337,#16338,#16339,#16340),.UNSPECIFIED.,.F.,.F.,(4,1,1,
1,1,1,1,1,4),(65.9734457253858,66.1884884595021,67.1865307406262,68.1845730217502,
69.1826153028742,70.1806575839982,71.1786998651223,72.1767421462463,72.2566310325654),
 .UNSPECIFIED.);
#486=B_SPLINE_CURVE_WITH_KNOTS('',3,(#16345,#16346,#16347,#16348,#16349,
#16350,#16351,#16352,#16353,#16354),.UNSPECIFIED.,.F.,.F.,(4,1,1,1,1,1,
1,4),(59.6902604182062,60.5004399296115,61.4980827904709,62.4957256513303,
63.4933685121897,64.4910113730492,65.4886542339086,65.9734457253858),
 .UNSPECIFIED.);
#487=B_SPLINE_CURVE_WITH_KNOTS('',3,(#16355,#16356,#16357,#16358,#16359,
#16360,#16361,#16362,#16363,#16364),.UNSPECIFIED.,.F.,.F.,(4,1,1,1,1,1,
1,4),(59.6902604182062,60.200234772758,61.198277053882,62.196319335006,
63.19436161613,64.1924038972541,65.1904461783781,65.9734457253858),
 .UNSPECIFIED.);
#488=B_SPLINE_CURVE_WITH_KNOTS('',3,(#16369,#16370,#16371,#16372,#16373,
#16374,#16375,#16376,#16377,#16378,#16379),.UNSPECIFIED.,.F.,.F.,(4,1,1,
1,1,1,1,1,4),(53.4070751110266,53.5169399035957,54.5145827644551,55.5122256253145,
56.5098684861739,57.5075113470333,58.5051542078927,59.5027970687521,59.6902604182062),
 .UNSPECIFIED.);
#489=B_SPLINE_CURVE_WITH_KNOTS('',3,(#16380,#16381,#16382,#16383,#16384,
#16385,#16386,#16387,#16388,#16389),.UNSPECIFIED.,.F.,.F.,(4,1,1,1,1,1,
1,4),(53.4070751110266,54.2119810860138,55.2100233671378,56.2080656482619,
57.2061079293859,58.2041502105099,59.2021924916339,59.6902604182062),
 .UNSPECIFIED.);
#490=B_SPLINE_CURVE_WITH_KNOTS('',3,(#16394,#16395,#16396,#16397,#16398,
#16399,#16400,#16401,#16402,#16403),.UNSPECIFIED.,.F.,.F.,(4,1,1,1,1,1,
1,4),(47.123889803847,47.5310827384393,48.5287255992987,49.5263684601581,
50.5240113210175,51.5216541818769,52.5192970427363,53.4070751110266),
 .UNSPECIFIED.);
#491=B_SPLINE_CURVE_WITH_KNOTS('',3,(#16404,#16405,#16406,#16407,#16408,
#16409,#16410,#16411,#16412,#16413,#16414),.UNSPECIFIED.,.F.,.F.,(4,1,1,
1,1,1,1,1,4),(47.123889803847,47.2256851181456,48.2237273992696,49.2217696803937,
50.2198119615177,51.2178542426417,52.2158965237657,53.2139388048898,53.4070751110266),
 .UNSPECIFIED.);
#492=B_SPLINE_CURVE_WITH_KNOTS('',3,(#16419,#16420,#16421,#16422,#16423,
#16424,#16425,#16426,#16427,#16428),.UNSPECIFIED.,.F.,.F.,(4,1,1,1,1,1,
1,4),(40.8407044966674,41.5452255732828,42.5428684341422,43.5405112950016,
44.538154155861,45.5357970167204,46.5334398775799,47.123889803847),
 .UNSPECIFIED.);
#493=B_SPLINE_CURVE_WITH_KNOTS('',3,(#16429,#16430,#16431,#16432,#16433,
#16434,#16435,#16436,#16437,#16438),.UNSPECIFIED.,.F.,.F.,(4,1,1,1,1,1,
1,4),(40.8407044966675,41.2374314314014,42.2354737125255,43.2335159936495,
44.2315582747735,45.2296005558975,46.2276428370216,47.123889803847),
 .UNSPECIFIED.);
#494=B_SPLINE_CURVE_WITH_KNOTS('',3,(#16443,#16444,#16445,#16446,#16447,
#16448,#16449,#16450,#16451,#16452,#16453),.UNSPECIFIED.,.F.,.F.,(4,1,1,
1,1,1,1,1,4),(34.5575191894878,34.561725547267,35.5593684081264,36.5570112689858,
37.5546541298452,38.5522969907046,39.549939851564,40.5475827124234,40.8407044966674),
 .UNSPECIFIED.);
#495=B_SPLINE_CURVE_WITH_KNOTS('',3,(#16454,#16455,#16456,#16457,#16458,
#16459,#16460,#16461,#16462,#16463),.UNSPECIFIED.,.F.,.F.,(4,1,1,1,1,1,
1,4),(34.5575191894879,35.2491777446573,36.2472200257813,37.2452623069053,
38.2433045880294,39.2413468691534,40.2393891502774,40.8407044966675),
 .UNSPECIFIED.);
#496=B_SPLINE_CURVE_WITH_KNOTS('',3,(#16468,#16469,#16470,#16471,#16472,
#16473,#16474,#16475,#16476,#16477),.UNSPECIFIED.,.F.,.F.,(4,1,1,1,1,1,
1,4),(28.2743338823082,28.5758683821105,29.5735112429699,30.5711541038294,
31.5687969646888,32.5664398255482,33.5640826864076,34.5575191894878),
 .UNSPECIFIED.);
#497=B_SPLINE_CURVE_WITH_KNOTS('',3,(#16478,#16479,#16480,#16481,#16482,
#16483,#16484,#16485,#16486,#16487),.UNSPECIFIED.,.F.,.F.,(4,1,1,1,1,1,
1,4),(28.2743338823083,29.2609240579131,30.2589663390371,31.2570086201612,
32.2550509012852,33.2530931824092,34.2511354635333,34.5575191894879),
 .UNSPECIFIED.);
#498=B_SPLINE_CURVE_WITH_KNOTS('',3,(#16492,#16493,#16494,#16495,#16496,
#16497,#16498,#16499,#16500,#16501),.UNSPECIFIED.,.F.,.F.,(4,1,1,1,1,1,
1,4),(21.9911485751286,22.5900112169541,23.5876540778135,24.5852969386729,
25.5829397995323,26.5805826603917,27.5782255212511,28.2743338823082),
 .UNSPECIFIED.);
#499=B_SPLINE_CURVE_WITH_KNOTS('',3,(#16502,#16503,#16504,#16505,#16506,
#16507,#16508,#16509,#16510,#16511,#16512),.UNSPECIFIED.,.F.,.F.,(4,1,1,
1,1,1,1,1,4),(21.9911485751287,22.2746280900449,23.272670371169,24.270712652293,
25.268754933417,26.266797214541,27.2648394956651,28.2628817767891,28.2743338823083),
 .UNSPECIFIED.);
#500=B_SPLINE_CURVE_WITH_KNOTS('',3,(#16517,#16518,#16519,#16520,#16521,
#16522,#16523,#16524,#16525,#16526),.UNSPECIFIED.,.F.,.F.,(4,1,1,1,1,1,
1,4),(15.707963267949,16.6041540517977,17.6017969126571,18.5994397735165,
19.5970826343759,20.5947254952353,21.5923683560947,21.9911485751286),
 .UNSPECIFIED.);
#501=B_SPLINE_CURVE_WITH_KNOTS('',3,(#16527,#16528,#16529,#16530,#16531,
#16532,#16533,#16534,#16535,#16536),.UNSPECIFIED.,.F.,.F.,(4,1,1,1,1,1,
1,4),(15.7079632679491,16.2863744033008,17.2844166844248,18.2824589655488,
19.2805012466728,20.2785435277969,21.2765858089209,21.9911485751287),
 .UNSPECIFIED.);
#502=B_SPLINE_CURVE_WITH_KNOTS('',3,(#16539,#16540,#16541,#16542,#16543,
#16544,#16545,#16546,#16547,#16548,#16549,#16550,#16551,#16552,#16553,#16554,
#16555,#16556,#16557,#16558,#16559,#16560,#16561,#16562,#16563,#16564,#16565,
#16566,#16567,#16568,#16569,#16570,#16571,#16572,#16573,#16574,#16575,#16576,
#16577,#16578,#16579,#16580,#16581,#16582,#16583,#16584,#16585,#16586,#16587,
#16588,#16589,#16590,#16591,#16592,#16593,#16594,#16595,#16596,#16597,#16598,
#16599,#16600,#16601,#16602,#16603,#16604,#16605,#16606,#16607,#16608,#16609,
#16610,#16611,#16612,#16613,#16614,#16615,#16616,#16617,#16618,#16619,#16620,
#16621,#16622,#16623,#16624,#16625,#16626,#16627,#16628,#16629,#16630,#16631,
#16632,#16633,#16634,#16635,#16636,#16637,#16638,#16639,#16640,#16641,#16642,
#16643,#16644,#16645,#16646,#16647,#16648,#16649,#16650,#16651,#16652,#16653,
#16654,#16655,#16656,#16657,#16658,#16659),.UNSPECIFIED.,.F.,.F.,(4,3,3,
3,3,3,3,3,3,3,3,3,3,3,3,3,3,3,3,3,3,3,3,3,3,3,3,3,3,3,3,3,3,3,3,3,3,3,3,
3,4),(-0.753008129282056,-0.726412283548368,-0.715911613874471,-0.694893371653716,
-0.683361029549332,-0.673826434412814,-0.652889016486892,-0.639679181765185,
-0.63195159856097,-0.60480408471638,-0.59150990338668,-0.582561183693184,
-0.554067746128576,-0.540494882749548,-0.528208608719221,-0.505843484121927,
-0.4921308028701,-0.483102814228457,-0.456032674248847,-0.436199115577779,
-0.427073928162626,-0.400948091236321,-0.382860905241332,-0.374822254310016,
-0.34584221065474,-0.333939649620793,-0.324058619604945,-0.29393738163796,
-0.278576588250954,-0.269234263278142,-0.238815915606663,-0.225742435796944,
-0.216239773488962,-0.18666367230127,-0.170750005528772,-0.161294486761502,
-0.129614927749849,-0.114924930935507,-0.106250072717365,-0.0979353687381955,
-0.0965360155478562),.UNSPECIFIED.);
#503=B_SPLINE_CURVE_WITH_KNOTS('',3,(#16661,#16662,#16663,#16664,#16665,
#16666,#16667,#16668,#16669,#16670,#16671,#16672,#16673,#16674,#16675,#16676,
#16677,#16678,#16679,#16680,#16681,#16682,#16683,#16684,#16685,#16686,#16687,
#16688,#16689,#16690,#16691,#16692,#16693,#16694,#16695,#16696,#16697),
 .UNSPECIFIED.,.F.,.F.,(4,3,3,3,3,3,3,3,3,3,3,3,4),(-0.204609524178132,
-0.173922074105667,-0.152149392827302,-0.142793959810126,-0.12983323009626,
-0.11308637627832,-0.0998536142809363,-0.090547498816978,-0.0679106241127335,
-0.0514558350659385,-0.042025593252969,-0.0155529233063705,0.),
 .UNSPECIFIED.);
#504=B_SPLINE_CURVE_WITH_KNOTS('',3,(#16700,#16701,#16702,#16703,#16704,
#16705,#16706,#16707,#16708,#16709,#16710,#16711,#16712,#16713,#16714,#16715),
 .UNSPECIFIED.,.F.,.F.,(4,3,3,3,3,4),(-0.0965360155478562,-0.0724020116608921,
-0.0590232605257019,-0.050388474335024,-0.0186937936910934,0.),
 .UNSPECIFIED.);
#505=B_SPLINE_CURVE_WITH_KNOTS('',3,(#17504,#17505,#17506,#17507,#17508,
#17509,#17510,#17511),.UNSPECIFIED.,.F.,.F.,(4,1,1,1,1,4),(11.6159397475006,
12.61358260836,13.6112254692194,14.6088683300789,15.6065111909383,15.707963267949),
 .UNSPECIFIED.);
#506=B_SPLINE_CURVE_WITH_KNOTS('',3,(#17512,#17513,#17514,#17515,#17516,
#17517,#17518,#17519,#17520,#17521,#17522,#17523,#17524,#17525,#17526,#17527,
#17528,#17529,#17530,#17531,#17532,#17533,#17534,#17535,#17536,#17537,#17538,
#17539,#17540,#17541,#17542,#17543,#17544,#17545,#17546,#17547,#17548,#17549,
#17550,#17551,#17552,#17553,#17554,#17555,#17556,#17557,#17558,#17559,#17560),
 .UNSPECIFIED.,.F.,.F.,(4,3,3,3,3,3,3,3,3,3,3,3,3,3,3,3,4),(-0.275362278356892,
-0.263988733943187,-0.242277787653762,-0.228409792083558,-0.208856161945484,
-0.197709057767663,-0.168075464588018,-0.150222803571495,-0.140083955862437,
-0.125365894046572,-0.0997819296507484,-0.0889593225835958,-0.0667194919376969,
-0.0511923416312717,-0.0404361839568205,-0.0141940669149386,0.),
 .UNSPECIFIED.);
#507=B_SPLINE_CURVE_WITH_KNOTS('',3,(#17561,#17562,#17563,#17564,#17565,
#17566,#17567,#17568,#17569,#17570,#17571,#17572,#17573,#17574,#17575,#17576,
#17577,#17578,#17579),.UNSPECIFIED.,.F.,.F.,(4,3,3,3,3,3,4),(-191.027404416132,
-190.549786424147,-189.552143563287,-188.554500702428,-187.556857841568,
-186.559214980709,-186.304397428656),.UNSPECIFIED.);
#508=B_SPLINE_CURVE_WITH_KNOTS('',3,(#17582,#17583,#17584,#17585,#17586,
#17587,#17588,#17589,#17590),.UNSPECIFIED.,.F.,.F.,(4,1,1,1,1,1,4),(10.3752088276283,
11.2961629976806,12.2942052788047,13.2922475599287,14.2902898410527,15.2883321221767,
15.7079632679491),.UNSPECIFIED.);
#509=B_SPLINE_CURVE_WITH_KNOTS('',3,(#18384,#18385,#18386,#18387,#18388,
#18389,#18390,#18391,#18392,#18393,#18394,#18395,#18396,#18397,#18398,#18399,
#18400,#18401,#18402,#18403,#18404,#18405),.UNSPECIFIED.,.F.,.F.,(4,3,3,
3,3,3,3,4),(183.335115714669,183.639779726821,184.637822007945,185.635864289069,
186.633906570193,187.631948851317,188.629991132441,188.954231742812),
 .UNSPECIFIED.);
#510=B_SPLINE_CURVE_WITH_KNOTS('',3,(#18406,#18407,#18408,#18409,#18410,
#18411,#18412,#18413,#18414,#18415,#18416,#18417,#18418,#18419,#18420,#18421,
#18422,#18423,#18424,#18425,#18426,#18427,#18428,#18429,#18430,#18431,#18432,
#18433,#18434,#18435,#18436,#18437,#18438,#18439,#18440,#18441,#18442,#18443,
#18444,#18445,#18446,#18447,#18448,#18449,#18450,#18451,#18452,#18453,#18454,
#18455,#18456,#18457),.UNSPECIFIED.,.F.,.F.,(4,3,3,3,3,3,3,3,3,3,3,3,3,
3,3,3,3,4),(-0.276631791712714,-0.267404104599176,-0.245529112929484,-0.233826742508505,
-0.212230201958684,-0.201819484750363,-0.173281546649687,-0.162756755581661,
-0.152537502224722,-0.140478169692516,-0.120739781640826,-0.110641775261762,
-0.100726383882944,-0.0755447879122082,-0.0587891884452614,-0.0493012364577666,
-0.0182848522583483,0.),.UNSPECIFIED.);
#545=SHAPE_REPRESENTATION_RELATIONSHIP('SRR','None',#19525,#555);
#555=ADVANCED_BREP_SHAPE_REPRESENTATION('',(#575),#19468);
#565=STYLED_ITEM('',(#19583),#575);
#575=MANIFOLD_SOLID_BREP('Body1',#7158);
#647=FACE_BOUND('',#1674,.T.);
#648=FACE_BOUND('',#1677,.T.);
#800=PLANE('',#7755);
#801=PLANE('',#7756);
#802=PLANE('',#7757);
#803=PLANE('',#7758);
#804=PLANE('',#7759);
#805=PLANE('',#7760);
#806=PLANE('',#7761);
#807=PLANE('',#7762);
#808=PLANE('',#7766);
#809=PLANE('',#7767);
#1127=FACE_OUTER_BOUND('',#1601,.T.);
#1128=FACE_OUTER_BOUND('',#1602,.T.);
#1129=FACE_OUTER_BOUND('',#1603,.T.);
#1130=FACE_OUTER_BOUND('',#1604,.T.);
#1131=FACE_OUTER_BOUND('',#1605,.T.);
#1132=FACE_OUTER_BOUND('',#1606,.T.);
#1133=FACE_OUTER_BOUND('',#1607,.T.);
#1134=FACE_OUTER_BOUND('',#1608,.T.);
#1135=FACE_OUTER_BOUND('',#1609,.T.);
#1136=FACE_OUTER_BOUND('',#1610,.T.);
#1137=FACE_OUTER_BOUND('',#1611,.T.);
#1138=FACE_OUTER_BOUND('',#1612,.T.);
#1139=FACE_OUTER_BOUND('',#1613,.T.);
#1140=FACE_OUTER_BOUND('',#1614,.T.);
#1141=FACE_OUTER_BOUND('',#1615,.T.);
#1142=FACE_OUTER_BOUND('',#1616,.T.);
#1143=FACE_OUTER_BOUND('',#1617,.T.);
#1144=FACE_OUTER_BOUND('',#1618,.T.);
#1145=FACE_OUTER_BOUND('',#1619,.T.);
#1146=FACE_OUTER_BOUND('',#1620,.T.);
#1147=FACE_OUTER_BOUND('',#1621,.T.);
#1148=FACE_OUTER_BOUND('',#1622,.T.);
#1149=FACE_OUTER_BOUND('',#1623,.T.);
#1150=FACE_OUTER_BOUND('',#1624,.T.);
#1151=FACE_OUTER_BOUND('',#1625,.T.);
#1152=FACE_OUTER_BOUND('',#1626,.T.);
#1153=FACE_OUTER_BOUND('',#1627,.T.);
#1154=FACE_OUTER_BOUND('',#1628,.T.);
#1155=FACE_OUTER_BOUND('',#1629,.T.);
#1156=FACE_OUTER_BOUND('',#1630,.T.);
#1157=FACE_OUTER_BOUND('',#1631,.T.);
#1158=FACE_OUTER_BOUND('',#1632,.T.);
#1159=FACE_OUTER_BOUND('',#1633,.T.);
#1160=FACE_OUTER_BOUND('',#1634,.T.);
#1161=FACE_OUTER_BOUND('',#1635,.T.);
#1162=FACE_OUTER_BOUND('',#1636,.T.);
#1163=FACE_OUTER_BOUND('',#1637,.T.);
#1164=FACE_OUTER_BOUND('',#1638,.T.);
#1165=FACE_OUTER_BOUND('',#1639,.T.);
#1166=FACE_OUTER_BOUND('',#1640,.T.);
#1167=FACE_OUTER_BOUND('',#1641,.T.);
#1168=FACE_OUTER_BOUND('',#1642,.T.);
#1169=FACE_OUTER_BOUND('',#1643,.T.);
#1170=FACE_OUTER_BOUND('',#1644,.T.);
#1171=FACE_OUTER_BOUND('',#1645,.T.);
#1172=FACE_OUTER_BOUND('',#1646,.T.);
#1173=FACE_OUTER_BOUND('',#1647,.T.);
#1174=FACE_OUTER_BOUND('',#1648,.T.);
#1175=FACE_OUTER_BOUND('',#1649,.T.);
#1176=FACE_OUTER_BOUND('',#1650,.T.);
#1177=FACE_OUTER_BOUND('',#1651,.T.);
#1178=FACE_OUTER_BOUND('',#1652,.T.);
#1179=FACE_OUTER_BOUND('',#1653,.T.);
#1180=FACE_OUTER_BOUND('',#1654,.T.);
#1181=FACE_OUTER_BOUND('',#1655,.T.);
#1182=FACE_OUTER_BOUND('',#1656,.T.);
#1183=FACE_OUTER_BOUND('',#1657,.T.);
#1184=FACE_OUTER_BOUND('',#1658,.T.);
#1185=FACE_OUTER_BOUND('',#1659,.T.);
#1186=FACE_OUTER_BOUND('',#1660,.T.);
#1187=FACE_OUTER_BOUND('',#1661,.T.);
#1188=FACE_OUTER_BOUND('',#1662,.T.);
#1189=FACE_OUTER_BOUND('',#1663,.T.);
#1190=FACE_OUTER_BOUND('',#1664,.T.);
#1191=FACE_OUTER_BOUND('',#1665,.T.);
#1192=FACE_OUTER_BOUND('',#1666,.T.);
#1193=FACE_OUTER_BOUND('',#1667,.T.);
#1194=FACE_OUTER_BOUND('',#1668,.T.);
#1195=FACE_OUTER_BOUND('',#1669,.T.);
#1196=FACE_OUTER_BOUND('',#1670,.T.);
#1197=FACE_OUTER_BOUND('',#1671,.T.);
#1198=FACE_OUTER_BOUND('',#1672,.T.);
#1199=FACE_OUTER_BOUND('',#1673,.T.);
#1200=FACE_OUTER_BOUND('',#1675,.T.);
#1201=FACE_OUTER_BOUND('',#1676,.T.);
#1202=FACE_OUTER_BOUND('',#1678,.T.);
#1601=EDGE_LOOP('',(#6037,#6038,#6039,#6040));
#1602=EDGE_LOOP('',(#6041,#6042,#6043,#6044));
#1603=EDGE_LOOP('',(#6045,#6046,#6047,#6048));
#1604=EDGE_LOOP('',(#6049,#6050,#6051,#6052));
#1605=EDGE_LOOP('',(#6053,#6054,#6055,#6056));
#1606=EDGE_LOOP('',(#6057,#6058,#6059,#6060));
#1607=EDGE_LOOP('',(#6061,#6062,#6063,#6064));
#1608=EDGE_LOOP('',(#6065,#6066,#6067,#6068));
#1609=EDGE_LOOP('',(#6069,#6070,#6071,#6072));
#1610=EDGE_LOOP('',(#6073,#6074,#6075,#6076));
#1611=EDGE_LOOP('',(#6077,#6078,#6079,#6080));
#1612=EDGE_LOOP('',(#6081,#6082,#6083,#6084));
#1613=EDGE_LOOP('',(#6085,#6086,#6087,#6088));
#1614=EDGE_LOOP('',(#6089,#6090,#6091,#6092));
#1615=EDGE_LOOP('',(#6093,#6094,#6095,#6096));
#1616=EDGE_LOOP('',(#6097,#6098,#6099,#6100));
#1617=EDGE_LOOP('',(#6101,#6102,#6103,#6104));
#1618=EDGE_LOOP('',(#6105,#6106,#6107,#6108));
#1619=EDGE_LOOP('',(#6109,#6110,#6111,#6112));
#1620=EDGE_LOOP('',(#6113,#6114,#6115,#6116));
#1621=EDGE_LOOP('',(#6117,#6118,#6119,#6120));
#1622=EDGE_LOOP('',(#6121,#6122,#6123,#6124));
#1623=EDGE_LOOP('',(#6125,#6126,#6127,#6128));
#1624=EDGE_LOOP('',(#6129,#6130,#6131,#6132));
#1625=EDGE_LOOP('',(#6133,#6134,#6135,#6136));
#1626=EDGE_LOOP('',(#6137,#6138,#6139,#6140));
#1627=EDGE_LOOP('',(#6141,#6142,#6143,#6144));
#1628=EDGE_LOOP('',(#6145,#6146,#6147,#6148));
#1629=EDGE_LOOP('',(#6149,#6150,#6151,#6152));
#1630=EDGE_LOOP('',(#6153,#6154,#6155,#6156));
#1631=EDGE_LOOP('',(#6157,#6158,#6159,#6160));
#1632=EDGE_LOOP('',(#6161,#6162,#6163,#6164));
#1633=EDGE_LOOP('',(#6165,#6166,#6167,#6168));
#1634=EDGE_LOOP('',(#6169,#6170,#6171,#6172));
#1635=EDGE_LOOP('',(#6173,#6174,#6175,#6176));
#1636=EDGE_LOOP('',(#6177,#6178,#6179,#6180));
#1637=EDGE_LOOP('',(#6181,#6182,#6183,#6184));
#1638=EDGE_LOOP('',(#6185,#6186,#6187,#6188));
#1639=EDGE_LOOP('',(#6189,#6190,#6191,#6192));
#1640=EDGE_LOOP('',(#6193,#6194,#6195,#6196));
#1641=EDGE_LOOP('',(#6197,#6198,#6199,#6200));
#1642=EDGE_LOOP('',(#6201,#6202,#6203,#6204));
#1643=EDGE_LOOP('',(#6205,#6206,#6207,#6208));
#1644=EDGE_LOOP('',(#6209,#6210,#6211,#6212));
#1645=EDGE_LOOP('',(#6213,#6214,#6215,#6216));
#1646=EDGE_LOOP('',(#6217,#6218,#6219,#6220));
#1647=EDGE_LOOP('',(#6221,#6222,#6223,#6224));
#1648=EDGE_LOOP('',(#6225,#6226,#6227,#6228));
#1649=EDGE_LOOP('',(#6229,#6230,#6231,#6232));
#1650=EDGE_LOOP('',(#6233,#6234,#6235,#6236));
#1651=EDGE_LOOP('',(#6237,#6238,#6239,#6240));
#1652=EDGE_LOOP('',(#6241,#6242,#6243,#6244));
#1653=EDGE_LOOP('',(#6245,#6246,#6247,#6248));
#1654=EDGE_LOOP('',(#6249,#6250,#6251,#6252));
#1655=EDGE_LOOP('',(#6253,#6254,#6255,#6256));
#1656=EDGE_LOOP('',(#6257,#6258,#6259,#6260));
#1657=EDGE_LOOP('',(#6261,#6262,#6263,#6264));
#1658=EDGE_LOOP('',(#6265,#6266,#6267,#6268));
#1659=EDGE_LOOP('',(#6269,#6270,#6271,#6272));
#1660=EDGE_LOOP('',(#6273,#6274,#6275,#6276));
#1661=EDGE_LOOP('',(#6277,#6278,#6279,#6280,#6281,#6282,#6283,#6284));
#1662=EDGE_LOOP('',(#6285,#6286,#6287,#6288,#6289,#6290,#6291,#6292,#6293,
#6294,#6295,#6296,#6297,#6298,#6299,#6300,#6301,#6302,#6303,#6304,#6305,
#6306,#6307,#6308,#6309,#6310,#6311,#6312,#6313,#6314,#6315,#6316,#6317,
#6318,#6319,#6320,#6321,#6322,#6323,#6324,#6325,#6326,#6327,#6328,#6329,
#6330,#6331,#6332,#6333,#6334,#6335,#6336,#6337,#6338,#6339,#6340,#6341,
#6342,#6343,#6344,#6345,#6346,#6347,#6348));
#1663=EDGE_LOOP('',(#6349,#6350,#6351,#6352));
#1664=EDGE_LOOP('',(#6353,#6354,#6355,#6356,#6357,#6358,#6359,#6360,#6361,
#6362,#6363,#6364,#6365,#6366,#6367,#6368,#6369,#6370,#6371,#6372,#6373,
#6374,#6375,#6376,#6377,#6378,#6379,#6380,#6381,#6382,#6383,#6384,#6385,
#6386,#6387,#6388,#6389,#6390,#6391,#6392,#6393,#6394,#6395,#6396,#6397,
#6398,#6399,#6400,#6401,#6402,#6403,#6404,#6405,#6406,#6407,#6408,#6409,
#6410,#6411,#6412,#6413,#6414,#6415,#6416,#6417));
#1665=EDGE_LOOP('',(#6418,#6419,#6420,#6421));
#1666=EDGE_LOOP('',(#6422,#6423,#6424,#6425));
#1667=EDGE_LOOP('',(#6426,#6427,#6428,#6429));
#1668=EDGE_LOOP('',(#6430,#6431,#6432,#6433));
#1669=EDGE_LOOP('',(#6434,#6435,#6436,#6437));
#1670=EDGE_LOOP('',(#6438,#6439,#6440,#6441));
#1671=EDGE_LOOP('',(#6442,#6443,#6444,#6445));
#1672=EDGE_LOOP('',(#6446,#6447,#6448,#6449,#6450,#6451));
#1673=EDGE_LOOP('',(#6452));
#1674=EDGE_LOOP('',(#6453,#6454,#6455,#6456));
#1675=EDGE_LOOP('',(#6457,#6458,#6459,#6460));
#1676=EDGE_LOOP('',(#6461));
#1677=EDGE_LOOP('',(#6462,#6463,#6464,#6465,#6466,#6467));
#1678=EDGE_LOOP('',(#6468));
#2073=LINE('',#14341,#2547);
#2074=LINE('',#14365,#2548);
#2075=LINE('',#14413,#2549);
#2076=LINE('',#14461,#2550);
#2077=LINE('',#14512,#2551);
#2078=LINE('',#14560,#2552);
#2079=LINE('',#14608,#2553);
#2080=LINE('',#14656,#2554);
#2081=LINE('',#14710,#2555);
#2082=LINE('',#14758,#2556);
#2083=LINE('',#14806,#2557);
#2084=LINE('',#14860,#2558);
#2085=LINE('',#14908,#2559);
#2086=LINE('',#14956,#2560);
#2087=LINE('',#15004,#2561);
#2088=LINE('',#15058,#2562);
#2089=LINE('',#15106,#2563);
#2090=LINE('',#15154,#2564);
#2091=LINE('',#15208,#2565);
#2092=LINE('',#15256,#2566);
#2093=LINE('',#15304,#2567);
#2094=LINE('',#15358,#2568);
#2095=LINE('',#15406,#2569);
#2096=LINE('',#15454,#2570);
#2097=LINE('',#15502,#2571);
#2098=LINE('',#15556,#2572);
#2099=LINE('',#15604,#2573);
#2100=LINE('',#15652,#2574);
#2101=LINE('',#15706,#2575);
#2102=LINE('',#15754,#2576);
#2103=LINE('',#15802,#2577);
#2104=LINE('',#15828,#2578);
#2105=LINE('',#15852,#2579);
#2106=LINE('',#15876,#2580);
#2107=LINE('',#15901,#2581);
#2108=LINE('',#15926,#2582);
#2109=LINE('',#15950,#2583);
#2110=LINE('',#15975,#2584);
#2111=LINE('',#16000,#2585);
#2112=LINE('',#16024,#2586);
#2113=LINE('',#16048,#2587);
#2114=LINE('',#16073,#2588);
#2115=LINE('',#16098,#2589);
#2116=LINE('',#16122,#2590);
#2117=LINE('',#16147,#2591);
#2118=LINE('',#16172,#2592);
#2119=LINE('',#16196,#2593);
#2120=LINE('',#16221,#2594);
#2121=LINE('',#16246,#2595);
#2122=LINE('',#16270,#2596);
#2123=LINE('',#16294,#2597);
#2124=LINE('',#16319,#2598);
#2125=LINE('',#16344,#2599);
#2126=LINE('',#16368,#2600);
#2127=LINE('',#16393,#2601);
#2128=LINE('',#16418,#2602);
#2129=LINE('',#16442,#2603);
#2130=LINE('',#16467,#2604);
#2131=LINE('',#16491,#2605);
#2132=LINE('',#16516,#2606);
#2133=LINE('',#16717,#2607);
#2134=LINE('',#18462,#2608);
#2135=LINE('',#18464,#2609);
#2136=LINE('',#18466,#2610);
#2137=LINE('',#18467,#2611);
#2138=LINE('',#18470,#2612);
#2139=LINE('',#18472,#2613);
#2140=LINE('',#18473,#2614);
#2141=LINE('',#18476,#2615);
#2142=LINE('',#18478,#2616);
#2143=LINE('',#18479,#2617);
#2144=LINE('',#18482,#2618);
#2145=LINE('',#18484,#2619);
#2146=LINE('',#18485,#2620);
#2147=LINE('',#18488,#2621);
#2148=LINE('',#18490,#2622);
#2149=LINE('',#18491,#2623);
#2150=LINE('',#18493,#2624);
#2151=LINE('',#18494,#2625);
#2152=LINE('',#18501,#2626);
#2547=VECTOR('',#9015,0.15);
#2548=VECTOR('',#9020,0.15);
#2549=VECTOR('',#9023,0.15);
#2550=VECTOR('',#9026,0.15);
#2551=VECTOR('',#9029,0.15);
#2552=VECTOR('',#9032,0.15);
#2553=VECTOR('',#9035,0.15);
#2554=VECTOR('',#9038,0.15);
#2555=VECTOR('',#9041,0.15);
#2556=VECTOR('',#9044,0.15);
#2557=VECTOR('',#9047,0.15);
#2558=VECTOR('',#9050,0.15);
#2559=VECTOR('',#9053,0.15);
#2560=VECTOR('',#9056,0.15);
#2561=VECTOR('',#9059,0.15);
#2562=VECTOR('',#9062,0.15);
#2563=VECTOR('',#9065,0.15);
#2564=VECTOR('',#9068,0.15);
#2565=VECTOR('',#9071,0.15);
#2566=VECTOR('',#9074,0.15);
#2567=VECTOR('',#9077,0.15);
#2568=VECTOR('',#9080,0.15);
#2569=VECTOR('',#9083,0.15);
#2570=VECTOR('',#9086,0.15);
#2571=VECTOR('',#9089,0.15);
#2572=VECTOR('',#9092,0.15);
#2573=VECTOR('',#9095,0.15);
#2574=VECTOR('',#9098,0.15);
#2575=VECTOR('',#9101,0.15);
#2576=VECTOR('',#9104,0.15);
#2577=VECTOR('',#9107,0.117775);
#2578=VECTOR('',#9112,0.117775);
#2579=VECTOR('',#9115,0.117775);
#2580=VECTOR('',#9118,0.117775);
#2581=VECTOR('',#9121,0.117775);
#2582=VECTOR('',#9124,0.117775);
#2583=VECTOR('',#9127,0.117775);
#2584=VECTOR('',#9130,0.117775);
#2585=VECTOR('',#9133,0.117775);
#2586=VECTOR('',#9136,0.117775);
#2587=VECTOR('',#9139,0.117775);
#2588=VECTOR('',#9142,0.117775);
#2589=VECTOR('',#9145,0.117775);
#2590=VECTOR('',#9148,0.117775);
#2591=VECTOR('',#9151,0.117775);
#2592=VECTOR('',#9154,0.117775);
#2593=VECTOR('',#9157,0.117775);
#2594=VECTOR('',#9160,0.117775);
#2595=VECTOR('',#9163,0.117775);
#2596=VECTOR('',#9166,0.117775);
#2597=VECTOR('',#9169,0.117775);
#2598=VECTOR('',#9172,0.117775);
#2599=VECTOR('',#9175,0.117775);
#2600=VECTOR('',#9178,0.117775);
#2601=VECTOR('',#9181,0.117775);
#2602=VECTOR('',#9184,0.117775);
#2603=VECTOR('',#9187,0.117775);
#2604=VECTOR('',#9190,0.117775);
#2605=VECTOR('',#9193,0.117775);
#2606=VECTOR('',#9196,0.117775);
#2607=VECTOR('',#9201,0.1);
#2608=VECTOR('',#9212,1.);
#2609=VECTOR('',#9213,1.);
#2610=VECTOR('',#9214,1.);
#2611=VECTOR('',#9215,1.);
#2612=VECTOR('',#9218,1.);
#2613=VECTOR('',#9219,1.);
#2614=VECTOR('',#9220,1.);
#2615=VECTOR('',#9223,1.);
#2616=VECTOR('',#9224,1.);
#2617=VECTOR('',#9225,1.);
#2618=VECTOR('',#9228,1.);
#2619=VECTOR('',#9229,1.);
#2620=VECTOR('',#9230,1.);
#2621=VECTOR('',#9233,1.);
#2622=VECTOR('',#9234,1.);
#2623=VECTOR('',#9235,1.);
#2624=VECTOR('',#9238,1.);
#2625=VECTOR('',#9239,1.);
#2626=VECTOR('',#9248,0.275);
#2831=CIRCLE('',#7688,0.14635);
#2832=CIRCLE('',#7719,0.117775);
#2833=CIRCLE('',#7750,0.14635);
#2834=CIRCLE('',#7751,0.05);
#2835=CIRCLE('',#7753,0.117775);
#2836=CIRCLE('',#7763,0.275);
#2837=CIRCLE('',#7765,0.275);
#3323=VERTEX_POINT('',#14339);
#3324=VERTEX_POINT('',#14340);
#3325=VERTEX_POINT('',#14342);
#3326=VERTEX_POINT('',#14353);
#3327=VERTEX_POINT('',#14363);
#3328=VERTEX_POINT('',#14364);
#3329=VERTEX_POINT('',#14411);
#3330=VERTEX_POINT('',#14412);
#3331=VERTEX_POINT('',#14459);
#3332=VERTEX_POINT('',#14460);
#3333=VERTEX_POINT('',#14510);
#3334=VERTEX_POINT('',#14511);
#3335=VERTEX_POINT('',#14558);
#3336=VERTEX_POINT('',#14559);
#3337=VERTEX_POINT('',#14606);
#3338=VERTEX_POINT('',#14607);
#3339=VERTEX_POINT('',#14654);
#3340=VERTEX_POINT('',#14655);
#3341=VERTEX_POINT('',#14708);
#3342=VERTEX_POINT('',#14709);
#3343=VERTEX_POINT('',#14756);
#3344=VERTEX_POINT('',#14757);
#3345=VERTEX_POINT('',#14804);
#3346=VERTEX_POINT('',#14805);
#3347=VERTEX_POINT('',#14858);
#3348=VERTEX_POINT('',#14859);
#3349=VERTEX_POINT('',#14906);
#3350=VERTEX_POINT('',#14907);
#3351=VERTEX_POINT('',#14954);
#3352=VERTEX_POINT('',#14955);
#3353=VERTEX_POINT('',#15002);
#3354=VERTEX_POINT('',#15003);
#3355=VERTEX_POINT('',#15056);
#3356=VERTEX_POINT('',#15057);
#3357=VERTEX_POINT('',#15104);
#3358=VERTEX_POINT('',#15105);
#3359=VERTEX_POINT('',#15152);
#3360=VERTEX_POINT('',#15153);
#3361=VERTEX_POINT('',#15206);
#3362=VERTEX_POINT('',#15207);
#3363=VERTEX_POINT('',#15254);
#3364=VERTEX_POINT('',#15255);
#3365=VERTEX_POINT('',#15302);
#3366=VERTEX_POINT('',#15303);
#3367=VERTEX_POINT('',#15356);
#3368=VERTEX_POINT('',#15357);
#3369=VERTEX_POINT('',#15404);
#3370=VERTEX_POINT('',#15405);
#3371=VERTEX_POINT('',#15452);
#3372=VERTEX_POINT('',#15453);
#3373=VERTEX_POINT('',#15500);
#3374=VERTEX_POINT('',#15501);
#3375=VERTEX_POINT('',#15554);
#3376=VERTEX_POINT('',#15555);
#3377=VERTEX_POINT('',#15602);
#3378=VERTEX_POINT('',#15603);
#3379=VERTEX_POINT('',#15650);
#3380=VERTEX_POINT('',#15651);
#3381=VERTEX_POINT('',#15704);
#3382=VERTEX_POINT('',#15705);
#3383=VERTEX_POINT('',#15752);
#3384=VERTEX_POINT('',#15753);
#3385=VERTEX_POINT('',#15800);
#3386=VERTEX_POINT('',#15801);
#3387=VERTEX_POINT('',#15803);
#3388=VERTEX_POINT('',#15814);
#3389=VERTEX_POINT('',#15826);
#3390=VERTEX_POINT('',#15827);
#3391=VERTEX_POINT('',#15850);
#3392=VERTEX_POINT('',#15851);
#3393=VERTEX_POINT('',#15874);
#3394=VERTEX_POINT('',#15875);
#3395=VERTEX_POINT('',#15899);
#3396=VERTEX_POINT('',#15900);
#3397=VERTEX_POINT('',#15924);
#3398=VERTEX_POINT('',#15925);
#3399=VERTEX_POINT('',#15948);
#3400=VERTEX_POINT('',#15949);
#3401=VERTEX_POINT('',#15973);
#3402=VERTEX_POINT('',#15974);
#3403=VERTEX_POINT('',#15998);
#3404=VERTEX_POINT('',#15999);
#3405=VERTEX_POINT('',#16022);
#3406=VERTEX_POINT('',#16023);
#3407=VERTEX_POINT('',#16046);
#3408=VERTEX_POINT('',#16047);
#3409=VERTEX_POINT('',#16071);
#3410=VERTEX_POINT('',#16072);
#3411=VERTEX_POINT('',#16096);
#3412=VERTEX_POINT('',#16097);
#3413=VERTEX_POINT('',#16120);
#3414=VERTEX_POINT('',#16121);
#3415=VERTEX_POINT('',#16145);
#3416=VERTEX_POINT('',#16146);
#3417=VERTEX_POINT('',#16170);
#3418=VERTEX_POINT('',#16171);
#3419=VERTEX_POINT('',#16194);
#3420=VERTEX_POINT('',#16195);
#3421=VERTEX_POINT('',#16219);
#3422=VERTEX_POINT('',#16220);
#3423=VERTEX_POINT('',#16244);
#3424=VERTEX_POINT('',#16245);
#3425=VERTEX_POINT('',#16268);
#3426=VERTEX_POINT('',#16269);
#3427=VERTEX_POINT('',#16292);
#3428=VERTEX_POINT('',#16293);
#3429=VERTEX_POINT('',#16317);
#3430=VERTEX_POINT('',#16318);
#3431=VERTEX_POINT('',#16342);
#3432=VERTEX_POINT('',#16343);
#3433=VERTEX_POINT('',#16366);
#3434=VERTEX_POINT('',#16367);
#3435=VERTEX_POINT('',#16391);
#3436=VERTEX_POINT('',#16392);
#3437=VERTEX_POINT('',#16416);
#3438=VERTEX_POINT('',#16417);
#3439=VERTEX_POINT('',#16440);
#3440=VERTEX_POINT('',#16441);
#3441=VERTEX_POINT('',#16465);
#3442=VERTEX_POINT('',#16466);
#3443=VERTEX_POINT('',#16489);
#3444=VERTEX_POINT('',#16490);
#3445=VERTEX_POINT('',#16514);
#3446=VERTEX_POINT('',#16515);
#3447=VERTEX_POINT('',#16538);
#3448=VERTEX_POINT('',#16660);
#3449=VERTEX_POINT('',#16698);
#3450=VERTEX_POINT('',#16716);
#3451=VERTEX_POINT('',#17503);
#3452=VERTEX_POINT('',#17581);
#3453=VERTEX_POINT('',#18460);
#3454=VERTEX_POINT('',#18461);
#3455=VERTEX_POINT('',#18463);
#3456=VERTEX_POINT('',#18465);
#3457=VERTEX_POINT('',#18469);
#3458=VERTEX_POINT('',#18471);
#3459=VERTEX_POINT('',#18475);
#3460=VERTEX_POINT('',#18477);
#3461=VERTEX_POINT('',#18481);
#3462=VERTEX_POINT('',#18483);
#3463=VERTEX_POINT('',#18487);
#3464=VERTEX_POINT('',#18489);
#3465=VERTEX_POINT('',#18497);
#3466=VERTEX_POINT('',#18500);
#4259=EDGE_CURVE('',#3323,#3324,#2073,.T.);
#4260=EDGE_CURVE('',#3323,#3325,#382,.T.);
#4261=EDGE_CURVE('',#3325,#3326,#2831,.F.);
#4262=EDGE_CURVE('',#3326,#3324,#383,.T.);
#4263=EDGE_CURVE('',#3327,#3328,#2074,.T.);
#4264=EDGE_CURVE('',#3327,#3323,#384,.T.);
#4265=EDGE_CURVE('',#3324,#3328,#385,.T.);
#4266=EDGE_CURVE('',#3329,#3330,#2075,.T.);
#4267=EDGE_CURVE('',#3329,#3327,#386,.T.);
#4268=EDGE_CURVE('',#3328,#3330,#387,.T.);
#4269=EDGE_CURVE('',#3331,#3332,#2076,.T.);
#4270=EDGE_CURVE('',#3331,#3329,#388,.T.);
#4271=EDGE_CURVE('',#3330,#3332,#389,.T.);
#4272=EDGE_CURVE('',#3333,#3334,#2077,.T.);
#4273=EDGE_CURVE('',#3333,#3331,#390,.T.);
#4274=EDGE_CURVE('',#3332,#3334,#391,.T.);
#4275=EDGE_CURVE('',#3335,#3336,#2078,.T.);
#4276=EDGE_CURVE('',#3335,#3333,#392,.T.);
#4277=EDGE_CURVE('',#3334,#3336,#393,.T.);
#4278=EDGE_CURVE('',#3337,#3338,#2079,.T.);
#4279=EDGE_CURVE('',#3337,#3335,#394,.T.);
#4280=EDGE_CURVE('',#3336,#3338,#395,.T.);
#4281=EDGE_CURVE('',#3339,#3340,#2080,.T.);
#4282=EDGE_CURVE('',#3339,#3337,#396,.T.);
#4283=EDGE_CURVE('',#3338,#3340,#397,.T.);
#4284=EDGE_CURVE('',#3341,#3342,#2081,.T.);
#4285=EDGE_CURVE('',#3341,#3339,#398,.T.);
#4286=EDGE_CURVE('',#3340,#3342,#399,.T.);
#4287=EDGE_CURVE('',#3343,#3344,#2082,.T.);
#4288=EDGE_CURVE('',#3343,#3341,#400,.T.);
#4289=EDGE_CURVE('',#3342,#3344,#401,.T.);
#4290=EDGE_CURVE('',#3345,#3346,#2083,.T.);
#4291=EDGE_CURVE('',#3345,#3343,#402,.T.);
#4292=EDGE_CURVE('',#3344,#3346,#403,.T.);
#4293=EDGE_CURVE('',#3347,#3348,#2084,.T.);
#4294=EDGE_CURVE('',#3347,#3345,#404,.T.);
#4295=EDGE_CURVE('',#3346,#3348,#405,.T.);
#4296=EDGE_CURVE('',#3349,#3350,#2085,.T.);
#4297=EDGE_CURVE('',#3349,#3347,#406,.T.);
#4298=EDGE_CURVE('',#3348,#3350,#407,.T.);
#4299=EDGE_CURVE('',#3351,#3352,#2086,.T.);
#4300=EDGE_CURVE('',#3351,#3349,#408,.T.);
#4301=EDGE_CURVE('',#3350,#3352,#409,.T.);
#4302=EDGE_CURVE('',#3353,#3354,#2087,.T.);
#4303=EDGE_CURVE('',#3353,#3351,#410,.T.);
#4304=EDGE_CURVE('',#3352,#3354,#411,.T.);
#4305=EDGE_CURVE('',#3355,#3356,#2088,.T.);
#4306=EDGE_CURVE('',#3355,#3353,#412,.T.);
#4307=EDGE_CURVE('',#3354,#3356,#413,.T.);
#4308=EDGE_CURVE('',#3357,#3358,#2089,.T.);
#4309=EDGE_CURVE('',#3357,#3355,#414,.T.);
#4310=EDGE_CURVE('',#3356,#3358,#415,.T.);
#4311=EDGE_CURVE('',#3359,#3360,#2090,.T.);
#4312=EDGE_CURVE('',#3359,#3357,#416,.T.);
#4313=EDGE_CURVE('',#3358,#3360,#417,.T.);
#4314=EDGE_CURVE('',#3361,#3362,#2091,.T.);
#4315=EDGE_CURVE('',#3361,#3359,#418,.T.);
#4316=EDGE_CURVE('',#3360,#3362,#419,.T.);
#4317=EDGE_CURVE('',#3363,#3364,#2092,.T.);
#4318=EDGE_CURVE('',#3363,#3361,#420,.T.);
#4319=EDGE_CURVE('',#3362,#3364,#421,.T.);
#4320=EDGE_CURVE('',#3365,#3366,#2093,.T.);
#4321=EDGE_CURVE('',#3365,#3363,#422,.T.);
#4322=EDGE_CURVE('',#3364,#3366,#423,.T.);
#4323=EDGE_CURVE('',#3367,#3368,#2094,.T.);
#4324=EDGE_CURVE('',#3367,#3365,#424,.T.);
#4325=EDGE_CURVE('',#3366,#3368,#425,.T.);
#4326=EDGE_CURVE('',#3369,#3370,#2095,.T.);
#4327=EDGE_CURVE('',#3369,#3367,#426,.T.);
#4328=EDGE_CURVE('',#3368,#3370,#427,.T.);
#4329=EDGE_CURVE('',#3371,#3372,#2096,.T.);
#4330=EDGE_CURVE('',#3371,#3369,#428,.T.);
#4331=EDGE_CURVE('',#3370,#3372,#429,.T.);
#4332=EDGE_CURVE('',#3373,#3374,#2097,.T.);
#4333=EDGE_CURVE('',#3373,#3371,#430,.T.);
#4334=EDGE_CURVE('',#3372,#3374,#431,.T.);
#4335=EDGE_CURVE('',#3375,#3376,#2098,.T.);
#4336=EDGE_CURVE('',#3375,#3373,#432,.T.);
#4337=EDGE_CURVE('',#3374,#3376,#433,.T.);
#4338=EDGE_CURVE('',#3377,#3378,#2099,.T.);
#4339=EDGE_CURVE('',#3377,#3375,#434,.T.);
#4340=EDGE_CURVE('',#3376,#3378,#435,.T.);
#4341=EDGE_CURVE('',#3379,#3380,#2100,.T.);
#4342=EDGE_CURVE('',#3379,#3377,#436,.T.);
#4343=EDGE_CURVE('',#3378,#3380,#437,.T.);
#4344=EDGE_CURVE('',#3381,#3382,#2101,.T.);
#4345=EDGE_CURVE('',#3381,#3379,#438,.T.);
#4346=EDGE_CURVE('',#3380,#3382,#439,.T.);
#4347=EDGE_CURVE('',#3383,#3384,#2102,.T.);
#4348=EDGE_CURVE('',#3383,#3381,#440,.T.);
#4349=EDGE_CURVE('',#3382,#3384,#441,.T.);
#4350=EDGE_CURVE('',#3385,#3386,#2103,.T.);
#4351=EDGE_CURVE('',#3385,#3387,#442,.T.);
#4352=EDGE_CURVE('',#3387,#3388,#2832,.T.);
#4353=EDGE_CURVE('',#3386,#3388,#443,.T.);
#4354=EDGE_CURVE('',#3389,#3390,#2104,.T.);
#4355=EDGE_CURVE('',#3389,#3385,#444,.T.);
#4356=EDGE_CURVE('',#3390,#3386,#445,.T.);
#4357=EDGE_CURVE('',#3391,#3392,#2105,.T.);
#4358=EDGE_CURVE('',#3391,#3389,#446,.T.);
#4359=EDGE_CURVE('',#3392,#3390,#447,.T.);
#4360=EDGE_CURVE('',#3393,#3394,#2106,.T.);
#4361=EDGE_CURVE('',#3393,#3391,#448,.T.);
#4362=EDGE_CURVE('',#3394,#3392,#449,.T.);
#4363=EDGE_CURVE('',#3395,#3396,#2107,.T.);
#4364=EDGE_CURVE('',#3395,#3393,#450,.T.);
#4365=EDGE_CURVE('',#3396,#3394,#451,.T.);
#4366=EDGE_CURVE('',#3397,#3398,#2108,.T.);
#4367=EDGE_CURVE('',#3397,#3395,#452,.T.);
#4368=EDGE_CURVE('',#3398,#3396,#453,.T.);
#4369=EDGE_CURVE('',#3399,#3400,#2109,.T.);
#4370=EDGE_CURVE('',#3399,#3397,#454,.T.);
#4371=EDGE_CURVE('',#3400,#3398,#455,.T.);
#4372=EDGE_CURVE('',#3401,#3402,#2110,.T.);
#4373=EDGE_CURVE('',#3401,#3399,#456,.T.);
#4374=EDGE_CURVE('',#3402,#3400,#457,.T.);
#4375=EDGE_CURVE('',#3403,#3404,#2111,.T.);
#4376=EDGE_CURVE('',#3403,#3401,#458,.T.);
#4377=EDGE_CURVE('',#3404,#3402,#459,.T.);
#4378=EDGE_CURVE('',#3405,#3406,#2112,.T.);
#4379=EDGE_CURVE('',#3405,#3403,#460,.T.);
#4380=EDGE_CURVE('',#3406,#3404,#461,.T.);
#4381=EDGE_CURVE('',#3407,#3408,#2113,.T.);
#4382=EDGE_CURVE('',#3407,#3405,#462,.T.);
#4383=EDGE_CURVE('',#3408,#3406,#463,.T.);
#4384=EDGE_CURVE('',#3409,#3410,#2114,.T.);
#4385=EDGE_CURVE('',#3409,#3407,#464,.T.);
#4386=EDGE_CURVE('',#3410,#3408,#465,.T.);
#4387=EDGE_CURVE('',#3411,#3412,#2115,.T.);
#4388=EDGE_CURVE('',#3411,#3409,#466,.T.);
#4389=EDGE_CURVE('',#3412,#3410,#467,.T.);
#4390=EDGE_CURVE('',#3413,#3414,#2116,.T.);
#4391=EDGE_CURVE('',#3413,#3411,#468,.T.);
#4392=EDGE_CURVE('',#3414,#3412,#469,.T.);
#4393=EDGE_CURVE('',#3415,#3416,#2117,.T.);
#4394=EDGE_CURVE('',#3415,#3413,#470,.T.);
#4395=EDGE_CURVE('',#3416,#3414,#471,.T.);
#4396=EDGE_CURVE('',#3417,#3418,#2118,.T.);
#4397=EDGE_CURVE('',#3417,#3415,#472,.T.);
#4398=EDGE_CURVE('',#3418,#3416,#473,.T.);
#4399=EDGE_CURVE('',#3419,#3420,#2119,.T.);
#4400=EDGE_CURVE('',#3419,#3417,#474,.T.);
#4401=EDGE_CURVE('',#3420,#3418,#475,.T.);
#4402=EDGE_CURVE('',#3421,#3422,#2120,.T.);
#4403=EDGE_CURVE('',#3421,#3419,#476,.T.);
#4404=EDGE_CURVE('',#3422,#3420,#477,.T.);
#4405=EDGE_CURVE('',#3423,#3424,#2121,.T.);
#4406=EDGE_CURVE('',#3423,#3421,#478,.T.);
#4407=EDGE_CURVE('',#3424,#3422,#479,.T.);
#4408=EDGE_CURVE('',#3425,#3426,#2122,.T.);
#4409=EDGE_CURVE('',#3425,#3423,#480,.T.);
#4410=EDGE_CURVE('',#3426,#3424,#481,.T.);
#4411=EDGE_CURVE('',#3427,#3428,#2123,.T.);
#4412=EDGE_CURVE('',#3427,#3425,#482,.T.);
#4413=EDGE_CURVE('',#3428,#3426,#483,.T.);
#4414=EDGE_CURVE('',#3429,#3430,#2124,.T.);
#4415=EDGE_CURVE('',#3429,#3427,#484,.T.);
#4416=EDGE_CURVE('',#3430,#3428,#485,.T.);
#4417=EDGE_CURVE('',#3431,#3432,#2125,.T.);
#4418=EDGE_CURVE('',#3431,#3429,#486,.T.);
#4419=EDGE_CURVE('',#3432,#3430,#487,.T.);
#4420=EDGE_CURVE('',#3433,#3434,#2126,.T.);
#4421=EDGE_CURVE('',#3433,#3431,#488,.T.);
#4422=EDGE_CURVE('',#3434,#3432,#489,.T.);
#4423=EDGE_CURVE('',#3435,#3436,#2127,.T.);
#4424=EDGE_CURVE('',#3435,#3433,#490,.T.);
#4425=EDGE_CURVE('',#3436,#3434,#491,.T.);
#4426=EDGE_CURVE('',#3437,#3438,#2128,.T.);
#4427=EDGE_CURVE('',#3437,#3435,#492,.T.);
#4428=EDGE_CURVE('',#3438,#3436,#493,.T.);
#4429=EDGE_CURVE('',#3439,#3440,#2129,.T.);
#4430=EDGE_CURVE('',#3439,#3437,#494,.T.);
#4431=EDGE_CURVE('',#3440,#3438,#495,.T.);
#4432=EDGE_CURVE('',#3441,#3442,#2130,.T.);
#4433=EDGE_CURVE('',#3441,#3439,#496,.T.);
#4434=EDGE_CURVE('',#3442,#3440,#497,.T.);
#4435=EDGE_CURVE('',#3443,#3444,#2131,.T.);
#4436=EDGE_CURVE('',#3443,#3441,#498,.T.);
#4437=EDGE_CURVE('',#3444,#3442,#499,.T.);
#4438=EDGE_CURVE('',#3445,#3446,#2132,.T.);
#4439=EDGE_CURVE('',#3445,#3443,#500,.T.);
#4440=EDGE_CURVE('',#3446,#3444,#501,.T.);
#4441=EDGE_CURVE('',#3388,#3447,#502,.T.);
#4442=EDGE_CURVE('',#3448,#3387,#503,.T.);
#4443=EDGE_CURVE('',#3449,#3448,#2833,.T.);
#4444=EDGE_CURVE('',#3447,#3449,#504,.T.);
#4445=EDGE_CURVE('',#3447,#3450,#2133,.T.);
#4446=EDGE_CURVE('',#3450,#3450,#2834,.T.);
#4447=EDGE_CURVE('',#3451,#3445,#505,.T.);
#4448=EDGE_CURVE('',#3325,#3451,#506,.T.);
#4449=EDGE_CURVE('',#3448,#3383,#507,.T.);
#4450=EDGE_CURVE('',#3452,#3446,#508,.T.);
#4451=EDGE_CURVE('',#3451,#3452,#2835,.T.);
#4452=EDGE_CURVE('',#3384,#3449,#509,.T.);
#4453=EDGE_CURVE('',#3452,#3326,#510,.T.);
#4454=EDGE_CURVE('',#3453,#3454,#2134,.T.);
#4455=EDGE_CURVE('',#3453,#3455,#2135,.T.);
#4456=EDGE_CURVE('',#3455,#3456,#2136,.T.);
#4457=EDGE_CURVE('',#3454,#3456,#2137,.T.);
#4458=EDGE_CURVE('',#3457,#3453,#2138,.T.);
#4459=EDGE_CURVE('',#3457,#3458,#2139,.T.);
#4460=EDGE_CURVE('',#3458,#3455,#2140,.T.);
#4461=EDGE_CURVE('',#3459,#3457,#2141,.T.);
#4462=EDGE_CURVE('',#3459,#3460,#2142,.T.);
#4463=EDGE_CURVE('',#3460,#3458,#2143,.T.);
#4464=EDGE_CURVE('',#3461,#3459,#2144,.T.);
#4465=EDGE_CURVE('',#3461,#3462,#2145,.T.);
#4466=EDGE_CURVE('',#3462,#3460,#2146,.T.);
#4467=EDGE_CURVE('',#3463,#3461,#2147,.T.);
#4468=EDGE_CURVE('',#3463,#3464,#2148,.T.);
#4469=EDGE_CURVE('',#3464,#3462,#2149,.T.);
#4470=EDGE_CURVE('',#3454,#3463,#2150,.T.);
#4471=EDGE_CURVE('',#3456,#3464,#2151,.T.);
#4472=EDGE_CURVE('',#3465,#3465,#2836,.T.);
#4473=EDGE_CURVE('',#3465,#3466,#2152,.T.);
#4474=EDGE_CURVE('',#3466,#3466,#2837,.T.);
#6037=ORIENTED_EDGE('',*,*,#4259,.F.);
#6038=ORIENTED_EDGE('',*,*,#4260,.T.);
#6039=ORIENTED_EDGE('',*,*,#4261,.T.);
#6040=ORIENTED_EDGE('',*,*,#4262,.T.);
#6041=ORIENTED_EDGE('',*,*,#4263,.F.);
#6042=ORIENTED_EDGE('',*,*,#4264,.T.);
#6043=ORIENTED_EDGE('',*,*,#4259,.T.);
#6044=ORIENTED_EDGE('',*,*,#4265,.T.);
#6045=ORIENTED_EDGE('',*,*,#4266,.F.);
#6046=ORIENTED_EDGE('',*,*,#4267,.T.);
#6047=ORIENTED_EDGE('',*,*,#4263,.T.);
#6048=ORIENTED_EDGE('',*,*,#4268,.T.);
#6049=ORIENTED_EDGE('',*,*,#4269,.F.);
#6050=ORIENTED_EDGE('',*,*,#4270,.T.);
#6051=ORIENTED_EDGE('',*,*,#4266,.T.);
#6052=ORIENTED_EDGE('',*,*,#4271,.T.);
#6053=ORIENTED_EDGE('',*,*,#4272,.F.);
#6054=ORIENTED_EDGE('',*,*,#4273,.T.);
#6055=ORIENTED_EDGE('',*,*,#4269,.T.);
#6056=ORIENTED_EDGE('',*,*,#4274,.T.);
#6057=ORIENTED_EDGE('',*,*,#4275,.F.);
#6058=ORIENTED_EDGE('',*,*,#4276,.T.);
#6059=ORIENTED_EDGE('',*,*,#4272,.T.);
#6060=ORIENTED_EDGE('',*,*,#4277,.T.);
#6061=ORIENTED_EDGE('',*,*,#4278,.F.);
#6062=ORIENTED_EDGE('',*,*,#4279,.T.);
#6063=ORIENTED_EDGE('',*,*,#4275,.T.);
#6064=ORIENTED_EDGE('',*,*,#4280,.T.);
#6065=ORIENTED_EDGE('',*,*,#4281,.F.);
#6066=ORIENTED_EDGE('',*,*,#4282,.T.);
#6067=ORIENTED_EDGE('',*,*,#4278,.T.);
#6068=ORIENTED_EDGE('',*,*,#4283,.T.);
#6069=ORIENTED_EDGE('',*,*,#4284,.F.);
#6070=ORIENTED_EDGE('',*,*,#4285,.T.);
#6071=ORIENTED_EDGE('',*,*,#4281,.T.);
#6072=ORIENTED_EDGE('',*,*,#4286,.T.);
#6073=ORIENTED_EDGE('',*,*,#4287,.F.);
#6074=ORIENTED_EDGE('',*,*,#4288,.T.);
#6075=ORIENTED_EDGE('',*,*,#4284,.T.);
#6076=ORIENTED_EDGE('',*,*,#4289,.T.);
#6077=ORIENTED_EDGE('',*,*,#4290,.F.);
#6078=ORIENTED_EDGE('',*,*,#4291,.T.);
#6079=ORIENTED_EDGE('',*,*,#4287,.T.);
#6080=ORIENTED_EDGE('',*,*,#4292,.T.);
#6081=ORIENTED_EDGE('',*,*,#4293,.F.);
#6082=ORIENTED_EDGE('',*,*,#4294,.T.);
#6083=ORIENTED_EDGE('',*,*,#4290,.T.);
#6084=ORIENTED_EDGE('',*,*,#4295,.T.);
#6085=ORIENTED_EDGE('',*,*,#4296,.F.);
#6086=ORIENTED_EDGE('',*,*,#4297,.T.);
#6087=ORIENTED_EDGE('',*,*,#4293,.T.);
#6088=ORIENTED_EDGE('',*,*,#4298,.T.);
#6089=ORIENTED_EDGE('',*,*,#4299,.F.);
#6090=ORIENTED_EDGE('',*,*,#4300,.T.);
#6091=ORIENTED_EDGE('',*,*,#4296,.T.);
#6092=ORIENTED_EDGE('',*,*,#4301,.T.);
#6093=ORIENTED_EDGE('',*,*,#4302,.F.);
#6094=ORIENTED_EDGE('',*,*,#4303,.T.);
#6095=ORIENTED_EDGE('',*,*,#4299,.T.);
#6096=ORIENTED_EDGE('',*,*,#4304,.T.);
#6097=ORIENTED_EDGE('',*,*,#4305,.F.);
#6098=ORIENTED_EDGE('',*,*,#4306,.T.);
#6099=ORIENTED_EDGE('',*,*,#4302,.T.);
#6100=ORIENTED_EDGE('',*,*,#4307,.T.);
#6101=ORIENTED_EDGE('',*,*,#4308,.F.);
#6102=ORIENTED_EDGE('',*,*,#4309,.T.);
#6103=ORIENTED_EDGE('',*,*,#4305,.T.);
#6104=ORIENTED_EDGE('',*,*,#4310,.T.);
#6105=ORIENTED_EDGE('',*,*,#4311,.F.);
#6106=ORIENTED_EDGE('',*,*,#4312,.T.);
#6107=ORIENTED_EDGE('',*,*,#4308,.T.);
#6108=ORIENTED_EDGE('',*,*,#4313,.T.);
#6109=ORIENTED_EDGE('',*,*,#4314,.F.);
#6110=ORIENTED_EDGE('',*,*,#4315,.T.);
#6111=ORIENTED_EDGE('',*,*,#4311,.T.);
#6112=ORIENTED_EDGE('',*,*,#4316,.T.);
#6113=ORIENTED_EDGE('',*,*,#4317,.F.);
#6114=ORIENTED_EDGE('',*,*,#4318,.T.);
#6115=ORIENTED_EDGE('',*,*,#4314,.T.);
#6116=ORIENTED_EDGE('',*,*,#4319,.T.);
#6117=ORIENTED_EDGE('',*,*,#4320,.F.);
#6118=ORIENTED_EDGE('',*,*,#4321,.T.);
#6119=ORIENTED_EDGE('',*,*,#4317,.T.);
#6120=ORIENTED_EDGE('',*,*,#4322,.T.);
#6121=ORIENTED_EDGE('',*,*,#4323,.F.);
#6122=ORIENTED_EDGE('',*,*,#4324,.T.);
#6123=ORIENTED_EDGE('',*,*,#4320,.T.);
#6124=ORIENTED_EDGE('',*,*,#4325,.T.);
#6125=ORIENTED_EDGE('',*,*,#4326,.F.);
#6126=ORIENTED_EDGE('',*,*,#4327,.T.);
#6127=ORIENTED_EDGE('',*,*,#4323,.T.);
#6128=ORIENTED_EDGE('',*,*,#4328,.T.);
#6129=ORIENTED_EDGE('',*,*,#4329,.F.);
#6130=ORIENTED_EDGE('',*,*,#4330,.T.);
#6131=ORIENTED_EDGE('',*,*,#4326,.T.);
#6132=ORIENTED_EDGE('',*,*,#4331,.T.);
#6133=ORIENTED_EDGE('',*,*,#4332,.F.);
#6134=ORIENTED_EDGE('',*,*,#4333,.T.);
#6135=ORIENTED_EDGE('',*,*,#4329,.T.);
#6136=ORIENTED_EDGE('',*,*,#4334,.T.);
#6137=ORIENTED_EDGE('',*,*,#4335,.F.);
#6138=ORIENTED_EDGE('',*,*,#4336,.T.);
#6139=ORIENTED_EDGE('',*,*,#4332,.T.);
#6140=ORIENTED_EDGE('',*,*,#4337,.T.);
#6141=ORIENTED_EDGE('',*,*,#4338,.F.);
#6142=ORIENTED_EDGE('',*,*,#4339,.T.);
#6143=ORIENTED_EDGE('',*,*,#4335,.T.);
#6144=ORIENTED_EDGE('',*,*,#4340,.T.);
#6145=ORIENTED_EDGE('',*,*,#4341,.F.);
#6146=ORIENTED_EDGE('',*,*,#4342,.T.);
#6147=ORIENTED_EDGE('',*,*,#4338,.T.);
#6148=ORIENTED_EDGE('',*,*,#4343,.T.);
#6149=ORIENTED_EDGE('',*,*,#4344,.F.);
#6150=ORIENTED_EDGE('',*,*,#4345,.T.);
#6151=ORIENTED_EDGE('',*,*,#4341,.T.);
#6152=ORIENTED_EDGE('',*,*,#4346,.T.);
#6153=ORIENTED_EDGE('',*,*,#4347,.F.);
#6154=ORIENTED_EDGE('',*,*,#4348,.T.);
#6155=ORIENTED_EDGE('',*,*,#4344,.T.);
#6156=ORIENTED_EDGE('',*,*,#4349,.T.);
#6157=ORIENTED_EDGE('',*,*,#4350,.F.);
#6158=ORIENTED_EDGE('',*,*,#4351,.T.);
#6159=ORIENTED_EDGE('',*,*,#4352,.T.);
#6160=ORIENTED_EDGE('',*,*,#4353,.F.);
#6161=ORIENTED_EDGE('',*,*,#4354,.F.);
#6162=ORIENTED_EDGE('',*,*,#4355,.T.);
#6163=ORIENTED_EDGE('',*,*,#4350,.T.);
#6164=ORIENTED_EDGE('',*,*,#4356,.F.);
#6165=ORIENTED_EDGE('',*,*,#4357,.F.);
#6166=ORIENTED_EDGE('',*,*,#4358,.T.);
#6167=ORIENTED_EDGE('',*,*,#4354,.T.);
#6168=ORIENTED_EDGE('',*,*,#4359,.F.);
#6169=ORIENTED_EDGE('',*,*,#4360,.F.);
#6170=ORIENTED_EDGE('',*,*,#4361,.T.);
#6171=ORIENTED_EDGE('',*,*,#4357,.T.);
#6172=ORIENTED_EDGE('',*,*,#4362,.F.);
#6173=ORIENTED_EDGE('',*,*,#4363,.F.);
#6174=ORIENTED_EDGE('',*,*,#4364,.T.);
#6175=ORIENTED_EDGE('',*,*,#4360,.T.);
#6176=ORIENTED_EDGE('',*,*,#4365,.F.);
#6177=ORIENTED_EDGE('',*,*,#4366,.F.);
#6178=ORIENTED_EDGE('',*,*,#4367,.T.);
#6179=ORIENTED_EDGE('',*,*,#4363,.T.);
#6180=ORIENTED_EDGE('',*,*,#4368,.F.);
#6181=ORIENTED_EDGE('',*,*,#4369,.F.);
#6182=ORIENTED_EDGE('',*,*,#4370,.T.);
#6183=ORIENTED_EDGE('',*,*,#4366,.T.);
#6184=ORIENTED_EDGE('',*,*,#4371,.F.);
#6185=ORIENTED_EDGE('',*,*,#4372,.F.);
#6186=ORIENTED_EDGE('',*,*,#4373,.T.);
#6187=ORIENTED_EDGE('',*,*,#4369,.T.);
#6188=ORIENTED_EDGE('',*,*,#4374,.F.);
#6189=ORIENTED_EDGE('',*,*,#4375,.F.);
#6190=ORIENTED_EDGE('',*,*,#4376,.T.);
#6191=ORIENTED_EDGE('',*,*,#4372,.T.);
#6192=ORIENTED_EDGE('',*,*,#4377,.F.);
#6193=ORIENTED_EDGE('',*,*,#4378,.F.);
#6194=ORIENTED_EDGE('',*,*,#4379,.T.);
#6195=ORIENTED_EDGE('',*,*,#4375,.T.);
#6196=ORIENTED_EDGE('',*,*,#4380,.F.);
#6197=ORIENTED_EDGE('',*,*,#4381,.F.);
#6198=ORIENTED_EDGE('',*,*,#4382,.T.);
#6199=ORIENTED_EDGE('',*,*,#4378,.T.);
#6200=ORIENTED_EDGE('',*,*,#4383,.F.);
#6201=ORIENTED_EDGE('',*,*,#4384,.F.);
#6202=ORIENTED_EDGE('',*,*,#4385,.T.);
#6203=ORIENTED_EDGE('',*,*,#4381,.T.);
#6204=ORIENTED_EDGE('',*,*,#4386,.F.);
#6205=ORIENTED_EDGE('',*,*,#4387,.F.);
#6206=ORIENTED_EDGE('',*,*,#4388,.T.);
#6207=ORIENTED_EDGE('',*,*,#4384,.T.);
#6208=ORIENTED_EDGE('',*,*,#4389,.F.);
#6209=ORIENTED_EDGE('',*,*,#4390,.F.);
#6210=ORIENTED_EDGE('',*,*,#4391,.T.);
#6211=ORIENTED_EDGE('',*,*,#4387,.T.);
#6212=ORIENTED_EDGE('',*,*,#4392,.F.);
#6213=ORIENTED_EDGE('',*,*,#4393,.F.);
#6214=ORIENTED_EDGE('',*,*,#4394,.T.);
#6215=ORIENTED_EDGE('',*,*,#4390,.T.);
#6216=ORIENTED_EDGE('',*,*,#4395,.F.);
#6217=ORIENTED_EDGE('',*,*,#4396,.F.);
#6218=ORIENTED_EDGE('',*,*,#4397,.T.);
#6219=ORIENTED_EDGE('',*,*,#4393,.T.);
#6220=ORIENTED_EDGE('',*,*,#4398,.F.);
#6221=ORIENTED_EDGE('',*,*,#4399,.F.);
#6222=ORIENTED_EDGE('',*,*,#4400,.T.);
#6223=ORIENTED_EDGE('',*,*,#4396,.T.);
#6224=ORIENTED_EDGE('',*,*,#4401,.F.);
#6225=ORIENTED_EDGE('',*,*,#4402,.F.);
#6226=ORIENTED_EDGE('',*,*,#4403,.T.);
#6227=ORIENTED_EDGE('',*,*,#4399,.T.);
#6228=ORIENTED_EDGE('',*,*,#4404,.F.);
#6229=ORIENTED_EDGE('',*,*,#4405,.F.);
#6230=ORIENTED_EDGE('',*,*,#4406,.T.);
#6231=ORIENTED_EDGE('',*,*,#4402,.T.);
#6232=ORIENTED_EDGE('',*,*,#4407,.F.);
#6233=ORIENTED_EDGE('',*,*,#4408,.F.);
#6234=ORIENTED_EDGE('',*,*,#4409,.T.);
#6235=ORIENTED_EDGE('',*,*,#4405,.T.);
#6236=ORIENTED_EDGE('',*,*,#4410,.F.);
#6237=ORIENTED_EDGE('',*,*,#4411,.F.);
#6238=ORIENTED_EDGE('',*,*,#4412,.T.);
#6239=ORIENTED_EDGE('',*,*,#4408,.T.);
#6240=ORIENTED_EDGE('',*,*,#4413,.F.);
#6241=ORIENTED_EDGE('',*,*,#4414,.F.);
#6242=ORIENTED_EDGE('',*,*,#4415,.T.);
#6243=ORIENTED_EDGE('',*,*,#4411,.T.);
#6244=ORIENTED_EDGE('',*,*,#4416,.F.);
#6245=ORIENTED_EDGE('',*,*,#4417,.F.);
#6246=ORIENTED_EDGE('',*,*,#4418,.T.);
#6247=ORIENTED_EDGE('',*,*,#4414,.T.);
#6248=ORIENTED_EDGE('',*,*,#4419,.F.);
#6249=ORIENTED_EDGE('',*,*,#4420,.F.);
#6250=ORIENTED_EDGE('',*,*,#4421,.T.);
#6251=ORIENTED_EDGE('',*,*,#4417,.T.);
#6252=ORIENTED_EDGE('',*,*,#4422,.F.);
#6253=ORIENTED_EDGE('',*,*,#4423,.F.);
#6254=ORIENTED_EDGE('',*,*,#4424,.T.);
#6255=ORIENTED_EDGE('',*,*,#4420,.T.);
#6256=ORIENTED_EDGE('',*,*,#4425,.F.);
#6257=ORIENTED_EDGE('',*,*,#4426,.F.);
#6258=ORIENTED_EDGE('',*,*,#4427,.T.);
#6259=ORIENTED_EDGE('',*,*,#4423,.T.);
#6260=ORIENTED_EDGE('',*,*,#4428,.F.);
#6261=ORIENTED_EDGE('',*,*,#4429,.F.);
#6262=ORIENTED_EDGE('',*,*,#4430,.T.);
#6263=ORIENTED_EDGE('',*,*,#4426,.T.);
#6264=ORIENTED_EDGE('',*,*,#4431,.F.);
#6265=ORIENTED_EDGE('',*,*,#4432,.F.);
#6266=ORIENTED_EDGE('',*,*,#4433,.T.);
#6267=ORIENTED_EDGE('',*,*,#4429,.T.);
#6268=ORIENTED_EDGE('',*,*,#4434,.F.);
#6269=ORIENTED_EDGE('',*,*,#4435,.F.);
#6270=ORIENTED_EDGE('',*,*,#4436,.T.);
#6271=ORIENTED_EDGE('',*,*,#4432,.T.);
#6272=ORIENTED_EDGE('',*,*,#4437,.F.);
#6273=ORIENTED_EDGE('',*,*,#4438,.F.);
#6274=ORIENTED_EDGE('',*,*,#4439,.T.);
#6275=ORIENTED_EDGE('',*,*,#4435,.T.);
#6276=ORIENTED_EDGE('',*,*,#4440,.F.);
#6277=ORIENTED_EDGE('',*,*,#4441,.F.);
#6278=ORIENTED_EDGE('',*,*,#4352,.F.);
#6279=ORIENTED_EDGE('',*,*,#4442,.F.);
#6280=ORIENTED_EDGE('',*,*,#4443,.F.);
#6281=ORIENTED_EDGE('',*,*,#4444,.F.);
#6282=ORIENTED_EDGE('',*,*,#4445,.T.);
#6283=ORIENTED_EDGE('',*,*,#4446,.F.);
#6284=ORIENTED_EDGE('',*,*,#4445,.F.);
#6285=ORIENTED_EDGE('',*,*,#4442,.T.);
#6286=ORIENTED_EDGE('',*,*,#4351,.F.);
#6287=ORIENTED_EDGE('',*,*,#4355,.F.);
#6288=ORIENTED_EDGE('',*,*,#4358,.F.);
#6289=ORIENTED_EDGE('',*,*,#4361,.F.);
#6290=ORIENTED_EDGE('',*,*,#4364,.F.);
#6291=ORIENTED_EDGE('',*,*,#4367,.F.);
#6292=ORIENTED_EDGE('',*,*,#4370,.F.);
#6293=ORIENTED_EDGE('',*,*,#4373,.F.);
#6294=ORIENTED_EDGE('',*,*,#4376,.F.);
#6295=ORIENTED_EDGE('',*,*,#4379,.F.);
#6296=ORIENTED_EDGE('',*,*,#4382,.F.);
#6297=ORIENTED_EDGE('',*,*,#4385,.F.);
#6298=ORIENTED_EDGE('',*,*,#4388,.F.);
#6299=ORIENTED_EDGE('',*,*,#4391,.F.);
#6300=ORIENTED_EDGE('',*,*,#4394,.F.);
#6301=ORIENTED_EDGE('',*,*,#4397,.F.);
#6302=ORIENTED_EDGE('',*,*,#4400,.F.);
#6303=ORIENTED_EDGE('',*,*,#4403,.F.);
#6304=ORIENTED_EDGE('',*,*,#4406,.F.);
#6305=ORIENTED_EDGE('',*,*,#4409,.F.);
#6306=ORIENTED_EDGE('',*,*,#4412,.F.);
#6307=ORIENTED_EDGE('',*,*,#4415,.F.);
#6308=ORIENTED_EDGE('',*,*,#4418,.F.);
#6309=ORIENTED_EDGE('',*,*,#4421,.F.);
#6310=ORIENTED_EDGE('',*,*,#4424,.F.);
#6311=ORIENTED_EDGE('',*,*,#4427,.F.);
#6312=ORIENTED_EDGE('',*,*,#4430,.F.);
#6313=ORIENTED_EDGE('',*,*,#4433,.F.);
#6314=ORIENTED_EDGE('',*,*,#4436,.F.);
#6315=ORIENTED_EDGE('',*,*,#4439,.F.);
#6316=ORIENTED_EDGE('',*,*,#4447,.F.);
#6317=ORIENTED_EDGE('',*,*,#4448,.F.);
#6318=ORIENTED_EDGE('',*,*,#4260,.F.);
#6319=ORIENTED_EDGE('',*,*,#4264,.F.);
#6320=ORIENTED_EDGE('',*,*,#4267,.F.);
#6321=ORIENTED_EDGE('',*,*,#4270,.F.);
#6322=ORIENTED_EDGE('',*,*,#4273,.F.);
#6323=ORIENTED_EDGE('',*,*,#4276,.F.);
#6324=ORIENTED_EDGE('',*,*,#4279,.F.);
#6325=ORIENTED_EDGE('',*,*,#4282,.F.);
#6326=ORIENTED_EDGE('',*,*,#4285,.F.);
#6327=ORIENTED_EDGE('',*,*,#4288,.F.);
#6328=ORIENTED_EDGE('',*,*,#4291,.F.);
#6329=ORIENTED_EDGE('',*,*,#4294,.F.);
#6330=ORIENTED_EDGE('',*,*,#4297,.F.);
#6331=ORIENTED_EDGE('',*,*,#4300,.F.);
#6332=ORIENTED_EDGE('',*,*,#4303,.F.);
#6333=ORIENTED_EDGE('',*,*,#4306,.F.);
#6334=ORIENTED_EDGE('',*,*,#4309,.F.);
#6335=ORIENTED_EDGE('',*,*,#4312,.F.);
#6336=ORIENTED_EDGE('',*,*,#4315,.F.);
#6337=ORIENTED_EDGE('',*,*,#4318,.F.);
#6338=ORIENTED_EDGE('',*,*,#4321,.F.);
#6339=ORIENTED_EDGE('',*,*,#4324,.F.);
#6340=ORIENTED_EDGE('',*,*,#4327,.F.);
#6341=ORIENTED_EDGE('',*,*,#4330,.F.);
#6342=ORIENTED_EDGE('',*,*,#4333,.F.);
#6343=ORIENTED_EDGE('',*,*,#4336,.F.);
#6344=ORIENTED_EDGE('',*,*,#4339,.F.);
#6345=ORIENTED_EDGE('',*,*,#4342,.F.);
#6346=ORIENTED_EDGE('',*,*,#4345,.F.);
#6347=ORIENTED_EDGE('',*,*,#4348,.F.);
#6348=ORIENTED_EDGE('',*,*,#4449,.F.);
#6349=ORIENTED_EDGE('',*,*,#4438,.T.);
#6350=ORIENTED_EDGE('',*,*,#4450,.F.);
#6351=ORIENTED_EDGE('',*,*,#4451,.F.);
#6352=ORIENTED_EDGE('',*,*,#4447,.T.);
#6353=ORIENTED_EDGE('',*,*,#4441,.T.);
#6354=ORIENTED_EDGE('',*,*,#4444,.T.);
#6355=ORIENTED_EDGE('',*,*,#4452,.F.);
#6356=ORIENTED_EDGE('',*,*,#4349,.F.);
#6357=ORIENTED_EDGE('',*,*,#4346,.F.);
#6358=ORIENTED_EDGE('',*,*,#4343,.F.);
#6359=ORIENTED_EDGE('',*,*,#4340,.F.);
#6360=ORIENTED_EDGE('',*,*,#4337,.F.);
#6361=ORIENTED_EDGE('',*,*,#4334,.F.);
#6362=ORIENTED_EDGE('',*,*,#4331,.F.);
#6363=ORIENTED_EDGE('',*,*,#4328,.F.);
#6364=ORIENTED_EDGE('',*,*,#4325,.F.);
#6365=ORIENTED_EDGE('',*,*,#4322,.F.);
#6366=ORIENTED_EDGE('',*,*,#4319,.F.);
#6367=ORIENTED_EDGE('',*,*,#4316,.F.);
#6368=ORIENTED_EDGE('',*,*,#4313,.F.);
#6369=ORIENTED_EDGE('',*,*,#4310,.F.);
#6370=ORIENTED_EDGE('',*,*,#4307,.F.);
#6371=ORIENTED_EDGE('',*,*,#4304,.F.);
#6372=ORIENTED_EDGE('',*,*,#4301,.F.);
#6373=ORIENTED_EDGE('',*,*,#4298,.F.);
#6374=ORIENTED_EDGE('',*,*,#4295,.F.);
#6375=ORIENTED_EDGE('',*,*,#4292,.F.);
#6376=ORIENTED_EDGE('',*,*,#4289,.F.);
#6377=ORIENTED_EDGE('',*,*,#4286,.F.);
#6378=ORIENTED_EDGE('',*,*,#4283,.F.);
#6379=ORIENTED_EDGE('',*,*,#4280,.F.);
#6380=ORIENTED_EDGE('',*,*,#4277,.F.);
#6381=ORIENTED_EDGE('',*,*,#4274,.F.);
#6382=ORIENTED_EDGE('',*,*,#4271,.F.);
#6383=ORIENTED_EDGE('',*,*,#4268,.F.);
#6384=ORIENTED_EDGE('',*,*,#4265,.F.);
#6385=ORIENTED_EDGE('',*,*,#4262,.F.);
#6386=ORIENTED_EDGE('',*,*,#4453,.F.);
#6387=ORIENTED_EDGE('',*,*,#4450,.T.);
#6388=ORIENTED_EDGE('',*,*,#4440,.T.);
#6389=ORIENTED_EDGE('',*,*,#4437,.T.);
#6390=ORIENTED_EDGE('',*,*,#4434,.T.);
#6391=ORIENTED_EDGE('',*,*,#4431,.T.);
#6392=ORIENTED_EDGE('',*,*,#4428,.T.);
#6393=ORIENTED_EDGE('',*,*,#4425,.T.);
#6394=ORIENTED_EDGE('',*,*,#4422,.T.);
#6395=ORIENTED_EDGE('',*,*,#4419,.T.);
#6396=ORIENTED_EDGE('',*,*,#4416,.T.);
#6397=ORIENTED_EDGE('',*,*,#4413,.T.);
#6398=ORIENTED_EDGE('',*,*,#4410,.T.);
#6399=ORIENTED_EDGE('',*,*,#4407,.T.);
#6400=ORIENTED_EDGE('',*,*,#4404,.T.);
#6401=ORIENTED_EDGE('',*,*,#4401,.T.);
#6402=ORIENTED_EDGE('',*,*,#4398,.T.);
#6403=ORIENTED_EDGE('',*,*,#4395,.T.);
#6404=ORIENTED_EDGE('',*,*,#4392,.T.);
#6405=ORIENTED_EDGE('',*,*,#4389,.T.);
#6406=ORIENTED_EDGE('',*,*,#4386,.T.);
#6407=ORIENTED_EDGE('',*,*,#4383,.T.);
#6408=ORIENTED_EDGE('',*,*,#4380,.T.);
#6409=ORIENTED_EDGE('',*,*,#4377,.T.);
#6410=ORIENTED_EDGE('',*,*,#4374,.T.);
#6411=ORIENTED_EDGE('',*,*,#4371,.T.);
#6412=ORIENTED_EDGE('',*,*,#4368,.T.);
#6413=ORIENTED_EDGE('',*,*,#4365,.T.);
#6414=ORIENTED_EDGE('',*,*,#4362,.T.);
#6415=ORIENTED_EDGE('',*,*,#4359,.T.);
#6416=ORIENTED_EDGE('',*,*,#4356,.T.);
#6417=ORIENTED_EDGE('',*,*,#4353,.T.);
#6418=ORIENTED_EDGE('',*,*,#4347,.T.);
#6419=ORIENTED_EDGE('',*,*,#4452,.T.);
#6420=ORIENTED_EDGE('',*,*,#4443,.T.);
#6421=ORIENTED_EDGE('',*,*,#4449,.T.);
#6422=ORIENTED_EDGE('',*,*,#4454,.F.);
#6423=ORIENTED_EDGE('',*,*,#4455,.T.);
#6424=ORIENTED_EDGE('',*,*,#4456,.T.);
#6425=ORIENTED_EDGE('',*,*,#4457,.F.);
#6426=ORIENTED_EDGE('',*,*,#4458,.F.);
#6427=ORIENTED_EDGE('',*,*,#4459,.T.);
#6428=ORIENTED_EDGE('',*,*,#4460,.T.);
#6429=ORIENTED_EDGE('',*,*,#4455,.F.);
#6430=ORIENTED_EDGE('',*,*,#4461,.F.);
#6431=ORIENTED_EDGE('',*,*,#4462,.T.);
#6432=ORIENTED_EDGE('',*,*,#4463,.T.);
#6433=ORIENTED_EDGE('',*,*,#4459,.F.);
#6434=ORIENTED_EDGE('',*,*,#4464,.F.);
#6435=ORIENTED_EDGE('',*,*,#4465,.T.);
#6436=ORIENTED_EDGE('',*,*,#4466,.T.);
#6437=ORIENTED_EDGE('',*,*,#4462,.F.);
#6438=ORIENTED_EDGE('',*,*,#4467,.F.);
#6439=ORIENTED_EDGE('',*,*,#4468,.T.);
#6440=ORIENTED_EDGE('',*,*,#4469,.T.);
#6441=ORIENTED_EDGE('',*,*,#4465,.F.);
#6442=ORIENTED_EDGE('',*,*,#4470,.F.);
#6443=ORIENTED_EDGE('',*,*,#4457,.T.);
#6444=ORIENTED_EDGE('',*,*,#4471,.T.);
#6445=ORIENTED_EDGE('',*,*,#4468,.F.);
#6446=ORIENTED_EDGE('',*,*,#4471,.F.);
#6447=ORIENTED_EDGE('',*,*,#4456,.F.);
#6448=ORIENTED_EDGE('',*,*,#4460,.F.);
#6449=ORIENTED_EDGE('',*,*,#4463,.F.);
#6450=ORIENTED_EDGE('',*,*,#4466,.F.);
#6451=ORIENTED_EDGE('',*,*,#4469,.F.);
#6452=ORIENTED_EDGE('',*,*,#4472,.T.);
#6453=ORIENTED_EDGE('',*,*,#4448,.T.);
#6454=ORIENTED_EDGE('',*,*,#4451,.T.);
#6455=ORIENTED_EDGE('',*,*,#4453,.T.);
#6456=ORIENTED_EDGE('',*,*,#4261,.F.);
#6457=ORIENTED_EDGE('',*,*,#4472,.F.);
#6458=ORIENTED_EDGE('',*,*,#4473,.T.);
#6459=ORIENTED_EDGE('',*,*,#4474,.T.);
#6460=ORIENTED_EDGE('',*,*,#4473,.F.);
#6461=ORIENTED_EDGE('',*,*,#4474,.F.);
#6462=ORIENTED_EDGE('',*,*,#4454,.T.);
#6463=ORIENTED_EDGE('',*,*,#4470,.T.);
#6464=ORIENTED_EDGE('',*,*,#4467,.T.);
#6465=ORIENTED_EDGE('',*,*,#4464,.T.);
#6466=ORIENTED_EDGE('',*,*,#4461,.T.);
#6467=ORIENTED_EDGE('',*,*,#4458,.T.);
#6468=ORIENTED_EDGE('',*,*,#4446,.T.);
#6665=CYLINDRICAL_SURFACE('',#7687,0.14635);
#6666=CYLINDRICAL_SURFACE('',#7689,0.14635);
#6667=CYLINDRICAL_SURFACE('',#7690,0.14635);
#6668=CYLINDRICAL_SURFACE('',#7691,0.14635);
#6669=CYLINDRICAL_SURFACE('',#7692,0.14635);
#6670=CYLINDRICAL_SURFACE('',#7693,0.14635);
#6671=CYLINDRICAL_SURFACE('',#7694,0.14635);
#6672=CYLINDRICAL_SURFACE('',#7695,0.14635);
#6673=CYLINDRICAL_SURFACE('',#7696,0.14635);
#6674=CYLINDRICAL_SURFACE('',#7697,0.14635);
#6675=CYLINDRICAL_SURFACE('',#7698,0.14635);
#6676=CYLINDRICAL_SURFACE('',#7699,0.14635);
#6677=CYLINDRICAL_SURFACE('',#7700,0.14635);
#6678=CYLINDRICAL_SURFACE('',#7701,0.14635);
#6679=CYLINDRICAL_SURFACE('',#7702,0.14635);
#6680=CYLINDRICAL_SURFACE('',#7703,0.14635);
#6681=CYLINDRICAL_SURFACE('',#7704,0.14635);
#6682=CYLINDRICAL_SURFACE('',#7705,0.14635);
#6683=CYLINDRICAL_SURFACE('',#7706,0.14635);
#6684=CYLINDRICAL_SURFACE('',#7707,0.14635);
#6685=CYLINDRICAL_SURFACE('',#7708,0.14635);
#6686=CYLINDRICAL_SURFACE('',#7709,0.14635);
#6687=CYLINDRICAL_SURFACE('',#7710,0.14635);
#6688=CYLINDRICAL_SURFACE('',#7711,0.14635);
#6689=CYLINDRICAL_SURFACE('',#7712,0.14635);
#6690=CYLINDRICAL_SURFACE('',#7713,0.14635);
#6691=CYLINDRICAL_SURFACE('',#7714,0.14635);
#6692=CYLINDRICAL_SURFACE('',#7715,0.14635);
#6693=CYLINDRICAL_SURFACE('',#7716,0.14635);
#6694=CYLINDRICAL_SURFACE('',#7717,0.14635);
#6695=CYLINDRICAL_SURFACE('',#7718,0.117775);
#6696=CYLINDRICAL_SURFACE('',#7720,0.117775);
#6697=CYLINDRICAL_SURFACE('',#7721,0.117775);
#6698=CYLINDRICAL_SURFACE('',#7722,0.117775);
#6699=CYLINDRICAL_SURFACE('',#7723,0.117775);
#6700=CYLINDRICAL_SURFACE('',#7724,0.117775);
#6701=CYLINDRICAL_SURFACE('',#7725,0.117775);
#6702=CYLINDRICAL_SURFACE('',#7726,0.117775);
#6703=CYLINDRICAL_SURFACE('',#7727,0.117775);
#6704=CYLINDRICAL_SURFACE('',#7728,0.117775);
#6705=CYLINDRICAL_SURFACE('',#7729,0.117775);
#6706=CYLINDRICAL_SURFACE('',#7730,0.117775);
#6707=CYLINDRICAL_SURFACE('',#7731,0.117775);
#6708=CYLINDRICAL_SURFACE('',#7732,0.117775);
#6709=CYLINDRICAL_SURFACE('',#7733,0.117775);
#6710=CYLINDRICAL_SURFACE('',#7734,0.117775);
#6711=CYLINDRICAL_SURFACE('',#7735,0.117775);
#6712=CYLINDRICAL_SURFACE('',#7736,0.117775);
#6713=CYLINDRICAL_SURFACE('',#7737,0.117775);
#6714=CYLINDRICAL_SURFACE('',#7738,0.117775);
#6715=CYLINDRICAL_SURFACE('',#7739,0.117775);
#6716=CYLINDRICAL_SURFACE('',#7740,0.117775);
#6717=CYLINDRICAL_SURFACE('',#7741,0.117775);
#6718=CYLINDRICAL_SURFACE('',#7742,0.117775);
#6719=CYLINDRICAL_SURFACE('',#7743,0.117775);
#6720=CYLINDRICAL_SURFACE('',#7744,0.117775);
#6721=CYLINDRICAL_SURFACE('',#7745,0.117775);
#6722=CYLINDRICAL_SURFACE('',#7746,0.117775);
#6723=CYLINDRICAL_SURFACE('',#7747,0.117775);
#6724=CYLINDRICAL_SURFACE('',#7748,0.117775);
#6725=CYLINDRICAL_SURFACE('',#7752,0.117775);
#6726=CYLINDRICAL_SURFACE('',#7754,0.14635);
#6727=CYLINDRICAL_SURFACE('',#7764,0.275);
#7049=ADVANCED_FACE('',(#1127),#6665,.T.);
#7050=ADVANCED_FACE('',(#1128),#6666,.T.);
#7051=ADVANCED_FACE('',(#1129),#6667,.T.);
#7052=ADVANCED_FACE('',(#1130),#6668,.T.);
#7053=ADVANCED_FACE('',(#1131),#6669,.T.);
#7054=ADVANCED_FACE('',(#1132),#6670,.T.);
#7055=ADVANCED_FACE('',(#1133),#6671,.T.);
#7056=ADVANCED_FACE('',(#1134),#6672,.T.);
#7057=ADVANCED_FACE('',(#1135),#6673,.T.);
#7058=ADVANCED_FACE('',(#1136),#6674,.T.);
#7059=ADVANCED_FACE('',(#1137),#6675,.T.);
#7060=ADVANCED_FACE('',(#1138),#6676,.T.);
#7061=ADVANCED_FACE('',(#1139),#6677,.T.);
#7062=ADVANCED_FACE('',(#1140),#6678,.T.);
#7063=ADVANCED_FACE('',(#1141),#6679,.T.);
#7064=ADVANCED_FACE('',(#1142),#6680,.T.);
#7065=ADVANCED_FACE('',(#1143),#6681,.T.);
#7066=ADVANCED_FACE('',(#1144),#6682,.T.);
#7067=ADVANCED_FACE('',(#1145),#6683,.T.);
#7068=ADVANCED_FACE('',(#1146),#6684,.T.);
#7069=ADVANCED_FACE('',(#1147),#6685,.T.);
#7070=ADVANCED_FACE('',(#1148),#6686,.T.);
#7071=ADVANCED_FACE('',(#1149),#6687,.T.);
#7072=ADVANCED_FACE('',(#1150),#6688,.T.);
#7073=ADVANCED_FACE('',(#1151),#6689,.T.);
#7074=ADVANCED_FACE('',(#1152),#6690,.T.);
#7075=ADVANCED_FACE('',(#1153),#6691,.T.);
#7076=ADVANCED_FACE('',(#1154),#6692,.T.);
#7077=ADVANCED_FACE('',(#1155),#6693,.T.);
#7078=ADVANCED_FACE('',(#1156),#6694,.T.);
#7079=ADVANCED_FACE('',(#1157),#6695,.T.);
#7080=ADVANCED_FACE('',(#1158),#6696,.T.);
#7081=ADVANCED_FACE('',(#1159),#6697,.T.);
#7082=ADVANCED_FACE('',(#1160),#6698,.T.);
#7083=ADVANCED_FACE('',(#1161),#6699,.T.);
#7084=ADVANCED_FACE('',(#1162),#6700,.T.);
#7085=ADVANCED_FACE('',(#1163),#6701,.T.);
#7086=ADVANCED_FACE('',(#1164),#6702,.T.);
#7087=ADVANCED_FACE('',(#1165),#6703,.T.);
#7088=ADVANCED_FACE('',(#1166),#6704,.T.);
#7089=ADVANCED_FACE('',(#1167),#6705,.T.);
#7090=ADVANCED_FACE('',(#1168),#6706,.T.);
#7091=ADVANCED_FACE('',(#1169),#6707,.T.);
#7092=ADVANCED_FACE('',(#1170),#6708,.T.);
#7093=ADVANCED_FACE('',(#1171),#6709,.T.);
#7094=ADVANCED_FACE('',(#1172),#6710,.T.);
#7095=ADVANCED_FACE('',(#1173),#6711,.T.);
#7096=ADVANCED_FACE('',(#1174),#6712,.T.);
#7097=ADVANCED_FACE('',(#1175),#6713,.T.);
#7098=ADVANCED_FACE('',(#1176),#6714,.T.);
#7099=ADVANCED_FACE('',(#1177),#6715,.T.);
#7100=ADVANCED_FACE('',(#1178),#6716,.T.);
#7101=ADVANCED_FACE('',(#1179),#6717,.T.);
#7102=ADVANCED_FACE('',(#1180),#6718,.T.);
#7103=ADVANCED_FACE('',(#1181),#6719,.T.);
#7104=ADVANCED_FACE('',(#1182),#6720,.T.);
#7105=ADVANCED_FACE('',(#1183),#6721,.T.);
#7106=ADVANCED_FACE('',(#1184),#6722,.T.);
#7107=ADVANCED_FACE('',(#1185),#6723,.T.);
#7108=ADVANCED_FACE('',(#1186),#6724,.T.);
#7109=ADVANCED_FACE('',(#1187),#75,.T.);
#7110=ADVANCED_FACE('',(#1188),#168,.F.);
#7111=ADVANCED_FACE('',(#1189),#6725,.T.);
#7112=ADVANCED_FACE('',(#1190),#169,.F.);
#7113=ADVANCED_FACE('',(#1191),#6726,.T.);
#7114=ADVANCED_FACE('',(#1192),#800,.F.);
#7115=ADVANCED_FACE('',(#1193),#801,.F.);
#7116=ADVANCED_FACE('',(#1194),#802,.F.);
#7117=ADVANCED_FACE('',(#1195),#803,.F.);
#7118=ADVANCED_FACE('',(#1196),#804,.F.);
#7119=ADVANCED_FACE('',(#1197),#805,.F.);
#7120=ADVANCED_FACE('',(#1198),#806,.F.);
#7121=ADVANCED_FACE('',(#1199,#647),#807,.T.);
#7122=ADVANCED_FACE('',(#1200),#6727,.T.);
#7123=ADVANCED_FACE('',(#1201,#648),#808,.F.);
#7124=ADVANCED_FACE('',(#1202),#809,.T.);
#7158=CLOSED_SHELL('',(#7049,#7050,#7051,#7052,#7053,#7054,#7055,#7056,
#7057,#7058,#7059,#7060,#7061,#7062,#7063,#7064,#7065,#7066,#7067,#7068,
#7069,#7070,#7071,#7072,#7073,#7074,#7075,#7076,#7077,#7078,#7079,#7080,
#7081,#7082,#7083,#7084,#7085,#7086,#7087,#7088,#7089,#7090,#7091,#7092,
#7093,#7094,#7095,#7096,#7097,#7098,#7099,#7100,#7101,#7102,#7103,#7104,
#7105,#7106,#7107,#7108,#7109,#7110,#7111,#7112,#7113,#7114,#7115,#7116,
#7117,#7118,#7119,#7120,#7121,#7122,#7123,#7124));
#7686=AXIS2_PLACEMENT_3D('',#14337,#9011,#9012);
#7687=AXIS2_PLACEMENT_3D('',#14338,#9013,#9014);
#7688=AXIS2_PLACEMENT_3D('',#14354,#9016,#9017);
#7689=AXIS2_PLACEMENT_3D('',#14362,#9018,#9019);
#7690=AXIS2_PLACEMENT_3D('',#14410,#9021,#9022);
#7691=AXIS2_PLACEMENT_3D('',#14458,#9024,#9025);
#7692=AXIS2_PLACEMENT_3D('',#14509,#9027,#9028);
#7693=AXIS2_PLACEMENT_3D('',#14557,#9030,#9031);
#7694=AXIS2_PLACEMENT_3D('',#14605,#9033,#9034);
#7695=AXIS2_PLACEMENT_3D('',#14653,#9036,#9037);
#7696=AXIS2_PLACEMENT_3D('',#14707,#9039,#9040);
#7697=AXIS2_PLACEMENT_3D('',#14755,#9042,#9043);
#7698=AXIS2_PLACEMENT_3D('',#14803,#9045,#9046);
#7699=AXIS2_PLACEMENT_3D('',#14857,#9048,#9049);
#7700=AXIS2_PLACEMENT_3D('',#14905,#9051,#9052);
#7701=AXIS2_PLACEMENT_3D('',#14953,#9054,#9055);
#7702=AXIS2_PLACEMENT_3D('',#15001,#9057,#9058);
#7703=AXIS2_PLACEMENT_3D('',#15055,#9060,#9061);
#7704=AXIS2_PLACEMENT_3D('',#15103,#9063,#9064);
#7705=AXIS2_PLACEMENT_3D('',#15151,#9066,#9067);
#7706=AXIS2_PLACEMENT_3D('',#15205,#9069,#9070);
#7707=AXIS2_PLACEMENT_3D('',#15253,#9072,#9073);
#7708=AXIS2_PLACEMENT_3D('',#15301,#9075,#9076);
#7709=AXIS2_PLACEMENT_3D('',#15355,#9078,#9079);
#7710=AXIS2_PLACEMENT_3D('',#15403,#9081,#9082);
#7711=AXIS2_PLACEMENT_3D('',#15451,#9084,#9085);
#7712=AXIS2_PLACEMENT_3D('',#15499,#9087,#9088);
#7713=AXIS2_PLACEMENT_3D('',#15553,#9090,#9091);
#7714=AXIS2_PLACEMENT_3D('',#15601,#9093,#9094);
#7715=AXIS2_PLACEMENT_3D('',#15649,#9096,#9097);
#7716=AXIS2_PLACEMENT_3D('',#15703,#9099,#9100);
#7717=AXIS2_PLACEMENT_3D('',#15751,#9102,#9103);
#7718=AXIS2_PLACEMENT_3D('',#15799,#9105,#9106);
#7719=AXIS2_PLACEMENT_3D('',#15815,#9108,#9109);
#7720=AXIS2_PLACEMENT_3D('',#15825,#9110,#9111);
#7721=AXIS2_PLACEMENT_3D('',#15849,#9113,#9114);
#7722=AXIS2_PLACEMENT_3D('',#15873,#9116,#9117);
#7723=AXIS2_PLACEMENT_3D('',#15898,#9119,#9120);
#7724=AXIS2_PLACEMENT_3D('',#15923,#9122,#9123);
#7725=AXIS2_PLACEMENT_3D('',#15947,#9125,#9126);
#7726=AXIS2_PLACEMENT_3D('',#15972,#9128,#9129);
#7727=AXIS2_PLACEMENT_3D('',#15997,#9131,#9132);
#7728=AXIS2_PLACEMENT_3D('',#16021,#9134,#9135);
#7729=AXIS2_PLACEMENT_3D('',#16045,#9137,#9138);
#7730=AXIS2_PLACEMENT_3D('',#16070,#9140,#9141);
#7731=AXIS2_PLACEMENT_3D('',#16095,#9143,#9144);
#7732=AXIS2_PLACEMENT_3D('',#16119,#9146,#9147);
#7733=AXIS2_PLACEMENT_3D('',#16144,#9149,#9150);
#7734=AXIS2_PLACEMENT_3D('',#16169,#9152,#9153);
#7735=AXIS2_PLACEMENT_3D('',#16193,#9155,#9156);
#7736=AXIS2_PLACEMENT_3D('',#16218,#9158,#9159);
#7737=AXIS2_PLACEMENT_3D('',#16243,#9161,#9162);
#7738=AXIS2_PLACEMENT_3D('',#16267,#9164,#9165);
#7739=AXIS2_PLACEMENT_3D('',#16291,#9167,#9168);
#7740=AXIS2_PLACEMENT_3D('',#16316,#9170,#9171);
#7741=AXIS2_PLACEMENT_3D('',#16341,#9173,#9174);
#7742=AXIS2_PLACEMENT_3D('',#16365,#9176,#9177);
#7743=AXIS2_PLACEMENT_3D('',#16390,#9179,#9180);
#7744=AXIS2_PLACEMENT_3D('',#16415,#9182,#9183);
#7745=AXIS2_PLACEMENT_3D('',#16439,#9185,#9186);
#7746=AXIS2_PLACEMENT_3D('',#16464,#9188,#9189);
#7747=AXIS2_PLACEMENT_3D('',#16488,#9191,#9192);
#7748=AXIS2_PLACEMENT_3D('',#16513,#9194,#9195);
#7749=AXIS2_PLACEMENT_3D('',#16537,#9197,#9198);
#7750=AXIS2_PLACEMENT_3D('',#16699,#9199,#9200);
#7751=AXIS2_PLACEMENT_3D('',#16718,#9202,#9203);
#7752=AXIS2_PLACEMENT_3D('',#17580,#9204,#9205);
#7753=AXIS2_PLACEMENT_3D('',#17591,#9206,#9207);
#7754=AXIS2_PLACEMENT_3D('',#18458,#9208,#9209);
#7755=AXIS2_PLACEMENT_3D('',#18459,#9210,#9211);
#7756=AXIS2_PLACEMENT_3D('',#18468,#9216,#9217);
#7757=AXIS2_PLACEMENT_3D('',#18474,#9221,#9222);
#7758=AXIS2_PLACEMENT_3D('',#18480,#9226,#9227);
#7759=AXIS2_PLACEMENT_3D('',#18486,#9231,#9232);
#7760=AXIS2_PLACEMENT_3D('',#18492,#9236,#9237);
#7761=AXIS2_PLACEMENT_3D('',#18495,#9240,#9241);
#7762=AXIS2_PLACEMENT_3D('',#18496,#9242,#9243);
#7763=AXIS2_PLACEMENT_3D('',#18498,#9244,#9245);
#7764=AXIS2_PLACEMENT_3D('',#18499,#9246,#9247);
#7765=AXIS2_PLACEMENT_3D('',#18502,#9249,#9250);
#7766=AXIS2_PLACEMENT_3D('',#18503,#9251,#9252);
#7767=AXIS2_PLACEMENT_3D('',#18504,#9253,#9254);
#9011=DIRECTION('axis',(0.,0.,1.));
#9012=DIRECTION('refdir',(1.,0.,0.));
#9013=DIRECTION('center_axis',(0.,0.,1.));
#9014=DIRECTION('ref_axis',(1.,0.,0.));
#9015=DIRECTION('',(0.,0.,-1.));
#9016=DIRECTION('center_axis',(0.,0.,-1.));
#9017=DIRECTION('ref_axis',(1.,0.,0.));
#9018=DIRECTION('center_axis',(0.,0.,1.));
#9019=DIRECTION('ref_axis',(1.,0.,0.));
#9020=DIRECTION('',(0.,0.,-1.));
#9021=DIRECTION('center_axis',(0.,0.,1.));
#9022=DIRECTION('ref_axis',(1.,0.,0.));
#9023=DIRECTION('',(0.,0.,-1.));
#9024=DIRECTION('center_axis',(0.,0.,1.));
#9025=DIRECTION('ref_axis',(1.,0.,0.));
#9026=DIRECTION('',(0.,0.,-1.));
#9027=DIRECTION('center_axis',(0.,0.,1.));
#9028=DIRECTION('ref_axis',(1.,0.,0.));
#9029=DIRECTION('',(0.,0.,-1.));
#9030=DIRECTION('center_axis',(0.,0.,1.));
#9031=DIRECTION('ref_axis',(1.,0.,0.));
#9032=DIRECTION('',(0.,0.,-1.));
#9033=DIRECTION('center_axis',(0.,0.,1.));
#9034=DIRECTION('ref_axis',(1.,0.,0.));
#9035=DIRECTION('',(0.,0.,-1.));
#9036=DIRECTION('center_axis',(0.,0.,1.));
#9037=DIRECTION('ref_axis',(1.,0.,0.));
#9038=DIRECTION('',(0.,0.,-1.));
#9039=DIRECTION('center_axis',(0.,0.,1.));
#9040=DIRECTION('ref_axis',(1.,0.,0.));
#9041=DIRECTION('',(0.,0.,-1.));
#9042=DIRECTION('center_axis',(0.,0.,1.));
#9043=DIRECTION('ref_axis',(1.,0.,0.));
#9044=DIRECTION('',(0.,0.,-1.));
#9045=DIRECTION('center_axis',(0.,0.,1.));
#9046=DIRECTION('ref_axis',(1.,0.,0.));
#9047=DIRECTION('',(0.,0.,-1.));
#9048=DIRECTION('center_axis',(0.,0.,1.));
#9049=DIRECTION('ref_axis',(1.,0.,0.));
#9050=DIRECTION('',(0.,0.,-1.));
#9051=DIRECTION('center_axis',(0.,0.,1.));
#9052=DIRECTION('ref_axis',(1.,0.,0.));
#9053=DIRECTION('',(0.,0.,-1.));
#9054=DIRECTION('center_axis',(0.,0.,1.));
#9055=DIRECTION('ref_axis',(1.,0.,0.));
#9056=DIRECTION('',(0.,0.,-1.));
#9057=DIRECTION('center_axis',(0.,0.,1.));
#9058=DIRECTION('ref_axis',(1.,0.,0.));
#9059=DIRECTION('',(0.,0.,-1.));
#9060=DIRECTION('center_axis',(0.,0.,1.));
#9061=DIRECTION('ref_axis',(1.,0.,0.));
#9062=DIRECTION('',(0.,0.,-1.));
#9063=DIRECTION('center_axis',(0.,0.,1.));
#9064=DIRECTION('ref_axis',(1.,0.,0.));
#9065=DIRECTION('',(0.,0.,-1.));
#9066=DIRECTION('center_axis',(0.,0.,1.));
#9067=DIRECTION('ref_axis',(1.,0.,0.));
#9068=DIRECTION('',(0.,0.,-1.));
#9069=DIRECTION('center_axis',(0.,0.,1.));
#9070=DIRECTION('ref_axis',(1.,0.,0.));
#9071=DIRECTION('',(0.,0.,-1.));
#9072=DIRECTION('center_axis',(0.,0.,1.));
#9073=DIRECTION('ref_axis',(1.,0.,0.));
#9074=DIRECTION('',(0.,0.,-1.));
#9075=DIRECTION('center_axis',(0.,0.,1.));
#9076=DIRECTION('ref_axis',(1.,0.,0.));
#9077=DIRECTION('',(0.,0.,-1.));
#9078=DIRECTION('center_axis',(0.,0.,1.));
#9079=DIRECTION('ref_axis',(1.,0.,0.));
#9080=DIRECTION('',(0.,0.,-1.));
#9081=DIRECTION('center_axis',(0.,0.,1.));
#9082=DIRECTION('ref_axis',(1.,0.,0.));
#9083=DIRECTION('',(0.,0.,-1.));
#9084=DIRECTION('center_axis',(0.,0.,1.));
#9085=DIRECTION('ref_axis',(1.,0.,0.));
#9086=DIRECTION('',(0.,0.,-1.));
#9087=DIRECTION('center_axis',(0.,0.,1.));
#9088=DIRECTION('ref_axis',(1.,0.,0.));
#9089=DIRECTION('',(0.,0.,-1.));
#9090=DIRECTION('center_axis',(0.,0.,1.));
#9091=DIRECTION('ref_axis',(1.,0.,0.));
#9092=DIRECTION('',(0.,0.,-1.));
#9093=DIRECTION('center_axis',(0.,0.,1.));
#9094=DIRECTION('ref_axis',(1.,0.,0.));
#9095=DIRECTION('',(0.,0.,-1.));
#9096=DIRECTION('center_axis',(0.,0.,1.));
#9097=DIRECTION('ref_axis',(1.,0.,0.));
#9098=DIRECTION('',(0.,0.,-1.));
#9099=DIRECTION('center_axis',(0.,0.,1.));
#9100=DIRECTION('ref_axis',(1.,0.,0.));
#9101=DIRECTION('',(0.,0.,-1.));
#9102=DIRECTION('center_axis',(0.,0.,1.));
#9103=DIRECTION('ref_axis',(1.,0.,0.));
#9104=DIRECTION('',(0.,0.,-1.));
#9105=DIRECTION('center_axis',(0.,0.,1.));
#9106=DIRECTION('ref_axis',(1.,-2.42503376499884E-13,0.));
#9107=DIRECTION('',(0.,0.,1.));
#9108=DIRECTION('center_axis',(0.,0.,-1.));
#9109=DIRECTION('ref_axis',(1.,-2.42503376499884E-13,0.));
#9110=DIRECTION('center_axis',(0.,0.,1.));
#9111=DIRECTION('ref_axis',(1.,-2.42503376499884E-13,0.));
#9112=DIRECTION('',(0.,0.,1.));
#9113=DIRECTION('center_axis',(0.,0.,1.));
#9114=DIRECTION('ref_axis',(1.,-2.42503376499884E-13,0.));
#9115=DIRECTION('',(0.,0.,1.));
#9116=DIRECTION('center_axis',(0.,0.,1.));
#9117=DIRECTION('ref_axis',(1.,-2.42503376499884E-13,0.));
#9118=DIRECTION('',(0.,0.,1.));
#9119=DIRECTION('center_axis',(0.,0.,1.));
#9120=DIRECTION('ref_axis',(1.,-2.42503376499884E-13,0.));
#9121=DIRECTION('',(0.,0.,1.));
#9122=DIRECTION('center_axis',(0.,0.,1.));
#9123=DIRECTION('ref_axis',(1.,-2.42503376499884E-13,0.));
#9124=DIRECTION('',(0.,0.,1.));
#9125=DIRECTION('center_axis',(0.,0.,1.));
#9126=DIRECTION('ref_axis',(1.,-2.42503376499884E-13,0.));
#9127=DIRECTION('',(0.,0.,1.));
#9128=DIRECTION('center_axis',(0.,0.,1.));
#9129=DIRECTION('ref_axis',(1.,-2.42503376499884E-13,0.));
#9130=DIRECTION('',(0.,0.,1.));
#9131=DIRECTION('center_axis',(0.,0.,1.));
#9132=DIRECTION('ref_axis',(1.,-2.42503376499884E-13,0.));
#9133=DIRECTION('',(0.,0.,1.));
#9134=DIRECTION('center_axis',(0.,0.,1.));
#9135=DIRECTION('ref_axis',(1.,-2.42503376499884E-13,0.));
#9136=DIRECTION('',(0.,0.,1.));
#9137=DIRECTION('center_axis',(0.,0.,1.));
#9138=DIRECTION('ref_axis',(1.,-2.42503376499884E-13,0.));
#9139=DIRECTION('',(0.,0.,1.));
#9140=DIRECTION('center_axis',(0.,0.,1.));
#9141=DIRECTION('ref_axis',(1.,-2.42503376499884E-13,0.));
#9142=DIRECTION('',(0.,0.,1.));
#9143=DIRECTION('center_axis',(0.,0.,1.));
#9144=DIRECTION('ref_axis',(1.,-2.42503376499884E-13,0.));
#9145=DIRECTION('',(0.,0.,1.));
#9146=DIRECTION('center_axis',(0.,0.,1.));
#9147=DIRECTION('ref_axis',(1.,-2.42503376499884E-13,0.));
#9148=DIRECTION('',(0.,0.,1.));
#9149=DIRECTION('center_axis',(0.,0.,1.));
#9150=DIRECTION('ref_axis',(1.,-2.42503376499884E-13,0.));
#9151=DIRECTION('',(0.,0.,1.));
#9152=DIRECTION('center_axis',(0.,0.,1.));
#9153=DIRECTION('ref_axis',(1.,-2.42503376499884E-13,0.));
#9154=DIRECTION('',(0.,0.,1.));
#9155=DIRECTION('center_axis',(0.,0.,1.));
#9156=DIRECTION('ref_axis',(1.,-2.42503376499884E-13,0.));
#9157=DIRECTION('',(0.,0.,1.));
#9158=DIRECTION('center_axis',(0.,0.,1.));
#9159=DIRECTION('ref_axis',(1.,-2.42503376499884E-13,0.));
#9160=DIRECTION('',(0.,0.,1.));
#9161=DIRECTION('center_axis',(0.,0.,1.));
#9162=DIRECTION('ref_axis',(1.,-2.42503376499884E-13,0.));
#9163=DIRECTION('',(0.,0.,1.));
#9164=DIRECTION('center_axis',(0.,0.,1.));
#9165=DIRECTION('ref_axis',(1.,-2.42503376499884E-13,0.));
#9166=DIRECTION('',(0.,0.,1.));
#9167=DIRECTION('center_axis',(0.,0.,1.));
#9168=DIRECTION('ref_axis',(1.,-2.42503376499884E-13,0.));
#9169=DIRECTION('',(0.,0.,1.));
#9170=DIRECTION('center_axis',(0.,0.,1.));
#9171=DIRECTION('ref_axis',(1.,-2.42503376499884E-13,0.));
#9172=DIRECTION('',(0.,0.,1.));
#9173=DIRECTION('center_axis',(0.,0.,1.));
#9174=DIRECTION('ref_axis',(1.,-2.42503376499884E-13,0.));
#9175=DIRECTION('',(0.,0.,1.));
#9176=DIRECTION('center_axis',(0.,0.,1.));
#9177=DIRECTION('ref_axis',(1.,-2.42503376499884E-13,0.));
#9178=DIRECTION('',(0.,0.,1.));
#9179=DIRECTION('center_axis',(0.,0.,1.));
#9180=DIRECTION('ref_axis',(1.,-2.42503376499884E-13,0.));
#9181=DIRECTION('',(0.,0.,1.));
#9182=DIRECTION('center_axis',(0.,0.,1.));
#9183=DIRECTION('ref_axis',(1.,-2.42503376499884E-13,0.));
#9184=DIRECTION('',(0.,0.,1.));
#9185=DIRECTION('center_axis',(0.,0.,1.));
#9186=DIRECTION('ref_axis',(1.,-2.42503376499884E-13,0.));
#9187=DIRECTION('',(0.,0.,1.));
#9188=DIRECTION('center_axis',(0.,0.,1.));
#9189=DIRECTION('ref_axis',(1.,-2.42503376499884E-13,0.));
#9190=DIRECTION('',(0.,0.,1.));
#9191=DIRECTION('center_axis',(0.,0.,1.));
#9192=DIRECTION('ref_axis',(1.,-2.42503376499884E-13,0.));
#9193=DIRECTION('',(0.,0.,1.));
#9194=DIRECTION('center_axis',(0.,0.,1.));
#9195=DIRECTION('ref_axis',(1.,-2.42503376499884E-13,0.));
#9196=DIRECTION('',(0.,0.,1.));
#9197=DIRECTION('center_axis',(0.,0.,-1.));
#9198=DIRECTION('ref_axis',(1.,0.,0.));
#9199=DIRECTION('center_axis',(0.,0.,-1.));
#9200=DIRECTION('ref_axis',(1.,0.,0.));
#9201=DIRECTION('',(0.707106781186547,8.65956056235493E-17,0.707106781186548));
#9202=DIRECTION('center_axis',(0.,0.,1.));
#9203=DIRECTION('ref_axis',(1.,0.,0.));
#9204=DIRECTION('center_axis',(0.,0.,1.));
#9205=DIRECTION('ref_axis',(1.,-2.42503376499884E-13,0.));
#9206=DIRECTION('center_axis',(0.,0.,-1.));
#9207=DIRECTION('ref_axis',(1.,-2.42503376499884E-13,0.));
#9208=DIRECTION('center_axis',(0.,0.,1.));
#9209=DIRECTION('ref_axis',(1.,0.,0.));
#9210=DIRECTION('center_axis',(-1.92296268638356E-16,-1.,0.));
#9211=DIRECTION('ref_axis',(1.,-1.92296268638356E-16,0.));
#9212=DIRECTION('',(1.,-1.92296268638356E-16,0.));
#9213=DIRECTION('',(0.,0.,1.));
#9214=DIRECTION('',(1.,-1.92296268638356E-16,0.));
#9215=DIRECTION('',(0.,0.,1.));
#9216=DIRECTION('center_axis',(-0.866025403784439,-0.5,0.));
#9217=DIRECTION('ref_axis',(0.5,-0.866025403784439,0.));
#9218=DIRECTION('',(0.5,-0.866025403784439,0.));
#9219=DIRECTION('',(0.,0.,1.));
#9220=DIRECTION('',(0.5,-0.866025403784439,0.));
#9221=DIRECTION('center_axis',(-0.866025403784439,0.5,0.));
#9222=DIRECTION('ref_axis',(-0.5,-0.866025403784439,0.));
#9223=DIRECTION('',(-0.5,-0.866025403784439,0.));
#9224=DIRECTION('',(0.,0.,1.));
#9225=DIRECTION('',(-0.5,-0.866025403784438,0.));
#9226=DIRECTION('center_axis',(1.92296268638356E-16,1.,0.));
#9227=DIRECTION('ref_axis',(-1.,1.92296268638356E-16,0.));
#9228=DIRECTION('',(-1.,1.92296268638356E-16,0.));
#9229=DIRECTION('',(0.,0.,1.));
#9230=DIRECTION('',(-1.,1.92296268638356E-16,0.));
#9231=DIRECTION('center_axis',(0.866025403784439,0.5,0.));
#9232=DIRECTION('ref_axis',(-0.5,0.866025403784439,0.));
#9233=DIRECTION('',(-0.5,0.866025403784439,0.));
#9234=DIRECTION('',(0.,0.,1.));
#9235=DIRECTION('',(-0.5,0.866025403784439,0.));
#9236=DIRECTION('center_axis',(0.866025403784439,-0.5,0.));
#9237=DIRECTION('ref_axis',(0.5,0.866025403784439,0.));
#9238=DIRECTION('',(0.5,0.866025403784439,0.));
#9239=DIRECTION('',(0.5,0.866025403784439,0.));
#9240=DIRECTION('center_axis',(0.,0.,1.));
#9241=DIRECTION('ref_axis',(1.,0.,0.));
#9242=DIRECTION('center_axis',(0.,0.,1.));
#9243=DIRECTION('ref_axis',(1.,0.,0.));
#9244=DIRECTION('center_axis',(0.,0.,1.));
#9245=DIRECTION('ref_axis',(1.,0.,0.));
#9246=DIRECTION('center_axis',(0.,0.,1.));
#9247=DIRECTION('ref_axis',(1.,0.,0.));
#9248=DIRECTION('',(0.,0.,-1.));
#9249=DIRECTION('center_axis',(0.,0.,1.));
#9250=DIRECTION('ref_axis',(1.,0.,0.));
#9251=DIRECTION('center_axis',(0.,0.,1.));
#9252=DIRECTION('ref_axis',(1.,0.,0.));
#9253=DIRECTION('center_axis',(0.,0.,1.));
#9254=DIRECTION('ref_axis',(1.,0.,0.));
#14337=CARTESIAN_POINT('',(0.,0.,0.));
#14338=CARTESIAN_POINT('Origin',(0.,0.,0.));
#14339=CARTESIAN_POINT('',(-0.14652705620645,9.44412402177196E-5,0.0160655045842905));
#14340=CARTESIAN_POINT('',(-0.146479946776166,0.000162062070299865,0.00893449541571059));
#14341=CARTESIAN_POINT('',(-0.14635,-1.79227059055215E-17,0.));
#14342=CARTESIAN_POINT('',(0.0634007094575209,0.131904027763685,0.));
#14343=CARTESIAN_POINT('Ctrl Pts',(-0.14652705620645,9.44412402177196E-5,
0.0160655045842905));
#14344=CARTESIAN_POINT('Ctrl Pts',(-0.146560923555419,0.00502618404349199,
0.0157963945919035));
#14345=CARTESIAN_POINT('Ctrl Pts',(-0.146333578783787,0.00995455679532004,
0.0155272845995164));
#14346=CARTESIAN_POINT('Ctrl Pts',(-0.14583475180505,0.0148550342388422,
0.0152581746071293));
#14347=CARTESIAN_POINT('Ctrl Pts',(-0.140929468554047,0.0630445487404258,
0.0126118447280274));
#14348=CARTESIAN_POINT('Ctrl Pts',(-0.10977174472993,0.108536575508351,
0.0099655148489255));
#14349=CARTESIAN_POINT('Ctrl Pts',(-0.0666135938566871,0.13056551637767,
0.00731918496982359));
#14350=CARTESIAN_POINT('Ctrl Pts',(-0.0268248419338395,0.150874636338504,
0.00487945664654906));
#14351=CARTESIAN_POINT('Ctrl Pts',(0.0231637104697219,0.151241233100125,
0.00243972832327453));
#14352=CARTESIAN_POINT('Ctrl Pts',(0.0635546915223951,0.132092229195826,
-2.16840434497101E-19));
#14353=CARTESIAN_POINT('',(-0.0634007094575146,0.131904027763688,0.));
#14354=CARTESIAN_POINT('Origin',(0.,0.,0.));
#14355=CARTESIAN_POINT('Ctrl Pts',(-0.0634007094575145,0.131904027763688,
-3.88578058618805E-16));
#14356=CARTESIAN_POINT('Ctrl Pts',(-0.107282641710421,0.110811831533068,
0.00264738937425961));
#14357=CARTESIAN_POINT('Ctrl Pts',(-0.139432201149969,0.0662847592091173,
0.00529477874851962));
#14358=CARTESIAN_POINT('Ctrl Pts',(-0.145436119191498,0.0182745223106641,
0.00794216812277962));
#14359=CARTESIAN_POINT('Ctrl Pts',(-0.146186273512714,0.0122759249909008,
0.00827294388708994));
#14360=CARTESIAN_POINT('Ctrl Pts',(-0.146528267289359,0.00622295186417552,
0.00860371965140026));
#14361=CARTESIAN_POINT('Ctrl Pts',(-0.146479946776166,0.000162062070299865,
0.00893449541571059));
#14362=CARTESIAN_POINT('Origin',(0.,0.,0.));
#14363=CARTESIAN_POINT('',(-0.146148830924315,7.59978318484386E-5,0.0660655045842905));
#14364=CARTESIAN_POINT('',(-0.146133770585873,6.2751561688711E-5,0.0589344954157103));
#14365=CARTESIAN_POINT('',(-0.14635,-1.79227059055215E-17,0.));
#14366=CARTESIAN_POINT('Ctrl Pts',(-0.146148830924315,7.59978318484386E-5,
0.0660655045842905));
#14367=CARTESIAN_POINT('Ctrl Pts',(-0.146240443598182,0.0195917497831913,
0.0650077071998482));
#14368=CARTESIAN_POINT('Ctrl Pts',(-0.142607114239671,0.0390747476468127,
0.0639499098154059));
#14369=CARTESIAN_POINT('Ctrl Pts',(-0.135087779856993,0.056920264102034,
0.0628921124309636));
#14370=CARTESIAN_POINT('Ctrl Pts',(-0.116276389754784,0.10156503643559,
0.0602457825518617));
#14371=CARTESIAN_POINT('Ctrl Pts',(-0.073143724514267,0.135961331060063,
0.0575994526727599));
#14372=CARTESIAN_POINT('Ctrl Pts',(-0.025432083612881,0.144366623974243,
0.054953122793658));
#14373=CARTESIAN_POINT('Ctrl Pts',(0.0222795572885053,0.152771916888423,
0.0523067929145561));
#14374=CARTESIAN_POINT('Ctrl Pts',(0.0745701738507606,0.135186208092309,
0.0496604630354541));
#14375=CARTESIAN_POINT('Ctrl Pts',(0.107505148494886,0.0996564726649905,
0.0470141331563522));
#14376=CARTESIAN_POINT('Ctrl Pts',(0.140440123139012,0.0641267372376721,
0.0443678032772503));
#14377=CARTESIAN_POINT('Ctrl Pts',(0.154019455865009,0.010652975179149,
0.0417214733981484));
#14378=CARTESIAN_POINT('Ctrl Pts',(0.14202839331759,-0.0362847016460775,
0.0390751435190465));
#14379=CARTESIAN_POINT('Ctrl Pts',(0.130037330770172,-0.0832223784713041,
0.0364288136399446));
#14380=CARTESIAN_POINT('Ctrl Pts',(0.0924758729493388,-0.123623970063234,
0.0337824837608427));
#14381=CARTESIAN_POINT('Ctrl Pts',(0.0465351214488668,-0.139005253038876,
0.0311361538817407));
#14382=CARTESIAN_POINT('Ctrl Pts',(0.000594369948394902,-0.154386536014517,
0.0284898240026388));
#14383=CARTESIAN_POINT('Ctrl Pts',(-0.0537256752317158,-0.144747510373871,
0.025843494123537));
#14384=CARTESIAN_POINT('Ctrl Pts',(-0.0915592764828275,-0.114484496435928,
0.0231971642444351));
#14385=CARTESIAN_POINT('Ctrl Pts',(-0.125545511528741,-0.0872989822136326,
0.0208199443577202));
#14386=CARTESIAN_POINT('Ctrl Pts',(-0.146227884351973,-0.0434707826450544,
0.0184427244710054));
#14387=CARTESIAN_POINT('Ctrl Pts',(-0.14652705620645,9.44412402177196E-5,
0.0160655045842905));
#14388=CARTESIAN_POINT('Ctrl Pts',(-0.146479946776166,0.000162062070299865,
0.00893449541571059));
#14389=CARTESIAN_POINT('Ctrl Pts',(-0.146141530330399,-0.0422858476614564,
0.0112511090256603));
#14390=CARTESIAN_POINT('Ctrl Pts',(-0.126658161292025,-0.0851220706608281,
0.0135677226356099));
#14391=CARTESIAN_POINT('Ctrl Pts',(-0.0941604943243988,-0.112386678841155,
0.0158843362455596));
#14392=CARTESIAN_POINT('Ctrl Pts',(-0.0570226747722624,-0.143544241621566,
0.0185317256198196));
#14393=CARTESIAN_POINT('Ctrl Pts',(-0.00288875902448078,-0.154365965709432,
0.0211791149940796));
#14394=CARTESIAN_POINT('Ctrl Pts',(0.0434083729543798,-0.140002007265973,
0.0238265043683396));
#14395=CARTESIAN_POINT('Ctrl Pts',(0.0897055049332404,-0.125638048822514,
0.0264738937425996));
#14396=CARTESIAN_POINT('Ctrl Pts',(0.12816585314318,-0.0860884078477292,
0.0291212831168596));
#14397=CARTESIAN_POINT('Ctrl Pts',(0.141191617966992,-0.0394144013492358,
0.0317686724911196));
#14398=CARTESIAN_POINT('Ctrl Pts',(0.154217382790803,0.00725960514925768,
0.0344160618653796));
#14399=CARTESIAN_POINT('Ctrl Pts',(0.141808564228487,0.0610579771714599,
0.0370634512396396));
#14400=CARTESIAN_POINT('Ctrl Pts',(0.109639063769471,0.0973098477439542,
0.0397108406138996));
#14401=CARTESIAN_POINT('Ctrl Pts',(0.0774695633104545,0.133561718316448,
0.0423582299881596));
#14402=CARTESIAN_POINT('Ctrl Pts',(0.0255393809547383,0.152267087439235,
0.0450056193624196));
#14403=CARTESIAN_POINT('Ctrl Pts',(-0.0223595433272462,0.144872892294413,
0.0476530087366796));
#14404=CARTESIAN_POINT('Ctrl Pts',(-0.070258467609231,0.137478697149591,
0.0503003981109396));
#14405=CARTESIAN_POINT('Ctrl Pts',(-0.114126133817484,0.10398493773716,
0.0529477874851996));
#14406=CARTESIAN_POINT('Ctrl Pts',(-0.133871661545403,0.059725601630819,
0.0555951768594596));
#14407=CARTESIAN_POINT('Ctrl Pts',(-0.142173753131161,0.0411165744656389,
0.0567082830448765));
#14408=CARTESIAN_POINT('Ctrl Pts',(-0.146211489678532,0.0206043892842972,
0.0578213892302934));
#14409=CARTESIAN_POINT('Ctrl Pts',(-0.146133770585873,6.2751561688711E-5,
0.0589344954157103));
#14410=CARTESIAN_POINT('Origin',(0.,0.,0.));
#14411=CARTESIAN_POINT('',(-0.146252097264499,-0.000124487410312429,0.116065504584291));
#14412=CARTESIAN_POINT('',(-0.146276374479508,-0.000129480650117819,0.10893449541571));
#14413=CARTESIAN_POINT('',(-0.14635,-1.79227059055215E-17,0.));
#14414=CARTESIAN_POINT('Ctrl Pts',(-0.146252097264499,-0.000124487410312429,
0.116065504584291));
#14415=CARTESIAN_POINT('Ctrl Pts',(-0.145977101830714,0.0338815411246725,
0.114219019807793));
#14416=CARTESIAN_POINT('Ctrl Pts',(-0.134160879762789,0.0680598926014691,
0.112372535031295));
#14417=CARTESIAN_POINT('Ctrl Pts',(-0.112484833627769,0.0939988017516943,
0.110526050254798));
#14418=CARTESIAN_POINT('Ctrl Pts',(-0.0814193359437304,0.131173714423195,
0.107879720375696));
#14419=CARTESIAN_POINT('Ctrl Pts',(-0.0301019434218634,0.151424966146533,
0.105233390496594));
#14420=CARTESIAN_POINT('Ctrl Pts',(0.0179785702873004,0.145483266051774,
0.102587060617492));
#14421=CARTESIAN_POINT('Ctrl Pts',(0.0660590839964643,0.139541565957016,
0.0999407307383904));
#14422=CARTESIAN_POINT('Ctrl Pts',(0.110902718892925,0.107406914044162,
0.0972944008592884));
#14423=CARTESIAN_POINT('Ctrl Pts',(0.131983829661647,0.0637877973597534,
0.0946480709801865));
#14424=CARTESIAN_POINT('Ctrl Pts',(0.15306494043037,0.0201686806753445,
0.0920017411010846));
#14425=CARTESIAN_POINT('Ctrl Pts',(0.150383527071356,-0.0349349007806195,
0.0893554112219828));
#14426=CARTESIAN_POINT('Ctrl Pts',(0.125166930059577,-0.0763010783846813,
0.0867090813428809));
#14427=CARTESIAN_POINT('Ctrl Pts',(0.0999503330477985,-0.117667255988743,
0.084062751463779));
#14428=CARTESIAN_POINT('Ctrl Pts',(0.0521985523832557,-0.145296029740903,
0.081416421584677));
#14429=CARTESIAN_POINT('Ctrl Pts',(0.00376830011669856,-0.146541450754272,
0.0787700917055751));
#14430=CARTESIAN_POINT('Ctrl Pts',(-0.0446619521498586,-0.147786871767642,
0.0761237618264732));
#14431=CARTESIAN_POINT('Ctrl Pts',(-0.09377067601843,-0.122648940042221,
0.0734774319473713));
#14432=CARTESIAN_POINT('Ctrl Pts',(-0.121079980470766,-0.0826333491581908,
0.0708311020682694));
#14433=CARTESIAN_POINT('Ctrl Pts',(-0.137473143648068,-0.0586128871159229,
0.0692425695736098));
#14434=CARTESIAN_POINT('Ctrl Pts',(-0.146011252866834,-0.02923151094855,
0.0676540370789502));
#14435=CARTESIAN_POINT('Ctrl Pts',(-0.146148830924315,7.59978318484386E-5,
0.0660655045842905));
#14436=CARTESIAN_POINT('Ctrl Pts',(-0.146133770585873,6.2751561688711E-5,
0.0589344954157103));
#14437=CARTESIAN_POINT('Ctrl Pts',(-0.146026644150963,-0.0282514289199324,
0.0604687786045534));
#14438=CARTESIAN_POINT('Ctrl Pts',(-0.138100435392092,-0.0566215672018456,
0.0620030617933965));
#14439=CARTESIAN_POINT('Ctrl Pts',(-0.122745086057252,-0.0801407530065182,
0.0635373449822396));
#14440=CARTESIAN_POINT('Ctrl Pts',(-0.0962495935935968,-0.120722858737265,
0.0661847343564996));
#14441=CARTESIAN_POINT('Ctrl Pts',(-0.0476352194187008,-0.146862157398507,
0.0688321237307596));
#14442=CARTESIAN_POINT('Ctrl Pts',(0.00082938917649622,-0.146587691816784,
0.0714795131050196));
#14443=CARTESIAN_POINT('Ctrl Pts',(0.0492939977716932,-0.146313226235061,
0.0741269024792796));
#14444=CARTESIAN_POINT('Ctrl Pts',(0.0976088407871913,-0.119624996410372,
0.0767742918535397));
#14445=CARTESIAN_POINT('Ctrl Pts',(0.123643642180798,-0.0787464320231966,
0.0794216812277997));
#14446=CARTESIAN_POINT('Ctrl Pts',(0.149678443574405,-0.0378678676360213,
0.0820690706020596));
#14447=CARTESIAN_POINT('Ctrl Pts',(0.153433203346121,0.0172010313136401,
0.0847164599763195));
#14448=CARTESIAN_POINT('Ctrl Pts',(0.133187835944515,0.06123527443138,0.0873638493505795));
#14449=CARTESIAN_POINT('Ctrl Pts',(0.11294246854291,0.10526951754912,0.0900112387248395));
#14450=CARTESIAN_POINT('Ctrl Pts',(0.0686969739679828,0.138269104834938,
0.0926586280990997));
#14451=CARTESIAN_POINT('Ctrl Pts',(0.0207181735233275,0.145118849380084,
0.0953060174733597));
#14452=CARTESIAN_POINT('Ctrl Pts',(-0.027260626921328,0.151968593925229,
0.0979534068476197));
#14453=CARTESIAN_POINT('Ctrl Pts',(-0.0789727332357116,0.132668495729702,
0.10060079622188));
#14454=CARTESIAN_POINT('Ctrl Pts',(-0.110731403441959,0.0960588230543748,
0.10324818559614));
#14455=CARTESIAN_POINT('Ctrl Pts',(-0.133469481440122,0.0698475998711364,
0.105143622202663));
#14456=CARTESIAN_POINT('Ctrl Pts',(-0.145979327216774,0.0347634013028336,
0.107039058809187));
#14457=CARTESIAN_POINT('Ctrl Pts',(-0.146276374479508,-0.000129480650117819,
0.10893449541571));
#14458=CARTESIAN_POINT('Origin',(0.,0.,0.));
#14459=CARTESIAN_POINT('',(-0.146589818999335,-3.81787486967988E-6,0.166065504584291));
#14460=CARTESIAN_POINT('',(-0.146589453522336,1.04004190909306E-5,0.15893449541571));
#14461=CARTESIAN_POINT('',(-0.14635,-1.79227059055215E-17,0.));
#14462=CARTESIAN_POINT('Ctrl Pts',(-0.146589818999335,-3.81787486967988E-6,
0.166065504584291));
#14463=CARTESIAN_POINT('Ctrl Pts',(-0.146571339149733,0.0482382848470949,
0.163430332415738));
#14464=CARTESIAN_POINT('Ctrl Pts',(-0.120433071521034,0.0964975486977609,
0.160795160247185));
#14465=CARTESIAN_POINT('Ctrl Pts',(-0.0800107885095625,0.122828684230981,
0.158159988078632));
#14466=CARTESIAN_POINT('Ctrl Pts',(-0.0394173515450545,0.149271309704865,
0.15551365819953));
#14467=CARTESIAN_POINT('Ctrl Pts',(0.0155813181737399,0.153599719825856,
0.152867328320428));
#14468=CARTESIAN_POINT('Ctrl Pts',(0.0598114643267532,0.133832733731537,
0.150220998441327));
#14469=CARTESIAN_POINT('Ctrl Pts',(0.104041610479766,0.114065747637217,
0.147574668562225));
#14470=CARTESIAN_POINT('Ctrl Pts',(0.137503233066998,0.0702033653275883,
0.144928338683123));
#14471=CARTESIAN_POINT('Ctrl Pts',(0.144880420813362,0.0223220882221681,
0.142282008804021));
#14472=CARTESIAN_POINT('Ctrl Pts',(0.152257608559726,-0.0255591888832524,
0.139635678924919));
#14473=CARTESIAN_POINT('Ctrl Pts',(0.133550361465222,-0.077459360784464,
0.136989349045817));
#14474=CARTESIAN_POINT('Ctrl Pts',(0.0973212811704284,-0.109622900294719,
0.134343019166715));
#14475=CARTESIAN_POINT('Ctrl Pts',(0.0610922008756344,-0.141786439804975,
0.131696689287613));
#14476=CARTESIAN_POINT('Ctrl Pts',(0.00734128738055008,-0.154213346924274,
0.129050359408511));
#14477=CARTESIAN_POINT('Ctrl Pts',(-0.0393288211819405,-0.141215634503184,
0.126404029529409));
#14478=CARTESIAN_POINT('Ctrl Pts',(-0.0859989297444312,-0.128217922082094,
0.123757699650308));
#14479=CARTESIAN_POINT('Ctrl Pts',(-0.125588233374328,-0.0897955901206149,
0.121111369771206));
#14480=CARTESIAN_POINT('Ctrl Pts',(-0.139976083766172,-0.043535137330043,
0.118465039892104));
#14481=CARTESIAN_POINT('Ctrl Pts',(-0.144324767489921,-0.0295530571287048,
0.117665194789499));
#14482=CARTESIAN_POINT('Ctrl Pts',(-0.146371217526823,-0.0148549394177889,
0.116865349686895));
#14483=CARTESIAN_POINT('Ctrl Pts',(-0.146252097264499,-0.000124487410312429,
0.116065504584291));
#14484=CARTESIAN_POINT('Ctrl Pts',(-0.146276374479508,-0.000129480650117819,
0.10893449541571));
#14485=CARTESIAN_POINT('Ctrl Pts',(-0.14639421831063,-0.0139720956278579,
0.109686448183447));
#14486=CARTESIAN_POINT('Ctrl Pts',(-0.14458995413065,-0.0277846002915201,
0.110438400951183));
#14487=CARTESIAN_POINT('Ctrl Pts',(-0.140739671041232,-0.041001045008257,
0.11119035371892));
#14488=CARTESIAN_POINT('Ctrl Pts',(-0.127184034336146,-0.0875319932404337,
0.11383774309318));
#14489=CARTESIAN_POINT('Ctrl Pts',(-0.0882675268278623,-0.12667464254966,
0.11648513246744));
#14490=CARTESIAN_POINT('Ctrl Pts',(-0.0418159243469935,-0.140499695546946,
0.1191325218417));
#14491=CARTESIAN_POINT('Ctrl Pts',(0.00463567813387508,-0.154324748544231,
0.12177991121596));
#14492=CARTESIAN_POINT('Ctrl Pts',(0.0586223755873289,-0.142832205229577,
0.12442730059022));
#14493=CARTESIAN_POINT('Ctrl Pts',(0.0954154960694136,-0.111286216216264,
0.12707468996448));
#14494=CARTESIAN_POINT('Ctrl Pts',(0.132208616551499,-0.0797402272029501,
0.12972207933874));
#14495=CARTESIAN_POINT('Ctrl Pts',(0.151808160062214,-0.0281407924909768,
0.132369468712999));
#14496=CARTESIAN_POINT('Ctrl Pts',(0.145236524363737,0.0198768833792122,
0.135016858087259));
#14497=CARTESIAN_POINT('Ctrl Pts',(0.138664888665259,0.0678945592494009,
0.13766424746152));
#14498=CARTESIAN_POINT('Ctrl Pts',(0.105922073757589,0.112330476277805,
0.14031163683578));
#14499=CARTESIAN_POINT('Ctrl Pts',(0.062005973158836,0.132830708741579,
0.14295902621004));
#14500=CARTESIAN_POINT('Ctrl Pts',(0.0180898725600832,0.153330941205352,
0.1456064155843));
#14501=CARTESIAN_POINT('Ctrl Pts',(-0.0369995137297515,0.149895489104495,
0.14825380495856));
#14502=CARTESIAN_POINT('Ctrl Pts',(-0.0780284182758478,0.124097962381086,
0.15090119433282));
#14503=CARTESIAN_POINT('Ctrl Pts',(-0.119057322821944,0.0983004356576776,
0.153548583707079));
#14504=CARTESIAN_POINT('Ctrl Pts',(-0.146025745624302,0.0501408343117172,
0.15619597308134));
#14505=CARTESIAN_POINT('Ctrl Pts',(-0.14658076309025,0.00167873146180186,
0.1588433624556));
#14506=CARTESIAN_POINT('Ctrl Pts',(-0.146587131676737,0.00112264969450139,
0.15887374010897));
#14507=CARTESIAN_POINT('Ctrl Pts',(-0.146590022522527,0.000566528098114988,
0.15890411776234));
#14508=CARTESIAN_POINT('Ctrl Pts',(-0.146589453522336,1.04004190909306E-5,
0.15893449541571));
#14509=CARTESIAN_POINT('Origin',(0.,0.,0.));
#14510=CARTESIAN_POINT('',(-0.146263250741535,0.000126870157254357,0.21606550458429));
#14511=CARTESIAN_POINT('',(-0.146245769975643,0.000123264779366826,0.20893449541571));
#14512=CARTESIAN_POINT('',(-0.14635,-1.79227059055215E-17,0.));
#14513=CARTESIAN_POINT('Ctrl Pts',(-0.146263250741535,0.000126870157254357,
0.21606550458429));
#14514=CARTESIAN_POINT('Ctrl Pts',(-0.146381923100139,0.0144435832128767,
0.215287974902784));
#14515=CARTESIAN_POINT('Ctrl Pts',(-0.144450237714319,0.0287289633064517,
0.214510445221278));
#14516=CARTESIAN_POINT('Ctrl Pts',(-0.140337374518256,0.0423560295890773,
0.213732915539772));
#14517=CARTESIAN_POINT('Ctrl Pts',(-0.126339204386259,0.0887358830222778,
0.21108658566067));
#14518=CARTESIAN_POINT('Ctrl Pts',(-0.0870745347363382,0.127489909020004,
0.208440255781569));
#14519=CARTESIAN_POINT('Ctrl Pts',(-0.0405154226099946,0.140879780169064,
0.205793925902467));
#14520=CARTESIAN_POINT('Ctrl Pts',(0.00604368951634975,0.154269651318124,
0.203147596023365));
#14521=CARTESIAN_POINT('Ctrl Pts',(0.0598972441191175,0.142295367618517,
0.200501266144263));
#14522=CARTESIAN_POINT('Ctrl Pts',(0.0963956219934077,0.110437747119808,
0.197854936265161));
#14523=CARTESIAN_POINT('Ctrl Pts',(0.132893999867697,0.0785801266211,0.195208606386059));
#14524=CARTESIAN_POINT('Ctrl Pts',(0.15203720101351,0.0268391693232909,
0.192562276506957));
#14525=CARTESIAN_POINT('Ctrl Pts',(0.145063081087281,-0.0211024746124516,
0.189915946627855));
#14526=CARTESIAN_POINT('Ctrl Pts',(0.138088961161051,-0.0690441185481943,
0.187269616748753));
#14527=CARTESIAN_POINT('Ctrl Pts',(0.10499752016278,-0.11318644912187,0.184623286869651));
#14528=CARTESIAN_POINT('Ctrl Pts',(0.060935231264163,-0.133324827106958,
0.181976956990549));
#14529=CARTESIAN_POINT('Ctrl Pts',(0.0168729423655461,-0.153463205092045,
0.179330627111448));
#14530=CARTESIAN_POINT('Ctrl Pts',(-0.0381601944334158,-0.149597630488544,
0.176684297232346));
#14531=CARTESIAN_POINT('Ctrl Pts',(-0.0789746466099193,-0.123497437688695,
0.174037967353244));
#14532=CARTESIAN_POINT('Ctrl Pts',(-0.119961184605052,-0.0972871987457574,
0.171380479763593));
#14533=CARTESIAN_POINT('Ctrl Pts',(-0.146608455341797,-0.0486544490602708,
0.168722992173942));
#14534=CARTESIAN_POINT('Ctrl Pts',(-0.146589818999335,-3.81787486967988E-6,
0.166065504584291));
#14535=CARTESIAN_POINT('Ctrl Pts',(-0.146589453522336,1.04004190909306E-5,
0.15893449541571));
#14536=CARTESIAN_POINT('Ctrl Pts',(-0.146540434588914,-0.0478995759235739,
0.1615515071366));
#14537=CARTESIAN_POINT('Ctrl Pts',(-0.120813506558866,-0.0958546957256878,
0.16416851885749));
#14538=CARTESIAN_POINT('Ctrl Pts',(-0.0808500697395765,-0.122278388912248,
0.16678553057838));
#14539=CARTESIAN_POINT('Ctrl Pts',(-0.0404227467934142,-0.149008802082514,
0.16943291995264));
#14540=CARTESIAN_POINT('Ctrl Pts',(0.0145735112284506,-0.153705024069172,
0.1720803093269));
#14541=CARTESIAN_POINT('Ctrl Pts',(0.0589475933459444,-0.134215943447351,
0.17472769870116));
#14542=CARTESIAN_POINT('Ctrl Pts',(0.103321675463438,-0.11472686282553,
0.17737508807542));
#14543=CARTESIAN_POINT('Ctrl Pts',(0.137073581676561,-0.0710524795952304,
0.18002247744968));
#14544=CARTESIAN_POINT('Ctrl Pts',(0.144743205110219,-0.0231979049720499,
0.18266986682394));
#14545=CARTESIAN_POINT('Ctrl Pts',(0.152412828543877,0.024656669651131,
0.1853172561982));
#14546=CARTESIAN_POINT('Ctrl Pts',(0.13400016919807,0.0766914356671922,
0.18796464557246));
#14547=CARTESIAN_POINT('Ctrl Pts',(0.0979391709064228,0.109071797518936,
0.19061203494672));
#14548=CARTESIAN_POINT('Ctrl Pts',(0.0618781726147763,0.141452159370678,
0.19325942432098));
#14549=CARTESIAN_POINT('Ctrl Pts',(0.00816883537729064,0.154178117058104,
0.195906813695239));
#14550=CARTESIAN_POINT('Ctrl Pts',(-0.0385872054932313,0.1414205281901,
0.198554203069499));
#14551=CARTESIAN_POINT('Ctrl Pts',(-0.0853432463637543,0.128662939322095,
0.201201592443759));
#14552=CARTESIAN_POINT('Ctrl Pts',(-0.125145990867313,0.0904218038986596,
0.20384898181802));
#14553=CARTESIAN_POINT('Ctrl Pts',(-0.139763737461459,0.0442135263146365,
0.20649637119228));
#14554=CARTESIAN_POINT('Ctrl Pts',(-0.144251162244238,0.030028291356252,
0.207309079266757));
#14555=CARTESIAN_POINT('Ctrl Pts',(-0.146365162502875,0.0150922359825044,
0.208121787341234));
#14556=CARTESIAN_POINT('Ctrl Pts',(-0.146245769975643,0.000123264779366826,
0.20893449541571));
#14557=CARTESIAN_POINT('Origin',(0.,0.,0.));
#14558=CARTESIAN_POINT('',(-0.146142672279203,-7.01165389862951E-5,0.266065504584291));
#14559=CARTESIAN_POINT('',(-0.146150215784492,-7.74481165901552E-5,0.258934495415711));
#14560=CARTESIAN_POINT('',(-0.14635,-1.79227059055215E-17,0.));
#14561=CARTESIAN_POINT('Ctrl Pts',(-0.146142672279203,-7.01165389862951E-5,
0.266065504584291));
#14562=CARTESIAN_POINT('Ctrl Pts',(-0.146017527260215,0.028828671850369,
0.264499287510729));
#14563=CARTESIAN_POINT('Ctrl Pts',(-0.137733916992107,0.0577936173630845,
0.262933070437168));
#14564=CARTESIAN_POINT('Ctrl Pts',(-0.121770841384076,0.0816117278206753,
0.261366853363607));
#14565=CARTESIAN_POINT('Ctrl Pts',(-0.0947991242083451,0.121855560193383,
0.258720523484505));
#14566=CARTESIAN_POINT('Ctrl Pts',(-0.0459036471244643,0.147405924851771,
0.256074193605403));
#14567=CARTESIAN_POINT('Ctrl Pts',(0.0025353607453442,0.146568017913755,
0.253427863726301));
#14568=CARTESIAN_POINT('Ctrl Pts',(0.050974368615152,0.145730110975738,
0.250781533847199));
#14569=CARTESIAN_POINT('Ctrl Pts',(0.0989569072708876,0.118503932441319,
0.248135203968097));
#14570=CARTESIAN_POINT('Ctrl Pts',(0.124520613871998,0.0773513325689396,
0.245488874088995));
#14571=CARTESIAN_POINT('Ctrl Pts',(0.150084320473109,0.0361987326965595,
0.242842544209893));
#14572=CARTESIAN_POINT('Ctrl Pts',(0.153229195019594,-0.0188802885137813,
0.240196214330791));
#14573=CARTESIAN_POINT('Ctrl Pts',(0.132515778953886,-0.0626751965094481,
0.237549884451689));
#14574=CARTESIAN_POINT('Ctrl Pts',(0.111802362888177,-0.106470104505115,
0.234903554572587));
#14575=CARTESIAN_POINT('Ctrl Pts',(0.0672306562102751,-0.138980899286108,
0.232257224693486));
#14576=CARTESIAN_POINT('Ctrl Pts',(0.0192018303028616,-0.145326878595667,
0.229610894814384));
#14577=CARTESIAN_POINT('Ctrl Pts',(-0.0288269956045516,-0.151672857905225,
0.226964564935282));
#14578=CARTESIAN_POINT('Ctrl Pts',(-0.0803129407414762,-0.131854021743351,
0.22431823505618));
#14579=CARTESIAN_POINT('Ctrl Pts',(-0.111690078002902,-0.0949417632280756,
0.221671905177078));
#14580=CARTESIAN_POINT('Ctrl Pts',(-0.133848162215005,-0.0688748557907962,
0.219803104979482));
#14581=CARTESIAN_POINT('Ctrl Pts',(-0.145978020566425,-0.0342834897603843,
0.217934304781886));
#14582=CARTESIAN_POINT('Ctrl Pts',(-0.146263250741535,0.000126870157254357,
0.21606550458429));
#14583=CARTESIAN_POINT('Ctrl Pts',(-0.146245769975643,0.000123264779366826,
0.20893449541571));
#14584=CARTESIAN_POINT('Ctrl Pts',(-0.145976242399967,-0.03366905549635,
0.210769176715493));
#14585=CARTESIAN_POINT('Ctrl Pts',(-0.134324750276972,-0.067629123606452,
0.212603858015276));
#14586=CARTESIAN_POINT('Ctrl Pts',(-0.112902327433,-0.0934976078712483,
0.214438539315059));
#14587=CARTESIAN_POINT('Ctrl Pts',(-0.0819904221256615,-0.130825044728502,
0.217085928689319));
#14588=CARTESIAN_POINT('Ctrl Pts',(-0.0307338628262512,-0.151304498698398,
0.21973331806358));
#14589=CARTESIAN_POINT('Ctrl Pts',(0.0173892134168267,-0.145555327884408,
0.22238070743784));
#14590=CARTESIAN_POINT('Ctrl Pts',(0.0655122896599044,-0.139806157070418,
0.2250280968121));
#14591=CARTESIAN_POINT('Ctrl Pts',(0.11050188284665,-0.107828361472542,
0.22767548618636));
#14592=CARTESIAN_POINT('Ctrl Pts',(0.131750448317205,-0.0642694140823833,
0.23032287556062));
#14593=CARTESIAN_POINT('Ctrl Pts',(0.15299901378776,-0.020710466692225,
0.232970264934879));
#14594=CARTESIAN_POINT('Ctrl Pts',(0.150506551542124,0.0344296324902152,
0.23561765430914));
#14595=CARTESIAN_POINT('Ctrl Pts',(0.125414737320077,0.0758938856636754,
0.2382650436834));
#14596=CARTESIAN_POINT('Ctrl Pts',(0.10032292309803,0.117358138837136,0.24091243305766));
#14597=CARTESIAN_POINT('Ctrl Pts',(0.0526317568995709,0.145146546001616,
0.24355982243192));
#14598=CARTESIAN_POINT('Ctrl Pts',(0.00418624259284972,0.146530589268381,
0.24620721180618));
#14599=CARTESIAN_POINT('Ctrl Pts',(-0.0442592717138715,0.147914632535146,
0.24885460118044));
#14600=CARTESIAN_POINT('Ctrl Pts',(-0.0934591341288551,0.122894311904195,
0.2515019905547));
#14601=CARTESIAN_POINT('Ctrl Pts',(-0.120877280418781,0.082930219442967,
0.25414937992896));
#14602=CARTESIAN_POINT('Ctrl Pts',(-0.137396572682769,0.0588520590724165,
0.255744418424543));
#14603=CARTESIAN_POINT('Ctrl Pts',(-0.146009100715185,0.0293493086505574,
0.257339456920127));
#14604=CARTESIAN_POINT('Ctrl Pts',(-0.146150215784492,-7.74481165901552E-5,
0.258934495415711));
#14605=CARTESIAN_POINT('Origin',(0.,0.,0.));
#14606=CARTESIAN_POINT('',(-0.146519404976022,-8.97763884284003E-5,0.316065504584291));
#14607=CARTESIAN_POINT('',(-0.146528765763263,-8.45393868379275E-5,0.30893449541571));
#14608=CARTESIAN_POINT('',(-0.14635,-1.79227059055215E-17,0.));
#14609=CARTESIAN_POINT('Ctrl Pts',(-0.146519404976022,-8.97763884284003E-5,
0.316065504584291));
#14610=CARTESIAN_POINT('Ctrl Pts',(-0.146208092107557,0.043076445171776,
0.313710600118674));
#14611=CARTESIAN_POINT('Ctrl Pts',(-0.125958424314353,0.0864965766126209,
0.311355695653057));
#14612=CARTESIAN_POINT('Ctrl Pts',(-0.0925183485457987,0.1137056160074,
0.309000791187441));
#14613=CARTESIAN_POINT('Ctrl Pts',(-0.0549399784004991,0.144281843189175,
0.306354461308339));
#14614=CARTESIAN_POINT('Ctrl Pts',(-0.00070450021881692,0.154386382754941,
0.303708131429237));
#14615=CARTESIAN_POINT('Ctrl Pts',(0.0453636543616171,0.139394227973128,
0.301061801550135));
#14616=CARTESIAN_POINT('Ctrl Pts',(0.0914318089420511,0.124402073191315,
0.298415471671033));
#14617=CARTESIAN_POINT('Ctrl Pts',(0.129332639921237,0.0843132240619223,
0.295769141791931));
#14618=CARTESIAN_POINT('Ctrl Pts',(0.141718340675246,0.0374769775398043,
0.293122811912829));
#14619=CARTESIAN_POINT('Ctrl Pts',(0.154104041429255,-0.00935926898231351,
0.290476482033727));
#14620=CARTESIAN_POINT('Ctrl Pts',(0.140974611958088,-0.0629429128971569,
0.287830152154626));
#14621=CARTESIAN_POINT('Ctrl Pts',(0.108339598692885,-0.0987478773661917,
0.285183822275524));
#14622=CARTESIAN_POINT('Ctrl Pts',(0.0757045854276824,-0.134552841835227,
0.282537492396422));
#14623=CARTESIAN_POINT('Ctrl Pts',(0.0235639883684441,-0.152579126858453,
0.27989116251732));
#14624=CARTESIAN_POINT('Ctrl Pts',(-0.0242166208952047,-0.144575818177467,
0.277244832638218));
#14625=CARTESIAN_POINT('Ctrl Pts',(-0.0719972301588528,-0.136572509496481,
0.274598502759116));
#14626=CARTESIAN_POINT('Ctrl Pts',(-0.115417851626912,-0.102539607111283,
0.271952172880014));
#14627=CARTESIAN_POINT('Ctrl Pts',(-0.13460418372715,-0.0580545058751705,
0.269305843000912));
#14628=CARTESIAN_POINT('Ctrl Pts',(-0.142435181350113,-0.0398976888130428,
0.268225730195372));
#14629=CARTESIAN_POINT('Ctrl Pts',(-0.146228976240411,-0.0199996345674016,
0.267145617389831));
#14630=CARTESIAN_POINT('Ctrl Pts',(-0.146142672279203,-7.01165389862951E-5,
0.266065504584291));
#14631=CARTESIAN_POINT('Ctrl Pts',(-0.146150215784492,-7.74481165901552E-5,
0.258934495415711));
#14632=CARTESIAN_POINT('Ctrl Pts',(-0.146243318595233,-0.0194921979337541,
0.259986846294387));
#14633=CARTESIAN_POINT('Ctrl Pts',(-0.142648899141753,-0.0388738684647463,
0.261039197173063));
#14634=CARTESIAN_POINT('Ctrl Pts',(-0.135204796371803,-0.0566427511368837,
0.26209154805174));
#14635=CARTESIAN_POINT('Ctrl Pts',(-0.116477735870028,-0.101343764964001,
0.264738937426));
#14636=CARTESIAN_POINT('Ctrl Pts',(-0.0733871847016099,-0.135837928326728,
0.26738632680026));
#14637=CARTESIAN_POINT('Ctrl Pts',(-0.0256708287318585,-0.144325142544676,
0.27003371617452));
#14638=CARTESIAN_POINT('Ctrl Pts',(0.0220455272378925,-0.152812356762624,
0.27268110554878));
#14639=CARTESIAN_POINT('Ctrl Pts',(0.0743876880089763,-0.135292621835792,
0.27532849492304));
#14640=CARTESIAN_POINT('Ctrl Pts',(0.10738025529095,-0.0997908762961729,
0.2779758842973));
#14641=CARTESIAN_POINT('Ctrl Pts',(0.140372822572925,-0.0642891307565533,
0.280623273671559));
#14642=CARTESIAN_POINT('Ctrl Pts',(0.154015796365789,-0.010805374604146,
0.283270663045819));
#14643=CARTESIAN_POINT('Ctrl Pts',(0.142059993874458,0.0361620845457957,
0.285918052420079));
#14644=CARTESIAN_POINT('Ctrl Pts',(0.130104191383128,0.0831295436957373,
0.288565441794339));
#14645=CARTESIAN_POINT('Ctrl Pts',(0.0925496126076039,0.123580705843213,
0.291212831168599));
#14646=CARTESIAN_POINT('Ctrl Pts',(0.0465981836912963,0.138986860871753,
0.29386022054286));
#14647=CARTESIAN_POINT('Ctrl Pts',(0.000646754774988913,0.154393015900293,
0.296507609917119));
#14648=CARTESIAN_POINT('Ctrl Pts',(-0.0537015242821025,0.144754163809898,
0.29915499929138));
#14649=CARTESIAN_POINT('Ctrl Pts',(-0.0915523499663989,0.114485393976436,
0.30180238866564));
#14650=CARTESIAN_POINT('Ctrl Pts',(-0.125542580994678,0.0873038870745135,
0.30417975758233));
#14651=CARTESIAN_POINT('Ctrl Pts',(-0.146229051243382,0.0434861464246214,
0.30655712649902));
#14652=CARTESIAN_POINT('Ctrl Pts',(-0.146528765763263,-8.45393868379275E-5,
0.30893449541571));
#14653=CARTESIAN_POINT('Origin',(0.,0.,0.));
#14654=CARTESIAN_POINT('',(-0.146416087288192,0.000126442170093593,0.366065504584291));
#14655=CARTESIAN_POINT('',(-0.146408012399712,0.000128195943346294,0.358934495415711));
#14656=CARTESIAN_POINT('',(-0.14635,-1.79227059055215E-17,0.));
#14657=CARTESIAN_POINT('Ctrl Pts',(-0.146416087288192,0.000126442170093593,
0.366065504584291));
#14658=CARTESIAN_POINT('Ctrl Pts',(-0.146499294961499,0.00925816812376314,
0.365568242605721));
#14659=CARTESIAN_POINT('Ctrl Pts',(-0.145718277739785,0.0183757049974218,
0.365070980627151));
#14660=CARTESIAN_POINT('Ctrl Pts',(-0.144021710151773,0.0273195705351122,
0.364573718648581));
#14661=CARTESIAN_POINT('Ctrl Pts',(-0.134992913071845,0.0749170536065741,
0.361927388769479));
#14662=CARTESIAN_POINT('Ctrl Pts',(-0.100034284522917,0.117595890322328,
0.359281058890377));
#14663=CARTESIAN_POINT('Ctrl Pts',(-0.0551469387876206,0.135821305661589,
0.356634729011275));
#14664=CARTESIAN_POINT('Ctrl Pts',(-0.0102595930523245,0.15404672100085,
0.353988399132173));
#14665=CARTESIAN_POINT('Ctrl Pts',(0.0445564698693406,0.147818714963618,
0.351342069253072));
#14666=CARTESIAN_POINT('Ctrl Pts',(0.0842110755700531,0.119987943896873,
0.34869573937397));
#14667=CARTESIAN_POINT('Ctrl Pts',(0.123865681270766,0.0921571728301272,
0.346049409494868));
#14668=CARTESIAN_POINT('Ctrl Pts',(0.148358829750526,0.0427236367338667,
0.343403079615766));
#14669=CARTESIAN_POINT('Ctrl Pts',(0.146479621605269,-0.00568615719458776,
0.340756749736664));
#14670=CARTESIAN_POINT('Ctrl Pts',(0.144600413460012,-0.0540959511230416,
0.338110419857562));
#14671=CARTESIAN_POINT('Ctrl Pts',(0.116348848689739,-0.101482002883689,
0.33546408997846));
#14672=CARTESIAN_POINT('Ctrl Pts',(0.0746561129649502,-0.126154971072205,
0.332817760099358));
#14673=CARTESIAN_POINT('Ctrl Pts',(0.0329633772401616,-0.150827939260721,
0.330171430220256));
#14674=CARTESIAN_POINT('Ctrl Pts',(-0.0221705294391424,-0.152787823877104,
0.327525100341154));
#14675=CARTESIAN_POINT('Ctrl Pts',(-0.0655099505772086,-0.131137554898038,
0.324878770462052));
#14676=CARTESIAN_POINT('Ctrl Pts',(-0.108849371715275,-0.109487285918972,
0.322232440582951));
#14677=CARTESIAN_POINT('Ctrl Pts',(-0.140394307312104,-0.0642268633444555,
0.319586110703849));
#14678=CARTESIAN_POINT('Ctrl Pts',(-0.14570614405606,-0.0160726946583056,
0.316939780824747));
#14679=CARTESIAN_POINT('Ctrl Pts',(-0.146291106736525,-0.0107697471190636,
0.316648355411261));
#14680=CARTESIAN_POINT('Ctrl Pts',(-0.146557930734812,-0.0054317060295066,
0.316356929997776));
#14681=CARTESIAN_POINT('Ctrl Pts',(-0.146519404976022,-8.97763884284003E-5,
0.316065504584291));
#14682=CARTESIAN_POINT('Ctrl Pts',(-0.146528765763263,-8.45393868379275E-5,
0.30893449541571));
#14683=CARTESIAN_POINT('Ctrl Pts',(-0.146562807199252,-0.00503327764821679,
0.30920451587328));
#14684=CARTESIAN_POINT('Ctrl Pts',(-0.14633385314783,-0.00997882882536714,
0.30947453633085));
#14685=CARTESIAN_POINT('Ctrl Pts',(-0.145831525524598,-0.0148964553326841,
0.309744556788419));
#14686=CARTESIAN_POINT('Ctrl Pts',(-0.140906503086998,-0.0631108472318147,
0.312391946162679));
#14687=CARTESIAN_POINT('Ctrl Pts',(-0.109703085900295,-0.108640943453547,
0.31503933553694));
#14688=CARTESIAN_POINT('Ctrl Pts',(-0.0665140418604196,-0.13063162118607,
0.3176867249112));
#14689=CARTESIAN_POINT('Ctrl Pts',(-0.0233249978205455,-0.152622298918592,
0.32033411428546));
#14690=CARTESIAN_POINT('Ctrl Pts',(0.0318496730725009,-0.151073558161906,
0.322981503659719));
#14691=CARTESIAN_POINT('Ctrl Pts',(0.0737371373950496,-0.126694801736668,
0.325628893033979));
#14692=CARTESIAN_POINT('Ctrl Pts',(0.115624601717599,-0.10231604531143,
0.328276282408239));
#14693=CARTESIAN_POINT('Ctrl Pts',(0.144224859469651,-0.0551072732176397,
0.3309236717825));
#14694=CARTESIAN_POINT('Ctrl Pts',(0.146437523492708,-0.0066925280449658,
0.33357106115676));
#14695=CARTESIAN_POINT('Ctrl Pts',(0.148650187515766,0.0417222171277085,
0.33621845053102));
#14696=CARTESIAN_POINT('Ctrl Pts',(0.124475257809829,0.0913429353792657,
0.33886583990528));
#14697=CARTESIAN_POINT('Ctrl Pts',(0.0849860939726622,0.119440788885456,
0.34151322927954));
#14698=CARTESIAN_POINT('Ctrl Pts',(0.0454969301354961,0.147538642391646,
0.344160618653799));
#14699=CARTESIAN_POINT('Ctrl Pts',(-0.00930646783289898,0.154113631152469,
0.346808008028059));
#14700=CARTESIAN_POINT('Ctrl Pts',(-0.0543213285795041,0.136154072578339,
0.349455397402319));
#14701=CARTESIAN_POINT('Ctrl Pts',(-0.0993361893261098,0.11819451400421,
0.352102786776579));
#14702=CARTESIAN_POINT('Ctrl Pts',(-0.134562512850926,0.0757004080951257,
0.35475017615084));
#14703=CARTESIAN_POINT('Ctrl Pts',(-0.143864833510727,0.0281362381501331,
0.3573975655251));
#14704=CARTESIAN_POINT('Ctrl Pts',(-0.145664973529558,0.0189318504589563,
0.357909875488637));
#14705=CARTESIAN_POINT('Ctrl Pts',(-0.146494308508217,0.00953759842677947,
0.358422185452174));
#14706=CARTESIAN_POINT('Ctrl Pts',(-0.146408012399712,0.000128195943346294,
0.358934495415711));
#14707=CARTESIAN_POINT('Origin',(0.,0.,0.));
#14708=CARTESIAN_POINT('',(-0.146110491840834,1.12683595067248E-5,0.416065504584291));
#14709=CARTESIAN_POINT('',(-0.146109756335714,8.81622270207575E-6,0.40893449541571));
#14710=CARTESIAN_POINT('',(-0.14635,-1.79227059055215E-17,0.));
#14711=CARTESIAN_POINT('Ctrl Pts',(-0.146110491840834,1.12683595067248E-5,
0.416065504584291));
#14712=CARTESIAN_POINT('Ctrl Pts',(-0.146126798292857,0.0237518011834032,
0.414779555213666));
#14713=CARTESIAN_POINT('Ctrl Pts',(-0.140669750958991,0.0474852665485293,
0.413493605843041));
#14714=CARTESIAN_POINT('Ctrl Pts',(-0.129698698951591,0.0683144158983218,
0.412207656472415));
#14715=CARTESIAN_POINT('Ctrl Pts',(-0.107121587134001,0.111178312051432,
0.409561326593314));
#14716=CARTESIAN_POINT('Ctrl Pts',(-0.0611933749717542,0.141742803557285,
0.406914996714211));
#14717=CARTESIAN_POINT('Ctrl Pts',(-0.0129361277491455,0.146018041789781,
0.40426866683511));
#14718=CARTESIAN_POINT('Ctrl Pts',(0.0353211194734639,0.150293280022276,
0.401622336956008));
#14719=CARTESIAN_POINT('Ctrl Pts',(0.0859074017564354,0.128279264981412,
0.398976007076906));
#14720=CARTESIAN_POINT('Ctrl Pts',(0.115668581836909,0.0900521576926538,
0.396329677197804));
#14721=CARTESIAN_POINT('Ctrl Pts',(0.145429761917382,0.0518250504038959,
0.393683347318702));
#14722=CARTESIAN_POINT('Ctrl Pts',(0.154365839795359,-0.0026151491327561,
0.3910370174396));
#14723=CARTESIAN_POINT('Ctrl Pts',(0.138386632036901,-0.0483503050946702,
0.388390687560498));
#14724=CARTESIAN_POINT('Ctrl Pts',(0.122407424278443,-0.094085461056585,
0.385744357681396));
#14725=CARTESIAN_POINT('Ctrl Pts',(0.0815129308835505,-0.131115573443762,
0.383098027802294));
#14726=CARTESIAN_POINT('Ctrl Pts',(0.0344212048624006,-0.142491377230642,
0.380451697923192));
#14727=CARTESIAN_POINT('Ctrl Pts',(-0.0126705211587486,-0.153867181017521,
0.37780536804409));
#14728=CARTESIAN_POINT('Ctrl Pts',(-0.0659594798061549,-0.139588676204105,
0.375159038164988));
#14729=CARTESIAN_POINT('Ctrl Pts',(-0.101054476324393,-0.106191359083811,
0.372512708285887));
#14730=CARTESIAN_POINT('Ctrl Pts',(-0.129554902927378,-0.0790696072742943,
0.370363640385355));
#14731=CARTESIAN_POINT('Ctrl Pts',(-0.146056480184715,-0.0393390709180539,
0.368214572484823));
#14732=CARTESIAN_POINT('Ctrl Pts',(-0.146416087288192,0.000126442170093593,
0.366065504584291));
#14733=CARTESIAN_POINT('Ctrl Pts',(-0.146408012399712,0.000128195943346294,
0.358934495415711));
#14734=CARTESIAN_POINT('Ctrl Pts',(-0.146048368712081,-0.0390859965171687,
0.361069574826434));
#14735=CARTESIAN_POINT('Ctrl Pts',(-0.1297855810823,-0.0785633296797545,
0.363204654237157));
#14736=CARTESIAN_POINT('Ctrl Pts',(-0.101613371150224,-0.105657280969165,
0.36533973364788));
#14737=CARTESIAN_POINT('Ctrl Pts',(-0.066681270335132,-0.139252396162569,
0.36798712302214));
#14738=CARTESIAN_POINT('Ctrl Pts',(-0.0134387509101597,-0.153808392568477,
0.370634512396399));
#14739=CARTESIAN_POINT('Ctrl Pts',(0.0337263783221333,-0.142657876135818,
0.373281901770659));
#14740=CARTESIAN_POINT('Ctrl Pts',(0.0808915075544263,-0.13150735970316,
0.375929291144919));
#14741=CARTESIAN_POINT('Ctrl Pts',(0.12197924659404,-0.0946503304319347,
0.378576680519179));
#14742=CARTESIAN_POINT('Ctrl Pts',(0.138169300408926,-0.0489692009616054,
0.38122406989344));
#14743=CARTESIAN_POINT('Ctrl Pts',(0.154359354223812,-0.00328807149127619,
0.3838714592677));
#14744=CARTESIAN_POINT('Ctrl Pts',(0.14565172281397,0.0512171581781573,
0.38651884864196));
#14745=CARTESIAN_POINT('Ctrl Pts',(0.11603494864959,0.0895802930905963,
0.38916623801622));
#14746=CARTESIAN_POINT('Ctrl Pts',(0.0864181744852101,0.127943428003035,
0.39181362739048));
#14747=CARTESIAN_POINT('Ctrl Pts',(0.0358922575662923,0.15016446815848,
0.394461016764739));
#14748=CARTESIAN_POINT('Ctrl Pts',(-0.0123993367959677,0.146065035738641,
0.397108406138999));
#14749=CARTESIAN_POINT('Ctrl Pts',(-0.0606909311582276,0.141965603318802,
0.399755795513259));
#14750=CARTESIAN_POINT('Ctrl Pts',(-0.106748202963829,0.111545698323679,
0.40240318488752));
#14751=CARTESIAN_POINT('Ctrl Pts',(-0.129474555904152,0.0687391998188283,
0.40505057426178));
#14752=CARTESIAN_POINT('Ctrl Pts',(-0.140588317483115,0.0478057390183907,
0.406345214646423));
#14753=CARTESIAN_POINT('Ctrl Pts',(-0.146122589096428,0.0239100770892618,
0.407639855031067));
#14754=CARTESIAN_POINT('Ctrl Pts',(-0.146109756335714,8.81622270207575E-6,
0.40893449541571));
#14755=CARTESIAN_POINT('Origin',(0.,0.,0.));
#14756=CARTESIAN_POINT('',(-0.146374718215768,-0.000132229735885947,0.466065504584291));
#14757=CARTESIAN_POINT('',(-0.146375609273197,-0.000132432188538665,0.458934495415711));
#14758=CARTESIAN_POINT('',(-0.14635,-1.79227059055215E-17,0.));
#14759=CARTESIAN_POINT('Ctrl Pts',(-0.146374718215768,-0.000132229735885947,
0.466065504584291));
#14760=CARTESIAN_POINT('Ctrl Pts',(-0.146022504084922,0.0379941335185874,
0.46399086782161));
#14761=CARTESIAN_POINT('Ctrl Pts',(-0.130761950520226,0.0763703265456945,
0.46191623105893));
#14762=CARTESIAN_POINT('Ctrl Pts',(-0.103994021541854,0.103314352404769,
0.45984159429625));
#14763=CARTESIAN_POINT('Ctrl Pts',(-0.0698498419286355,0.137683154682254,
0.457195264417148));
#14764=CARTESIAN_POINT('Ctrl Pts',(-0.0169824611430249,0.153451124186949,
0.454548934538046));
#14765=CARTESIAN_POINT('Ctrl Pts',(0.030409888879481,0.143401013202843,
0.451902604658944));
#14766=CARTESIAN_POINT('Ctrl Pts',(0.0778022389019875,0.133350902218736,
0.449256274779842));
#14767=CARTESIAN_POINT('Ctrl Pts',(0.119719558161389,0.0974827107458278,
0.44660994490074));
#14768=CARTESIAN_POINT('Ctrl Pts',(0.136975630157447,0.0522138743269898,
0.443963615021638));
#14769=CARTESIAN_POINT('Ctrl Pts',(0.154231702153504,0.00694503790815254,
0.441317285142536));
#14770=CARTESIAN_POINT('Ctrl Pts',(0.146826526886218,-0.0477244434566137,
0.438670955263434));
#14771=CARTESIAN_POINT('Ctrl Pts',(0.118149569579287,-0.0867714880447125,
0.436024625384332));
#14772=CARTESIAN_POINT('Ctrl Pts',(0.0894726122723542,-0.125818532632812,
0.43337829550523));
#14773=CARTESIAN_POINT('Ctrl Pts',(0.0395238729257754,-0.149243140444243,
0.430731965626129));
#14774=CARTESIAN_POINT('Ctrl Pts',(-0.00883432462988853,-0.146323499949933,
0.428085635747027));
#14775=CARTESIAN_POINT('Ctrl Pts',(-0.0571925221855517,-0.143403859455623,
0.425439305867925));
#14776=CARTESIAN_POINT('Ctrl Pts',(-0.1039601779503,-0.114139970655572,
0.422792975988823));
#14777=CARTESIAN_POINT('Ctrl Pts',(-0.127731000096207,-0.0719263758553634,
0.420146646109721));
#14778=CARTESIAN_POINT('Ctrl Pts',(-0.139950702323481,-0.0502259249733931,
0.418786265601244));
#14779=CARTESIAN_POINT('Ctrl Pts',(-0.146093241566443,-0.0251033736724598,
0.417425885092767));
#14780=CARTESIAN_POINT('Ctrl Pts',(-0.146110491840834,1.12683595067248E-5,
0.416065504584291));
#14781=CARTESIAN_POINT('Ctrl Pts',(-0.146109756335714,8.81622270207575E-6,
0.40893449541571));
#14782=CARTESIAN_POINT('Ctrl Pts',(-0.146096347589706,-0.0249652282079418,
0.410287244405327));
#14783=CARTESIAN_POINT('Ctrl Pts',(-0.140026707259891,-0.049945385460595,
0.411639993394943));
#14784=CARTESIAN_POINT('Ctrl Pts',(-0.127937780377622,-0.0715588049813403,
0.412992742384559));
#14785=CARTESIAN_POINT('Ctrl Pts',(-0.104279217835726,-0.113857219262079,
0.415640131758819));
#14786=CARTESIAN_POINT('Ctrl Pts',(-0.0575666586768896,-0.14326095580898,
0.41828752113308));
#14787=CARTESIAN_POINT('Ctrl Pts',(-0.00919685447762893,-0.146301592903247,
0.42093491050734));
#14788=CARTESIAN_POINT('Ctrl Pts',(0.039172949721632,-0.149342229997515,
0.4235822998816));
#14789=CARTESIAN_POINT('Ctrl Pts',(0.089199998961318,-0.126019767639148,
0.426229689255859));
#14790=CARTESIAN_POINT('Ctrl Pts',(0.117969334952632,-0.0870170915920772,
0.428877078630119));
#14791=CARTESIAN_POINT('Ctrl Pts',(0.146738670943946,-0.0480144155450057,
0.431524468004379));
#14792=CARTESIAN_POINT('Ctrl Pts',(0.154250293686888,0.00666847419077017,
0.43417185737864));
#14793=CARTESIAN_POINT('Ctrl Pts',(0.137063494116028,0.051984005222912,
0.4368192467529));
#14794=CARTESIAN_POINT('Ctrl Pts',(0.119876694545168,0.0972995362550541,
0.43946663612716));
#14795=CARTESIAN_POINT('Ctrl Pts',(0.0779914726605056,0.133247708583562,
0.442114025501419));
#14796=CARTESIAN_POINT('Ctrl Pts',(0.0305934116013849,0.143362412733947,
0.444761414875679));
#14797=CARTESIAN_POINT('Ctrl Pts',(-0.0168046494577345,0.153477116884331,
0.447408804249939));
#14798=CARTESIAN_POINT('Ctrl Pts',(-0.0697155496913122,0.137758352856595,
0.4500561936242));
#14799=CARTESIAN_POINT('Ctrl Pts',(-0.103903378920715,0.103406122000434,
0.45270358299846));
#14800=CARTESIAN_POINT('Ctrl Pts',(-0.130724942802416,0.0764555792150183,
0.45478055380421));
#14801=CARTESIAN_POINT('Ctrl Pts',(-0.146022533856355,0.0380362146017157,
0.45685752460996));
#14802=CARTESIAN_POINT('Ctrl Pts',(-0.146375609273197,-0.000132432188538665,
0.458934495415711));
#14803=CARTESIAN_POINT('Origin',(0.,0.,0.));
#14804=CARTESIAN_POINT('',(-0.146548608312775,6.99729089778146E-5,0.516065504584291));
#14805=CARTESIAN_POINT('',(-0.146550766805835,6.86360251013434E-5,0.508934495415711));
#14806=CARTESIAN_POINT('',(-0.14635,-1.79227059055215E-17,0.));
#14807=CARTESIAN_POINT('Ctrl Pts',(-0.146548608312775,6.99729089778146E-5,
0.516065504584291));
#14808=CARTESIAN_POINT('Ctrl Pts',(-0.146572081366671,0.00404546554386884,
0.515848510308657));
#14809=CARTESIAN_POINT('Ctrl Pts',(-0.146424333269732,0.00801918670503405,
0.515631516033023));
#14810=CARTESIAN_POINT('Ctrl Pts',(-0.146099725131082,0.0119784074854107,
0.51541452175739));
#14811=CARTESIAN_POINT('Ctrl Pts',(-0.142141002193345,0.06026265009261,
0.512768191878288));
#14812=CARTESIAN_POINT('Ctrl Pts',(-0.111878319621163,0.106390286678145,
0.510121861999186));
#14813=CARTESIAN_POINT('Ctrl Pts',(-0.069163383343408,0.129247972261684,
0.507475532120084));
#14814=CARTESIAN_POINT('Ctrl Pts',(-0.0264484470656534,0.152105657845224,
0.504829202240982));
#14815=CARTESIAN_POINT('Ctrl Pts',(0.0287187429176733,0.151693392426768,
0.50218287236188));
#14816=CARTESIAN_POINT('Ctrl Pts',(0.07108729581893,0.128199876374419,0.499536542482778));
#14817=CARTESIAN_POINT('Ctrl Pts',(0.113455848720186,0.10470636032207,0.496890212603677));
#14818=CARTESIAN_POINT('Ctrl Pts',(0.143025764539373,0.0581315936358261,
0.494243882724575));
#14819=CARTESIAN_POINT('Ctrl Pts',(0.146262427589597,0.00979357977770552,
0.491597552845473));
#14820=CARTESIAN_POINT('Ctrl Pts',(0.149499090639821,-0.0385444340804161,
0.488951222966371));
#14821=CARTESIAN_POINT('Ctrl Pts',(0.126402500921083,-0.0886456951104151,
0.486304893087269));
#14822=CARTESIAN_POINT('Ctrl Pts',(0.087544330920799,-0.117578067907642,
0.483658563208167));
#14823=CARTESIAN_POINT('Ctrl Pts',(0.0486861609205161,-0.146510440704867,
0.481012233329065));
#14824=CARTESIAN_POINT('Ctrl Pts',(-0.00593358936131212,-0.154273925269321,
0.478365903449963));
#14825=CARTESIAN_POINT('Ctrl Pts',(-0.0513146009011563,-0.137315052574797,
0.475719573570861));
#14826=CARTESIAN_POINT('Ctrl Pts',(-0.0966956124410008,-0.120356179880273,
0.473073243691759));
#14827=CARTESIAN_POINT('Ctrl Pts',(-0.132837885238862,-0.078674949926771,
0.470426913812657));
#14828=CARTESIAN_POINT('Ctrl Pts',(-0.14319853241738,-0.0313495174248821,
0.467780583933555));
#14829=CARTESIAN_POINT('Ctrl Pts',(-0.145436768368387,-0.0211256884885646,
0.467208890817134));
#14830=CARTESIAN_POINT('Ctrl Pts',(-0.146471775395962,-0.0106384445195334,
0.466637197700712));
#14831=CARTESIAN_POINT('Ctrl Pts',(-0.146374718215768,-0.000132229735885947,
0.466065504584291));
#14832=CARTESIAN_POINT('Ctrl Pts',(-0.146375609273197,-0.000132432188538665,
0.458934495415711));
#14833=CARTESIAN_POINT('Ctrl Pts',(-0.146472577787773,-0.0106150565970108,
0.45950491398422));
#14834=CARTESIAN_POINT('Ctrl Pts',(-0.145442327125792,-0.021078770125739,
0.46007533255273));
#14835=CARTESIAN_POINT('Ctrl Pts',(-0.143213999951756,-0.0312807998000163,
0.460645751121239));
#14836=CARTESIAN_POINT('Ctrl Pts',(-0.132872033528166,-0.0786297930597184,
0.463293140495499));
#14837=CARTESIAN_POINT('Ctrl Pts',(-0.0967233424557573,-0.120342081894533,
0.465940529869759));
#14838=CARTESIAN_POINT('Ctrl Pts',(-0.0513258840937604,-0.13731129538499,
0.46858791924402));
#14839=CARTESIAN_POINT('Ctrl Pts',(-0.00592842573176499,-0.154280508875447,
0.47123530861828));
#14840=CARTESIAN_POINT('Ctrl Pts',(0.0487177999198187,-0.146506647021548,
0.47388269799254));
#14841=CARTESIAN_POINT('Ctrl Pts',(0.0875820145025328,-0.117550537871965,
0.476530087366799));
#14842=CARTESIAN_POINT('Ctrl Pts',(0.126446229085248,-0.0885944287223814,
0.47917747674106));
#14843=CARTESIAN_POINT('Ctrl Pts',(0.149528432599094,-0.0384560722771122,
0.481824866115319));
#14844=CARTESIAN_POINT('Ctrl Pts',(0.146255790172295,0.0098985887573764,
0.484472255489579));
#14845=CARTESIAN_POINT('Ctrl Pts',(0.142983147745498,0.0582532497918637,
0.487119644863839));
#14846=CARTESIAN_POINT('Ctrl Pts',(0.113355659378058,0.10482421541557,0.4897670342381));
#14847=CARTESIAN_POINT('Ctrl Pts',(0.0709442366160257,0.128279591164298,
0.49241442361236));
#14848=CARTESIAN_POINT('Ctrl Pts',(0.0285328138539934,0.151734966913027,
0.49506181298662));
#14849=CARTESIAN_POINT('Ctrl Pts',(-0.0266625433026316,0.152074752786777,
0.497709202360879));
#14850=CARTESIAN_POINT('Ctrl Pts',(-0.0693595260588707,0.129143309401606,
0.500356591735139));
#14851=CARTESIAN_POINT('Ctrl Pts',(-0.11205650881511,0.106211866016435,
0.503003981109399));
#14852=CARTESIAN_POINT('Ctrl Pts',(-0.142255117170964,0.060009193372344,
0.505651370483659));
#14853=CARTESIAN_POINT('Ctrl Pts',(-0.146122837288996,0.0116984888307781,
0.50829875985792));
#14854=CARTESIAN_POINT('Ctrl Pts',(-0.146432431239741,0.00783142983325791,
0.508510671710517));
#14855=CARTESIAN_POINT('Ctrl Pts',(-0.14657331536999,0.00395086404934249,
0.508722583563114));
#14856=CARTESIAN_POINT('Ctrl Pts',(-0.146550766805835,6.86360251013434E-5,
0.508934495415711));
#14857=CARTESIAN_POINT('Origin',(0.,0.,0.));
#14858=CARTESIAN_POINT('',(-0.146165204287215,8.83645032875094E-5,0.566065504584291));
#14859=CARTESIAN_POINT('',(-0.146168951232552,9.12430751481418E-5,0.558934495415711));
#14860=CARTESIAN_POINT('',(-0.14635,-1.79227059055215E-17,0.));
#14861=CARTESIAN_POINT('Ctrl Pts',(-0.146165204287215,8.83645032875094E-5,
0.566065504584291));
#14862=CARTESIAN_POINT('Ctrl Pts',(-0.146267412293664,0.0186373661349918,
0.565059822916602));
#14863=CARTESIAN_POINT('Ctrl Pts',(-0.142994166834961,0.0371516370495788,
0.564054141248913));
#14864=CARTESIAN_POINT('Ctrl Pts',(-0.136179985035193,0.0542551712289143,
0.563048459581224));
#14865=CARTESIAN_POINT('Ctrl Pts',(-0.118249288396568,0.0992610562830057,
0.560402129702122));
#14866=CARTESIAN_POINT('Ctrl Pts',(-0.0758005933416487,0.134498778989873,
0.55775579982302));
#14867=CARTESIAN_POINT('Ctrl Pts',(-0.0282633354322908,0.143839479279877,
0.555109469943918));
#14868=CARTESIAN_POINT('Ctrl Pts',(0.0192739224770691,0.153180179569881,
0.552463140064816));
#14869=CARTESIAN_POINT('Ctrl Pts',(0.0718997432408687,0.136623857443018,
0.549816810185715));
#14870=CARTESIAN_POINT('Ctrl Pts',(0.105526460745998,0.101748602013432,
0.547170480306613));
#14871=CARTESIAN_POINT('Ctrl Pts',(0.139153178251127,0.0668733465838454,
0.544524150427511));
#14872=CARTESIAN_POINT('Ctrl Pts',(0.153780792497586,0.0136791578515372,
0.541877820548409));
#14873=CARTESIAN_POINT('Ctrl Pts',(0.142714014311998,-0.0334861471092027,
0.539231490669307));
#14874=CARTESIAN_POINT('Ctrl Pts',(0.13164723612641,-0.0806514520699426,
0.536585160790205));
#14875=CARTESIAN_POINT('Ctrl Pts',(0.0948860655087725,-0.121787873259113,
0.533938830911103));
#14876=CARTESIAN_POINT('Ctrl Pts',(0.0492566686055307,-0.138066623508903,
0.531292501032001));
#14877=CARTESIAN_POINT('Ctrl Pts',(0.00362727170228945,-0.154345373758693,
0.528646171152899));
#14878=CARTESIAN_POINT('Ctrl Pts',(-0.050870351486557,-0.145766453069103,
0.525999841273797));
#14879=CARTESIAN_POINT('Ctrl Pts',(-0.089291781429334,-0.116256568409877,
0.523353511394695));
#14880=CARTESIAN_POINT('Ctrl Pts',(-0.124562723435938,-0.0891664410515947,
0.520924175791227));
#14881=CARTESIAN_POINT('Ctrl Pts',(-0.146285818313441,-0.0444372186796531,
0.518494840187759));
#14882=CARTESIAN_POINT('Ctrl Pts',(-0.146548608312775,6.99729089778146E-5,
0.516065504584291));
#14883=CARTESIAN_POINT('Ctrl Pts',(-0.146550766805835,6.86360251013434E-5,
0.508934495415711));
#14884=CARTESIAN_POINT('Ctrl Pts',(-0.146291618860727,-0.0445493453248537,
0.511369972937373));
#14885=CARTESIAN_POINT('Ctrl Pts',(-0.124445252016267,-0.0893868858389474,
0.513805450459036));
#14886=CARTESIAN_POINT('Ctrl Pts',(-0.0890226177929609,-0.116463349340462,
0.516240927980699));
#14887=CARTESIAN_POINT('Ctrl Pts',(-0.0505178462986829,-0.145895746531099,
0.518888317354959));
#14888=CARTESIAN_POINT('Ctrl Pts',(0.00402852857008221,-0.154341804473332,
0.52153570672922));
#14889=CARTESIAN_POINT('Ctrl Pts',(0.0496314652424392,-0.137932794781367,
0.52418309610348));
#14890=CARTESIAN_POINT('Ctrl Pts',(0.0952344019147948,-0.121523785089403,
0.52683048547774));
#14891=CARTESIAN_POINT('Ctrl Pts',(0.131893900390741,-0.0802597077632436,
0.529477874851999));
#14892=CARTESIAN_POINT('Ctrl Pts',(0.14281802728161,-0.0330416298281342,
0.532125264226259));
#14893=CARTESIAN_POINT('Ctrl Pts',(0.153742154172479,0.0141764481069759,
0.53477265360052));
#14894=CARTESIAN_POINT('Ctrl Pts',(0.138930909478268,0.0673485266510362,
0.53742004297478));
#14895=CARTESIAN_POINT('Ctrl Pts',(0.105168604077417,0.102119062543277,
0.54006743234904));
#14896=CARTESIAN_POINT('Ctrl Pts',(0.0714062986765666,0.136889598435517,
0.5427148217233));
#14897=CARTESIAN_POINT('Ctrl Pts',(0.018692932569077,0.153258591675938,
0.545362211097559));
#14898=CARTESIAN_POINT('Ctrl Pts',(-0.0288260648428939,0.143728202535144,
0.548009600471819));
#14899=CARTESIAN_POINT('Ctrl Pts',(-0.0763450622548654,0.13419781339435,
0.550656989846079));
#14900=CARTESIAN_POINT('Ctrl Pts',(-0.118669690971318,0.0987680418723385,
0.55330437922034));
#14901=CARTESIAN_POINT('Ctrl Pts',(-0.136413096952957,0.0536675432455532,
0.5559517685946));
#14902=CARTESIAN_POINT('Ctrl Pts',(-0.143076734904351,0.036729792140314,
0.556946010868304));
#14903=CARTESIAN_POINT('Ctrl Pts',(-0.146273385252938,0.0184280612467595,
0.557940253142007));
#14904=CARTESIAN_POINT('Ctrl Pts',(-0.146168951232552,9.12430751481418E-5,
0.558934495415711));
#14905=CARTESIAN_POINT('Origin',(0.,0.,0.));
#14906=CARTESIAN_POINT('',(-0.146227179098081,-0.000117664897458569,0.616065504584291));
#14907=CARTESIAN_POINT('',(-0.146218520919543,-0.000115076211918358,0.608934495415711));
#14908=CARTESIAN_POINT('',(-0.14635,-1.79227059055215E-17,0.));
#14909=CARTESIAN_POINT('Ctrl Pts',(-0.146227179098081,-0.000117664897458569,
0.616065504584291));
#14910=CARTESIAN_POINT('Ctrl Pts',(-0.145977603365176,0.0329427899635141,
0.614271135524546));
#14911=CARTESIAN_POINT('Ctrl Pts',(-0.134874795495675,0.0661550248562671,
0.612476766464802));
#14912=CARTESIAN_POINT('Ctrl Pts',(-0.114309815624116,0.091770790457776,
0.610682397405058));
#14913=CARTESIAN_POINT('Ctrl Pts',(-0.0839806476072558,0.129548841477563,
0.608036067525956));
#14914=CARTESIAN_POINT('Ctrl Pts',(-0.0330710111925292,0.150804375664025,
0.605389737646855));
#14915=CARTESIAN_POINT('Ctrl Pts',(0.0151169520838501,0.145808400611758,
0.602743407767753));
#14916=CARTESIAN_POINT('Ctrl Pts',(0.0633049153602295,0.140812425559491,
0.600097077888651));
#14917=CARTESIAN_POINT('Ctrl Pts',(0.108771205498262,0.109564941268491,
0.597450748009549));
#14918=CARTESIAN_POINT('Ctrl Pts',(0.130705186191441,0.0663684129079872,
0.594804418130447));
#14919=CARTESIAN_POINT('Ctrl Pts',(0.152639166884621,0.023171884547483,
0.592158088251345));
#14920=CARTESIAN_POINT('Ctrl Pts',(0.151040838132949,-0.0319736878825246,
0.589511758372243));
#14921=CARTESIAN_POINT('Ctrl Pts',(0.126641780152193,-0.0738273082886534,
0.586865428493141));
#14922=CARTESIAN_POINT('Ctrl Pts',(0.102242722171437,-0.115680928694782,
0.584219098614039));
#14923=CARTESIAN_POINT('Ctrl Pts',(0.0550429349615966,-0.14424259707703,
0.581572768734937));
#14924=CARTESIAN_POINT('Ctrl Pts',(0.00664650371163741,-0.14643918846291,
0.578926438855836));
#14925=CARTESIAN_POINT('Ctrl Pts',(-0.0417499275383225,-0.148635779848789,
0.576280108976733));
#14926=CARTESIAN_POINT('Ctrl Pts',(-0.0913430028284016,-0.1244672942383,
0.573633779097631));
#14927=CARTESIAN_POINT('Ctrl Pts',(-0.119433191362276,-0.0849960277323969,
0.570987449218529));
#14928=CARTESIAN_POINT('Ctrl Pts',(-0.136848298201485,-0.0605249807527623,
0.569346801007117));
#14929=CARTESIAN_POINT('Ctrl Pts',(-0.145998464265635,-0.0301720919893573,
0.567706152795704));
#14930=CARTESIAN_POINT('Ctrl Pts',(-0.146165204287215,8.83645032875094E-5,
0.566065504584291));
#14931=CARTESIAN_POINT('Ctrl Pts',(-0.146168951232552,9.12430751481418E-5,
0.558934495415711));
#14932=CARTESIAN_POINT('Ctrl Pts',(-0.145995306636495,-0.0303977620653178,
0.560587642516267));
#14933=CARTESIAN_POINT('Ctrl Pts',(-0.136695352934655,-0.0609837708898569,
0.562240789616823));
#14934=CARTESIAN_POINT('Ctrl Pts',(-0.119031718004195,-0.0855580991331628,
0.563893936717379));
#14935=CARTESIAN_POINT('Ctrl Pts',(-0.090744749826965,-0.124912017153538,
0.566541326091639));
#14936=CARTESIAN_POINT('Ctrl Pts',(-0.0410086302256792,-0.148848627462727,
0.5691887154659));
#14937=CARTESIAN_POINT('Ctrl Pts',(0.00739494322942312,-0.146403732988417,
0.57183610484016));
#14938=CARTESIAN_POINT('Ctrl Pts',(0.0557985166845234,-0.143958838514108,
0.57448349421442));
#14939=CARTESIAN_POINT('Ctrl Pts',(0.10286954399344,-0.1151324392563,0.57713088358868));
#14940=CARTESIAN_POINT('Ctrl Pts',(0.127047076753504,-0.0731285067993286,
0.579778272962939));
#14941=CARTESIAN_POINT('Ctrl Pts',(0.151224609513568,-0.031124574342357,
0.5824256623372));
#14942=CARTESIAN_POINT('Ctrl Pts',(0.15250864772478,0.0240568913137802,
0.58507305171146));
#14943=CARTESIAN_POINT('Ctrl Pts',(0.130311035929276,0.0671399443948921,
0.58772044108572));
#14944=CARTESIAN_POINT('Ctrl Pts',(0.108113424133771,0.110222997476006,
0.59036783045998));
#14945=CARTESIAN_POINT('Ctrl Pts',(0.0624341623315493,0.141207637982093,
0.593015219834239));
#14946=CARTESIAN_POINT('Ctrl Pts',(0.0141966988324609,0.145901308974836,
0.595662609208499));
#14947=CARTESIAN_POINT('Ctrl Pts',(-0.0340407646666261,0.150594979967579,
0.598309998582759));
#14948=CARTESIAN_POINT('Ctrl Pts',(-0.0848364298625779,0.128997681446978,
0.60095738795702));
#14949=CARTESIAN_POINT('Ctrl Pts',(-0.114923272877171,0.091002085522857,
0.60360477733128));
#14950=CARTESIAN_POINT('Ctrl Pts',(-0.135113526827902,0.0655045372973676,
0.60538135002609));
#14951=CARTESIAN_POINT('Ctrl Pts',(-0.14597798884013,0.0326223532682757,
0.6071579227209));
#14952=CARTESIAN_POINT('Ctrl Pts',(-0.146218520919543,-0.000115076211918358,
0.608934495415711));
#14953=CARTESIAN_POINT('Origin',(0.,0.,0.));
#14954=CARTESIAN_POINT('',(-0.146586033401767,-2.15382961294558E-5,0.66606550458429));
#14955=CARTESIAN_POINT('',(-0.146582846697157,-3.00215943766004E-5,0.65893449541571));
#14956=CARTESIAN_POINT('',(-0.14635,-1.79227059055215E-17,0.));
#14957=CARTESIAN_POINT('Ctrl Pts',(-0.146586033401767,-2.15382961294558E-5,
0.66606550458429));
#14958=CARTESIAN_POINT('Ctrl Pts',(-0.146488810225965,0.0472697707580183,
0.663482448132491));
#14959=CARTESIAN_POINT('Ctrl Pts',(-0.121516563758978,0.0946492637554097,
0.660899391680692));
#14960=CARTESIAN_POINT('Ctrl Pts',(-0.0824084263440199,0.121233094478226,
0.658316335228893));
#14961=CARTESIAN_POINT('Ctrl Pts',(-0.0423423130056393,0.148468111155377,
0.655670005349791));
#14962=CARTESIAN_POINT('Ctrl Pts',(0.0125607065496858,0.153876184485078,
0.653023675470689));
#14963=CARTESIAN_POINT('Ctrl Pts',(0.0571706564953393,0.134981954220393,
0.650377345591587));
#14964=CARTESIAN_POINT('Ctrl Pts',(0.101780606440992,0.116087723955709,
0.647731015712485));
#14965=CARTESIAN_POINT('Ctrl Pts',(0.136097486776972,0.0728911900966409,
0.645084685833384));
#14966=CARTESIAN_POINT('Ctrl Pts',(0.144413921474191,0.0251640857912735,
0.642438355954282));
#14967=CARTESIAN_POINT('Ctrl Pts',(0.152730356171409,-0.0225630185140953,
0.63979202607518));
#14968=CARTESIAN_POINT('Ctrl Pts',(0.135046345229863,-0.0748206932657649,
0.637145696196077));
#14969=CARTESIAN_POINT('Ctrl Pts',(0.0994561386758346,-0.10768977857233,
0.634499366316975));
#14970=CARTESIAN_POINT('Ctrl Pts',(0.0638659321218069,-0.140558863878895,
0.631853036437873));
#14971=CARTESIAN_POINT('Ctrl Pts',(0.0103695299552984,-0.154039359740357,
0.629206706558772));
#14972=CARTESIAN_POINT('Ctrl Pts',(-0.0365469229059137,-0.141961031115491,
0.62656037667967));
#14973=CARTESIAN_POINT('Ctrl Pts',(-0.0834633757671259,-0.129882702490626,
0.623914046800568));
#14974=CARTESIAN_POINT('Ctrl Pts',(-0.123799879323041,-0.0922455493794331,
0.621267716921466));
#14975=CARTESIAN_POINT('Ctrl Pts',(-0.139093781291504,-0.0462766888972804,
0.618621387042364));
#14976=CARTESIAN_POINT('Ctrl Pts',(-0.14401750805555,-0.0314774500153124,
0.617769426223006));
#14977=CARTESIAN_POINT('Ctrl Pts',(-0.14634567687575,-0.0158146654998378,
0.616917465403648));
#14978=CARTESIAN_POINT('Ctrl Pts',(-0.146227179098081,-0.000117664897458569,
0.616065504584291));
#14979=CARTESIAN_POINT('Ctrl Pts',(-0.146218520919543,-0.000115076211918358,
0.608934495415711));
#14980=CARTESIAN_POINT('Ctrl Pts',(-0.1463364217222,-0.0161618722236638,
0.60980531209516));
#14981=CARTESIAN_POINT('Ctrl Pts',(-0.143901781624712,-0.032173889023867,
0.61067612877461));
#14982=CARTESIAN_POINT('Ctrl Pts',(-0.138761720114909,-0.0472643972675185,
0.611546945454059));
#14983=CARTESIAN_POINT('Ctrl Pts',(-0.123135303504819,-0.0931413908061287,
0.614194334828319));
#14984=CARTESIAN_POINT('Ctrl Pts',(-0.0825044494514074,-0.130501484555709,
0.616841724202579));
#14985=CARTESIAN_POINT('Ctrl Pts',(-0.0354801761942514,-0.142231836504824,
0.619489113576839));
#14986=CARTESIAN_POINT('Ctrl Pts',(0.0115440970629072,-0.15396218845394,
0.6221365029511));
#14987=CARTESIAN_POINT('Ctrl Pts',(0.0649617895238099,-0.140062798602586,
0.624783892325359));
#14988=CARTESIAN_POINT('Ctrl Pts',(0.100304854137336,-0.106900301471969,
0.627431281699619));
#14989=CARTESIAN_POINT('Ctrl Pts',(0.135647918750861,-0.0737378043413545,
0.630078671073879));
#14990=CARTESIAN_POINT('Ctrl Pts',(0.15291635551701,-0.0213121999314781,
0.63272606044814));
#14991=CARTESIAN_POINT('Ctrl Pts',(0.144200333369931,0.026362891994447,
0.6353734498224));
#14992=CARTESIAN_POINT('Ctrl Pts',(0.135484311222852,0.0740379839203748,
0.63802083919666));
#14993=CARTESIAN_POINT('Ctrl Pts',(0.100783830162543,0.11696256336235,0.640668228570919));
#14994=CARTESIAN_POINT('Ctrl Pts',(0.055993492972559,0.135474968031154,
0.643315617945179));
#14995=CARTESIAN_POINT('Ctrl Pts',(0.0112031557825773,0.153987372699956,
0.64596300731944));
#14996=CARTESIAN_POINT('Ctrl Pts',(-0.04367703753708,0.148087602595587,
0.6486103966937));
#14997=CARTESIAN_POINT('Ctrl Pts',(-0.0835091394177698,0.120478055479053,
0.65125778606796));
#14998=CARTESIAN_POINT('Ctrl Pts',(-0.122009894390588,0.0937913289882395,
0.653816689183877));
#14999=CARTESIAN_POINT('Ctrl Pts',(-0.146451680634158,0.0468218259492564,
0.656375592299793));
#15000=CARTESIAN_POINT('Ctrl Pts',(-0.146582846697157,-3.00215943766004E-5,
0.65893449541571));
#15001=CARTESIAN_POINT('Origin',(0.,0.,0.));
#15002=CARTESIAN_POINT('',(-0.146290249280603,0.000131112932912382,0.716065504584291));
#15003=CARTESIAN_POINT('',(-0.146307221518699,0.000133045872591754,0.708934495415711));
#15004=CARTESIAN_POINT('',(-0.14635,-1.79227059055215E-17,0.));
#15005=CARTESIAN_POINT('Ctrl Pts',(-0.146290249280603,0.000131112932912382,
0.716065504584291));
#15006=CARTESIAN_POINT('Ctrl Pts',(-0.146406294125046,0.0134819654399978,
0.715340090619538));
#15007=CARTESIAN_POINT('Ctrl Pts',(-0.144729088574721,0.0268041890186768,
0.714614676654786));
#15008=CARTESIAN_POINT('Ctrl Pts',(-0.141142411757643,0.0395908011096033,
0.713889262690033));
#15009=CARTESIAN_POINT('Ctrl Pts',(-0.128058117149462,0.0862367098911347,
0.711242932810931));
#15010=CARTESIAN_POINT('Ctrl Pts',(-0.0895623832093418,0.125754646095387,
0.708596602931829));
#15011=CARTESIAN_POINT('Ctrl Pts',(-0.0432753130058998,0.140056628595385,
0.705950273052727));
#15012=CARTESIAN_POINT('Ctrl Pts',(0.00301175719754219,0.154358611095384,
0.703303943173625));
#15013=CARTESIAN_POINT('Ctrl Pts',(0.0570901636643063,0.143444639891129,
0.700657613294523));
#15014=CARTESIAN_POINT('Ctrl Pts',(0.0942073689518517,0.11231021130972,
0.698011283415421));
#15015=CARTESIAN_POINT('Ctrl Pts',(0.131324574239397,0.0811757827283121,
0.695364953536319));
#15016=CARTESIAN_POINT('Ctrl Pts',(0.151480578347723,0.0298208967697505,
0.692718623657217));
#15017=CARTESIAN_POINT('Ctrl Pts',(0.145449661086834,-0.0182485073085286,
0.690072293778115));
#15018=CARTESIAN_POINT('Ctrl Pts',(0.139418743825945,-0.0663179113868083,
0.687425963899014));
#15019=CARTESIAN_POINT('Ctrl Pts',(0.107200905195838,-0.111101833584806,
0.684779634019911));
#15020=CARTESIAN_POINT('Ctrl Pts',(0.0635427568131047,-0.132101968137704,
0.68213330414081));
#15021=CARTESIAN_POINT('Ctrl Pts',(0.0198846084303716,-0.153102102690602,
0.679486974261708));
#15022=CARTESIAN_POINT('Ctrl Pts',(-0.0352138497049885,-0.150318449598402,
0.676840644382606));
#15023=CARTESIAN_POINT('Ctrl Pts',(-0.0765331864534889,-0.125025130675956,
0.674194314503504));
#15024=CARTESIAN_POINT('Ctrl Pts',(-0.117852523201989,-0.0997318117535095,
0.671547984624402));
#15025=CARTESIAN_POINT('Ctrl Pts',(-0.14539273856363,-0.0519288270008166,
0.6689016547453));
#15026=CARTESIAN_POINT('Ctrl Pts',(-0.146548242683733,-0.00349635461217019,
0.666255324866198));
#15027=CARTESIAN_POINT('Ctrl Pts',(-0.146575870647472,-0.00233834005587287,
0.666192051438896));
#15028=CARTESIAN_POINT('Ctrl Pts',(-0.146588414938392,-0.00117996563262623,
0.666128778011593));
#15029=CARTESIAN_POINT('Ctrl Pts',(-0.146586033401767,-2.15382961294558E-5,
0.66606550458429));
#15030=CARTESIAN_POINT('Ctrl Pts',(-0.146582846697157,-3.00215943766004E-5,
0.65893449541571));
#15031=CARTESIAN_POINT('Ctrl Pts',(-0.146587382388275,-0.00165014728799839,
0.659022981674053));
#15032=CARTESIAN_POINT('Ctrl Pts',(-0.146562848415234,-0.00327013229389975,
0.659111467932396));
#15033=CARTESIAN_POINT('Ctrl Pts',(-0.146508820881567,-0.00488913307276392,
0.659199954190739));
#15034=CARTESIAN_POINT('Ctrl Pts',(-0.144892390022949,-0.0533274503793473,
0.661847343564999));
#15035=CARTESIAN_POINT('Ctrl Pts',(-0.116875517863988,-0.100884760863813,
0.66449473293926));
#15036=CARTESIAN_POINT('Ctrl Pts',(-0.0752913709948059,-0.125777373450206,
0.66714212231352));
#15037=CARTESIAN_POINT('Ctrl Pts',(-0.0337072241256252,-0.150669986036599,
0.66978951168778));
#15038=CARTESIAN_POINT('Ctrl Pts',(0.021444197453776,-0.15289790072492,
0.672436901062039));
#15039=CARTESIAN_POINT('Ctrl Pts',(0.0649007096996251,-0.131440618146733,
0.675084290436299));
#15040=CARTESIAN_POINT('Ctrl Pts',(0.108357221945475,-0.109983335568545,
0.677731679810559));
#15041=CARTESIAN_POINT('Ctrl Pts',(0.140118824857774,-0.0648408557238465,
0.68037906918482));
#15042=CARTESIAN_POINT('Ctrl Pts',(0.145637072805965,-0.0166907532130915,
0.68302645855908));
#15043=CARTESIAN_POINT('Ctrl Pts',(0.151155320754156,0.031459349297663,
0.68567384793334));
#15044=CARTESIAN_POINT('Ctrl Pts',(0.130430213738242,0.0826170744744734,
0.688321237307599));
#15045=CARTESIAN_POINT('Ctrl Pts',(0.0929549153570804,0.113349556369966,
0.690968626681859));
#15046=CARTESIAN_POINT('Ctrl Pts',(0.0554796169759186,0.14408203826546,
0.693616016056119));
#15047=CARTESIAN_POINT('Ctrl Pts',(0.00125412722950909,0.154389276879634,
0.69626340543038));
#15048=CARTESIAN_POINT('Ctrl Pts',(-0.0448834941801804,0.139550027475769,
0.69891079480464));
#15049=CARTESIAN_POINT('Ctrl Pts',(-0.0910211155898686,0.124710778071904,
0.7015581841789));
#15050=CARTESIAN_POINT('Ctrl Pts',(-0.129070868662838,0.0847250406500019,
0.704205573553159));
#15051=CARTESIAN_POINT('Ctrl Pts',(-0.141604011991841,0.0379083368947344,
0.706852962927419));
#15052=CARTESIAN_POINT('Ctrl Pts',(-0.144888775625201,0.0256383259412015,
0.707546807090183));
#15053=CARTESIAN_POINT('Ctrl Pts',(-0.146420824649375,0.0128991016161637,
0.708240651252947));
#15054=CARTESIAN_POINT('Ctrl Pts',(-0.146307221518699,0.000133045872591754,
0.708934495415711));
#15055=CARTESIAN_POINT('Origin',(0.,0.,0.));
#15056=CARTESIAN_POINT('',(-0.1461301977291,-5.61458017395017E-5,0.766065504584291));
#15057=CARTESIAN_POINT('',(-0.14612241379348,-4.54149644099216E-5,0.758934495415711));
#15058=CARTESIAN_POINT('',(-0.14635,-1.79227059055215E-17,0.));
#15059=CARTESIAN_POINT('Ctrl Pts',(-0.1461301977291,-5.61458017395017E-5,
0.766065504584291));
#15060=CARTESIAN_POINT('Ctrl Pts',(-0.14603380141711,0.0278870014676159,
0.764551403227483));
#15061=CARTESIAN_POINT('Ctrl Pts',(-0.138327245009168,0.0558793842949389,
0.763037301870675));
#15062=CARTESIAN_POINT('Ctrl Pts',(-0.123350675409043,0.079203679241543,
0.761523200513867));
#15063=CARTESIAN_POINT('Ctrl Pts',(-0.0971747899961838,0.119969628197767,
0.758876870634766));
#15064=CARTESIAN_POINT('Ctrl Pts',(-0.048790709571801,0.146475657227381,
0.756230540755664));
#15065=CARTESIAN_POINT('Ctrl Pts',(-0.000344588961360588,0.146589539830481,
0.753584210876561));
#15066=CARTESIAN_POINT('Ctrl Pts',(0.0481015316490792,0.14670342243358,
0.750937880997459));
#15067=CARTESIAN_POINT('Ctrl Pts',(0.0966096924455767,0.120425158610167,
0.748291551118357));
#15068=CARTESIAN_POINT('Ctrl Pts',(0.122976945064223,0.0797827231418903,
0.745645221239255));
#15069=CARTESIAN_POINT('Ctrl Pts',(0.149344197682869,0.0391402876736125,
0.742998891360154));
#15070=CARTESIAN_POINT('Ctrl Pts',(0.153570542123663,-0.01586631943953,
0.740352561481052));
#15071=CARTESIAN_POINT('Ctrl Pts',(0.133721514043982,-0.0600597087159893,
0.73770623160195));
#15072=CARTESIAN_POINT('Ctrl Pts',(0.113872485964301,-0.104253097992448,
0.735059901722848));
#15073=CARTESIAN_POINT('Ctrl Pts',(0.0699480853641458,-0.137633269432224,
0.732413571843746));
#15074=CARTESIAN_POINT('Ctrl Pts',(0.0220532014503509,-0.144921593405036,
0.729767241964644));
#15075=CARTESIAN_POINT('Ctrl Pts',(-0.0258416824634434,-0.152209917377848,
0.727120912085542));
#15076=CARTESIAN_POINT('Ctrl Pts',(-0.0777070496908773,-0.133406393883698,
0.724474582206441));
#15077=CARTESIAN_POINT('Ctrl Pts',(-0.109803305666473,-0.0971176914572187,
0.721828252327339));
#15078=CARTESIAN_POINT('Ctrl Pts',(-0.133101311474982,-0.0707764758164216,
0.71990733641299));
#15079=CARTESIAN_POINT('Ctrl Pts',(-0.14598295937539,-0.0352223077304616,
0.71798642049864));
#15080=CARTESIAN_POINT('Ctrl Pts',(-0.146290249280603,0.000131112932912382,
0.716065504584291));
#15081=CARTESIAN_POINT('Ctrl Pts',(-0.146307221518699,0.000133045872591754,
0.708934495415711));
#15082=CARTESIAN_POINT('Ctrl Pts',(-0.145987367488279,-0.0358102803178394,
0.710888040627207));
#15083=CARTESIAN_POINT('Ctrl Pts',(-0.132622002370819,-0.0719663061161047,
0.712841585838703));
#15084=CARTESIAN_POINT('Ctrl Pts',(-0.1086007072861,-0.0984612847532928,
0.7147951310502));
#15085=CARTESIAN_POINT('Ctrl Pts',(-0.0760477256663158,-0.134366532557423,
0.71744252042446));
#15086=CARTESIAN_POINT('Ctrl Pts',(-0.0239252288417074,-0.152529358077047,
0.720089909798719));
#15087=CARTESIAN_POINT('Ctrl Pts',(0.0238920022682765,-0.144630254255197,
0.722737299172979));
#15088=CARTESIAN_POINT('Ctrl Pts',(0.071709233378259,-0.136731150433346,
0.725384688547239));
#15089=CARTESIAN_POINT('Ctrl Pts',(0.115221198773618,-0.102770117270024,
0.7280320779215));
#15090=CARTESIAN_POINT('Ctrl Pts',(0.134497183226257,-0.058303052428779,
0.730679467295759));
#15091=CARTESIAN_POINT('Ctrl Pts',(0.153773167678896,-0.0138359875875333,
0.733326856670019));
#15092=CARTESIAN_POINT('Ctrl Pts',(0.148813171188813,0.0411371089316358,
0.735974246044279));
#15093=CARTESIAN_POINT('Ctrl Pts',(0.121889126928366,0.0814357351225549,
0.738621635418539));
#15094=CARTESIAN_POINT('Ctrl Pts',(0.0949650826679194,0.121734361313473,
0.741269024792799));
#15095=CARTESIAN_POINT('Ctrl Pts',(0.0460769906371109,0.147358517176143,
0.74391641416706));
#15096=CARTESIAN_POINT('Ctrl Pts',(-0.00238189178169058,0.146571023090686,
0.74656380354132));
#15097=CARTESIAN_POINT('Ctrl Pts',(-0.0508407742004934,0.14578352900523,
0.74921119291558));
#15098=CARTESIAN_POINT('Ctrl Pts',(-0.0988704470072894,0.118584384971644,
0.751858582289839));
#15099=CARTESIAN_POINT('Ctrl Pts',(-0.124470852918682,0.0774321960944291,
0.754505971664099));
#15100=CARTESIAN_POINT('Ctrl Pts',(-0.138745545153454,0.0544858868428234,
0.75598214624797));
#15101=CARTESIAN_POINT('Ctrl Pts',(-0.146046671909043,0.027201385339783,
0.757458320831841));
#15102=CARTESIAN_POINT('Ctrl Pts',(-0.14612241379348,-4.54149644099216E-5,
0.758934495415711));
#15103=CARTESIAN_POINT('Origin',(0.,0.,0.));
#15104=CARTESIAN_POINT('',(-0.146495788566881,-0.000101744904923998,0.816065504584291));
#15105=CARTESIAN_POINT('',(-0.146473871348434,-0.000110945968026819,0.808934495415711));
#15106=CARTESIAN_POINT('',(-0.14635,-1.79227059055215E-17,0.));
#15107=CARTESIAN_POINT('Ctrl Pts',(-0.146495788566881,-0.000101744904923998,
0.816065504584291));
#15108=CARTESIAN_POINT('Ctrl Pts',(-0.14616118452328,0.0421270051992108,
0.813762715835428));
#15109=CARTESIAN_POINT('Ctrl Pts',(-0.126905337350145,0.0846218946815527,
0.811459927086565));
#15110=CARTESIAN_POINT('Ctrl Pts',(-0.0947343415465314,0.111866064832055,
0.809157138337701));
#15111=CARTESIAN_POINT('Ctrl Pts',(-0.0577639214515077,0.143174651664521,
0.806510808458599));
#15112=CARTESIAN_POINT('Ctrl Pts',(-0.00373742343573488,0.154342745753647,
0.803864478579497));
#15113=CARTESIAN_POINT('Ctrl Pts',(0.0426163743729279,0.140258534729872,
0.801218148700395));
#15114=CARTESIAN_POINT('Ctrl Pts',(0.0889701721815907,0.126174323706097,
0.798571818821294));
#15115=CARTESIAN_POINT('Ctrl Pts',(0.127651269783143,0.0868378075694234,
0.795925488942192));
#15116=CARTESIAN_POINT('Ctrl Pts',(0.140954720244851,0.040253928627653,
0.79327915906309));
#15117=CARTESIAN_POINT('Ctrl Pts',(0.154258170706558,-0.00632995031411615,
0.790632829183988));
#15118=CARTESIAN_POINT('Ctrl Pts',(0.14218397402842,-0.060161192060982,
0.787986499304886));
#15119=CARTESIAN_POINT('Ctrl Pts',(0.110258679990485,-0.0966003903512828,
0.785340169425784));
#15120=CARTESIAN_POINT('Ctrl Pts',(0.0783333859525485,-0.133039588641585,
0.782693839546682));
#15121=CARTESIAN_POINT('Ctrl Pts',(0.0265569945548152,-0.152086743475322,
0.780047509667581));
#15122=CARTESIAN_POINT('Ctrl Pts',(-0.021371625274328,-0.14502367242074,
0.777401179788479));
#15123=CARTESIAN_POINT('Ctrl Pts',(-0.0693002451034712,-0.137960601366157,
0.774754849909377));
#15124=CARTESIAN_POINT('Ctrl Pts',(-0.113381093364023,-0.104787304423254,
0.772108520030274));
#15125=CARTESIAN_POINT('Ctrl Pts',(-0.133437672293631,-0.0606877215103841,
0.769462190151172));
#15126=CARTESIAN_POINT('Ctrl Pts',(-0.1420188514214,-0.0418197768941368,
0.768329961628878));
#15127=CARTESIAN_POINT('Ctrl Pts',(-0.146202281842484,-0.0209517273285418,
0.767197733106584));
#15128=CARTESIAN_POINT('Ctrl Pts',(-0.1461301977291,-5.61458017395017E-5,
0.766065504584291));
#15129=CARTESIAN_POINT('Ctrl Pts',(-0.14612241379348,-4.54149644099216E-5,
0.758934495415711));
#15130=CARTESIAN_POINT('Ctrl Pts',(-0.146182508321779,-0.0216633562673834,
0.760105710206101));
#15131=CARTESIAN_POINT('Ctrl Pts',(-0.141694203021096,-0.0432575645610501,
0.76127692499649));
#15132=CARTESIAN_POINT('Ctrl Pts',(-0.132531725405586,-0.0626424774360703,
0.76244813978688));
#15133=CARTESIAN_POINT('Ctrl Pts',(-0.111821052965107,-0.106459728368519,
0.76509552916114));
#15134=CARTESIAN_POINT('Ctrl Pts',(-0.067228569068158,-0.138988996512573,
0.767742918535399));
#15135=CARTESIAN_POINT('Ctrl Pts',(-0.0191799219195066,-0.145330206128911,
0.770390307909659));
#15136=CARTESIAN_POINT('Ctrl Pts',(0.0288687252291434,-0.151671415745249,
0.773037697283919));
#15137=CARTESIAN_POINT('Ctrl Pts',(0.080373535629496,-0.131824566833873,
0.77568508665818));
#15138=CARTESIAN_POINT('Ctrl Pts',(0.111742660473083,-0.0948805356683208,
0.77833247603244));
#15139=CARTESIAN_POINT('Ctrl Pts',(0.14311178531667,-0.0579365045027684,
0.7809798654067));
#15140=CARTESIAN_POINT('Ctrl Pts',(0.154345224603492,-0.00389529108304171,
0.783627254780959));
#15141=CARTESIAN_POINT('Ctrl Pts',(0.140297486112651,0.0424894529122293,
0.786274644155219));
#15142=CARTESIAN_POINT('Ctrl Pts',(0.126249747621811,0.0888741969075009,
0.788922033529479));
#15143=CARTESIAN_POINT('Ctrl Pts',(0.0869208313533056,0.127602471478316,
0.79156942290374));
#15144=CARTESIAN_POINT('Ctrl Pts',(0.0403254011646538,0.140934737517831,
0.794216812278));
#15145=CARTESIAN_POINT('Ctrl Pts',(-0.00627002902399674,0.154267003557346,
0.79686420165226));
#15146=CARTESIAN_POINT('Ctrl Pts',(-0.0601319731327944,0.142203261065564,
0.799511591026519));
#15147=CARTESIAN_POINT('Ctrl Pts',(-0.0965888940360299,0.110269323781398,
0.802158980400779));
#15148=CARTESIAN_POINT('Ctrl Pts',(-0.127690529151203,0.0830262752573849,
0.804417485405756));
#15149=CARTESIAN_POINT('Ctrl Pts',(-0.146124951115714,0.0413218847513699,
0.806675990410734));
#15150=CARTESIAN_POINT('Ctrl Pts',(-0.146473871348434,-0.000110945968026819,
0.808934495415711));
#15151=CARTESIAN_POINT('Origin',(0.,0.,0.));
#15152=CARTESIAN_POINT('',(-0.146444331750498,0.000119944961782359,0.866065504584291));
#15153=CARTESIAN_POINT('',(-0.146471560192382,0.00011177640072981,0.858934495415711));
#15154=CARTESIAN_POINT('',(-0.14635,-1.79227059055215E-17,0.));
#15155=CARTESIAN_POINT('Ctrl Pts',(-0.146444331750498,0.000119944961782359,
0.866065504584291));
#15156=CARTESIAN_POINT('Ctrl Pts',(-0.146516681599632,0.00829054204730037,
0.865620358322474));
#15157=CARTESIAN_POINT('Ctrl Pts',(-0.145891801779796,0.0164500693154795,
0.865175212060658));
#15158=CARTESIAN_POINT('Ctrl Pts',(-0.14453063157077,0.0244848619971339,
0.864730065798841));
#15159=CARTESIAN_POINT('Ctrl Pts',(-0.136438672357208,0.0722505376181754,
0.862083735919739));
#15160=CARTESIAN_POINT('Ctrl Pts',(-0.102325254887189,0.115607931012472,
0.859437406040638));
#15161=CARTESIAN_POINT('Ctrl Pts',(-0.0578046270350215,0.134711681091902,
0.856791076161536));
#15162=CARTESIAN_POINT('Ctrl Pts',(-0.0132839991828526,0.153815431171333,
0.854144746282434));
#15163=CARTESIAN_POINT('Ctrl Pts',(0.0416438390514653,0.148665537935894,
0.851498416403331));
#15164=CARTESIAN_POINT('Ctrl Pts',(0.081837551941475,0.121619188541491,
0.848852086524229));
#15165=CARTESIAN_POINT('Ctrl Pts',(0.122031264831484,0.0945728391470885,
0.846205756645128));
#15166=CARTESIAN_POINT('Ctrl Pts',(0.147490852377186,0.0456300335937214,
0.843559426766026));
#15167=CARTESIAN_POINT('Ctrl Pts',(0.146563060809277,-0.0028073360113171,
0.840913096886925));
#15168=CARTESIAN_POINT('Ctrl Pts',(0.145635269241369,-0.0512447056163556,
0.838266767007823));
#15169=CARTESIAN_POINT('Ctrl Pts',(0.118320098559852,-0.0991766392730661,
0.835620437128721));
#15170=CARTESIAN_POINT('Ctrl Pts',(0.0771201321287374,-0.124663936845065,
0.832974107249619));
#15171=CARTESIAN_POINT('Ctrl Pts',(0.035920165697623,-0.150151234417064,
0.830327777370517));
#15172=CARTESIAN_POINT('Ctrl Pts',(-0.0191645964830881,-0.153193895904352,
0.827681447491415));
#15173=CARTESIAN_POINT('Ctrl Pts',(-0.0629209921278279,-0.132399247274726,
0.825035117612313));
#15174=CARTESIAN_POINT('Ctrl Pts',(-0.106677387772568,-0.111604598645101,
0.822388787733211));
#15175=CARTESIAN_POINT('Ctrl Pts',(-0.139105416881337,-0.0669726398985626,
0.819742457854109));
#15176=CARTESIAN_POINT('Ctrl Pts',(-0.145362260348583,-0.0189321207373897,
0.817096127975007));
#15177=CARTESIAN_POINT('Ctrl Pts',(-0.146174510965348,-0.0126955988357878,
0.816752586844768));
#15178=CARTESIAN_POINT('Ctrl Pts',(-0.146545706411658,-0.00640163348415362,
0.81640904571453));
#15179=CARTESIAN_POINT('Ctrl Pts',(-0.146495788566881,-0.000101744904923998,
0.816065504584291));
#15180=CARTESIAN_POINT('Ctrl Pts',(-0.146473871348434,-0.000110945968026819,
0.808934495415711));
#15181=CARTESIAN_POINT('Ctrl Pts',(-0.146533950748007,-0.00724512552769256,
0.809323379784994));
#15182=CARTESIAN_POINT('Ctrl Pts',(-0.146057826922151,-0.0143712538186879,
0.809712264154277));
#15183=CARTESIAN_POINT('Ctrl Pts',(-0.145017839345608,-0.0214141189368497,
0.81010114852356));
#15184=CARTESIAN_POINT('Ctrl Pts',(-0.137937966054276,-0.0693594922943736,
0.81274853789782));
#15185=CARTESIAN_POINT('Ctrl Pts',(-0.104726321773939,-0.113446106932874,
0.81539592727208));
#15186=CARTESIAN_POINT('Ctrl Pts',(-0.0605955455659204,-0.133480028752914,
0.818043316646339));
#15187=CARTESIAN_POINT('Ctrl Pts',(-0.0164647693578984,-0.153513950572954,
0.820690706020599));
#15188=CARTESIAN_POINT('Ctrl Pts',(0.0385851387778066,-0.149495179574532,
0.823338095394859));
#15189=CARTESIAN_POINT('Ctrl Pts',(0.0793384931690736,-0.12326451930694,
0.825985484769119));
#15190=CARTESIAN_POINT('Ctrl Pts',(0.120091847560339,-0.0970338590393495,
0.828632874143379));
#15191=CARTESIAN_POINT('Ctrl Pts',(0.146548648207165,-0.0485913095025905,
0.83128026351764));
#15192=CARTESIAN_POINT('Ctrl Pts',(0.146590321408106,-0.000126046730599388,
0.833927652891899));
#15193=CARTESIAN_POINT('Ctrl Pts',(0.146631994609047,0.0483392160413931,
0.836575042266159));
#15194=CARTESIAN_POINT('Ctrl Pts',(0.120258540364101,0.0968271920486179,
0.839222431640419));
#15195=CARTESIAN_POINT('Ctrl Pts',(0.0795503554414038,0.123127897600245,
0.841869821014679));
#15196=CARTESIAN_POINT('Ctrl Pts',(0.0388421705187073,0.149428603151872,
0.844517210388939));
#15197=CARTESIAN_POINT('Ctrl Pts',(-0.0162007450817403,0.153542038247903,
0.8471645997632));
#15198=CARTESIAN_POINT('Ctrl Pts',(-0.0603659086281491,0.133584038319734,
0.84981198913746));
#15199=CARTESIAN_POINT('Ctrl Pts',(-0.104531072174558,0.113626038391565,
0.85245937851172));
#15200=CARTESIAN_POINT('Ctrl Pts',(-0.137818483666928,0.0695966034391962,
0.855106767885979));
#15201=CARTESIAN_POINT('Ctrl Pts',(-0.144980798768897,0.0216634763286692,
0.857754157260239));
#15202=CARTESIAN_POINT('Ctrl Pts',(-0.146045237806912,0.0145398171508471,
0.858147603312063));
#15203=CARTESIAN_POINT('Ctrl Pts',(-0.146532654486068,0.00732993751956911,
0.858541049363887));
#15204=CARTESIAN_POINT('Ctrl Pts',(-0.146471560192382,0.00011177640072981,
0.858934495415711));
#15205=CARTESIAN_POINT('Origin',(0.,0.,0.));
#15206=CARTESIAN_POINT('',(-0.146114231148477,2.69008449349656E-5,0.916065504584291));
#15207=CARTESIAN_POINT('',(-0.146121644853617,4.41067432152685E-5,0.908934495415711));
#15208=CARTESIAN_POINT('',(-0.14635,-1.79227059055215E-17,0.));
#15209=CARTESIAN_POINT('Ctrl Pts',(-0.146114231148477,2.69008449349656E-5,
0.916065504584291));
#15210=CARTESIAN_POINT('Ctrl Pts',(-0.146151635159142,0.0228038459942234,
0.914831670930419));
#15211=CARTESIAN_POINT('Ctrl Pts',(-0.141147538069067,0.0455652341090756,
0.913597837276548));
#15212=CARTESIAN_POINT('Ctrl Pts',(-0.131015765267123,0.0657531838068269,
0.912364003622676));
#15213=CARTESIAN_POINT('Ctrl Pts',(-0.109285110563454,0.109052354902802,
0.909717673743574));
#15214=CARTESIAN_POINT('Ctrl Pts',(-0.0639662294071284,0.140513248471977,
0.907071343864472));
#15215=CARTESIAN_POINT('Ctrl Pts',(-0.015802286694576,0.145735718560985,
0.90442501398537));
#15216=CARTESIAN_POINT('Ctrl Pts',(0.0323616560179757,0.150958188649994,
0.901778684106268));
#15217=CARTESIAN_POINT('Ctrl Pts',(0.0833706602867547,0.129942235258839,
0.899132354227166));
#15218=CARTESIAN_POINT('Ctrl Pts',(0.113877102345416,0.0923071908936453,
0.896486024348064));
#15219=CARTESIAN_POINT('Ctrl Pts',(0.144383544404078,0.0546721465284523,
0.893839694468962));
#15220=CARTESIAN_POINT('Ctrl Pts',(0.15438742425262,0.000418011189221586,
0.891193364589861));
#15221=CARTESIAN_POINT('Ctrl Pts',(0.139309808695705,-0.0456222438118789,
0.888547034710759));
#15222=CARTESIAN_POINT('Ctrl Pts',(0.124232193138789,-0.0916624988129813,
0.885900704831657));
#15223=CARTESIAN_POINT('Ctrl Pts',(0.0840730821764119,-0.129488873475953,
0.883254374952555));
#15224=CARTESIAN_POINT('Ctrl Pts',(0.0372139327097935,-0.141787641004198,
0.880608045073453));
#15225=CARTESIAN_POINT('Ctrl Pts',(-0.00964521675682358,-0.154086408532443,
0.877961715194351));
#15226=CARTESIAN_POINT('Ctrl Pts',(-0.0632044047276821,-0.140857568925962,
0.875315385315249));
#15227=CARTESIAN_POINT('Ctrl Pts',(-0.0989487482345592,-0.108156170198829,
0.872669055436147));
#15228=CARTESIAN_POINT('Ctrl Pts',(-0.128680439645858,-0.0809555616469925,
0.870467871818862));
#15229=CARTESIAN_POINT('Ctrl Pts',(-0.146086572253705,-0.0402824710322022,
0.868266688201576));
#15230=CARTESIAN_POINT('Ctrl Pts',(-0.146444331750498,0.000119944961782359,
0.866065504584291));
#15231=CARTESIAN_POINT('Ctrl Pts',(-0.146471560192382,0.00011177640072981,
0.858934495415711));
#15232=CARTESIAN_POINT('Ctrl Pts',(-0.146121567926216,-0.0412390669452651,
0.861188438738147));
#15233=CARTESIAN_POINT('Ctrl Pts',(-0.127770397964496,-0.0828616943330661,
0.863442382060584));
#15234=CARTESIAN_POINT('Ctrl Pts',(-0.096778382793969,-0.110103055552942,
0.86569632538302));
#15235=CARTESIAN_POINT('Ctrl Pts',(-0.0603764330055066,-0.142099641055337,
0.86834371475728));
#15236=CARTESIAN_POINT('Ctrl Pts',(-0.00653531471701479,-0.154255992791443,
0.870991104131539));
#15237=CARTESIAN_POINT('Ctrl Pts',(0.040082974241256,-0.14100387723139,
0.873638493505799));
#15238=CARTESIAN_POINT('Ctrl Pts',(0.0867012631995282,-0.127751761671338,
0.876285882880059));
#15239=CARTESIAN_POINT('Ctrl Pts',(0.12609672282758,-0.0890911788151255,
0.878933272254319));
#15240=CARTESIAN_POINT('Ctrl Pts',(0.140224208991091,-0.042730661487191,
0.88158066162858));
#15241=CARTESIAN_POINT('Ctrl Pts',(0.154351695154603,0.00362985584074295,
0.88422805100284));
#15242=CARTESIAN_POINT('Ctrl Pts',(0.143211207853577,0.057690307640398,
0.886875440377099));
#15243=CARTESIAN_POINT('Ctrl Pts',(0.111905662524754,0.09468823006692,0.889522829751359));
#15244=CARTESIAN_POINT('Ctrl Pts',(0.0806001171959318,0.131686152493442,
0.892170219125619));
#15245=CARTESIAN_POINT('Ctrl Pts',(0.0291295138393125,0.15162154554683,
0.894817608499879));
#15246=CARTESIAN_POINT('Ctrl Pts',(-0.0189299673197759,0.145362975188259,
0.897464997874139));
#15247=CARTESIAN_POINT('Ctrl Pts',(-0.0669894484788628,0.139104404829688,
0.9001123872484));
#15248=CARTESIAN_POINT('Ctrl Pts',(-0.11163780744042,0.10665187105916,0.902759776622659));
#15249=CARTESIAN_POINT('Ctrl Pts',(-0.132423802349956,0.0628703013313112,
0.905407165996919));
#15250=CARTESIAN_POINT('Ctrl Pts',(-0.141655418982822,0.043425734493323,
0.90658294246985));
#15251=CARTESIAN_POINT('Ctrl Pts',(-0.146180218154578,0.0217465313827003,
0.907758718942781));
#15252=CARTESIAN_POINT('Ctrl Pts',(-0.146121644853617,4.41067432152685E-5,
0.908934495415711));
#15253=CARTESIAN_POINT('Origin',(0.,0.,0.));
#15254=CARTESIAN_POINT('',(-0.146345621585321,-0.000133809880645736,0.966065504584291));
#15255=CARTESIAN_POINT('',(-0.146309694201085,-0.000133223314395004,0.958934495415711));
#15256=CARTESIAN_POINT('',(-0.14635,-1.79227059055215E-17,0.));
#15257=CARTESIAN_POINT('Ctrl Pts',(-0.146345621585321,-0.000133809880645736,
0.966065504584291));
#15258=CARTESIAN_POINT('Ctrl Pts',(-0.146004672532387,0.0370537288701324,
0.964042983538364));
#15259=CARTESIAN_POINT('Ctrl Pts',(-0.131578083002406,0.0744765756810296,
0.962020462492437));
#15260=CARTESIAN_POINT('Ctrl Pts',(-0.106003654037246,0.101251356830495,
0.959997941446511));
#15261=CARTESIAN_POINT('Ctrl Pts',(-0.0725412702228666,0.136284319036219,
0.957351611567409));
#15262=CARTESIAN_POINT('Ctrl Pts',(-0.0199938687303381,0.153087872523943,
0.954705281688306));
#15263=CARTESIAN_POINT('Ctrl Pts',(0.0275867780614433,0.143970766496025,
0.952058951809204));
#15264=CARTESIAN_POINT('Ctrl Pts',(0.0751674248532248,0.134853660468108,
0.949412621930102));
#15265=CARTESIAN_POINT('Ctrl Pts',(0.11778131694426,0.0998158949245492,
0.946766292051));
#15266=CARTESIAN_POINT('Ctrl Pts',(0.135923405490256,0.0548948063954655,
0.944119962171899));
#15267=CARTESIAN_POINT('Ctrl Pts',(0.154065494036253,0.0099737178663825,
0.941473632292797));
#15268=CARTESIAN_POINT('Ctrl Pts',(0.147735779037212,-0.0448306936482241,
0.938827302413695));
#15269=CARTESIAN_POINT('Ctrl Pts',(0.119831470632095,-0.0844335867733556,
0.936180972534593));
#15270=CARTESIAN_POINT('Ctrl Pts',(0.0919271622269763,-0.124036479898489,
0.933534642655491));
#15271=CARTESIAN_POINT('Ctrl Pts',(0.0424482604157787,-0.148437854634144,
0.93088831277639));
#15272=CARTESIAN_POINT('Ctrl Pts',(-0.00595796300272124,-0.146468817862788,
0.928241982897288));
#15273=CARTESIAN_POINT('Ctrl Pts',(-0.0543641864212212,-0.144499781091432,
0.925595653018186));
#15274=CARTESIAN_POINT('Ctrl Pts',(-0.101697731447024,-0.116160332813065,
0.922949323139084));
#15275=CARTESIAN_POINT('Ctrl Pts',(-0.126293289834417,-0.0744218843624929,
0.920302993259982));
#15276=CARTESIAN_POINT('Ctrl Pts',(-0.139421333187579,-0.052143709087005,
0.918890497034752));
#15277=CARTESIAN_POINT('Ctrl Pts',(-0.146071410932229,-0.0260482098028304,
0.917478000809521));
#15278=CARTESIAN_POINT('Ctrl Pts',(-0.146114231148477,2.69008449349656E-5,
0.916065504584291));
#15279=CARTESIAN_POINT('Ctrl Pts',(-0.146121644853617,4.41067432152685E-5,
0.908934495415711));
#15280=CARTESIAN_POINT('Ctrl Pts',(-0.146048333958771,-0.027118852224649,
0.910406108317041));
#15281=CARTESIAN_POINT('Ctrl Pts',(-0.138795050353101,-0.0543181883240968,
0.91187772121837));
#15282=CARTESIAN_POINT('Ctrl Pts',(-0.124603830013468,-0.0772180274565794,
0.9133493341197));
#15283=CARTESIAN_POINT('Ctrl Pts',(-0.0990742319099257,-0.118414180831446,
0.91599672349396));
#15284=CARTESIAN_POINT('Ctrl Pts',(-0.0510914048453256,-0.145695881896007,
0.91864411286822));
#15285=CARTESIAN_POINT('Ctrl Pts',(-0.00263394834681351,-0.146566710184873,
0.92129150224248));
#15286=CARTESIAN_POINT('Ctrl Pts',(0.0458235081516972,-0.147437538473739,
0.92393889161674));
#15287=CARTESIAN_POINT('Ctrl Pts',(0.0947555940841207,-0.121897493986912,
0.926586280990999));
#15288=CARTESIAN_POINT('Ctrl Pts',(0.121748900601314,-0.0816452290135895,
0.929233670365259));
#15289=CARTESIAN_POINT('Ctrl Pts',(0.148742207118509,-0.0413929640402651,
0.931881059739519));
#15290=CARTESIAN_POINT('Ctrl Pts',(0.153796734220472,0.0135715214195569,
0.93452844911378));
#15291=CARTESIAN_POINT('Ctrl Pts',(0.134597248858856,0.0580716696672091,
0.93717583848804));
#15292=CARTESIAN_POINT('Ctrl Pts',(0.115397763497239,0.102571817914861,
0.9398232278623));
#15293=CARTESIAN_POINT('Ctrl Pts',(0.0719442656720451,0.136607628950342,
0.942470617236559));
#15294=CARTESIAN_POINT('Ctrl Pts',(0.0241406894609324,0.144588953003544,
0.945118006610819));
#15295=CARTESIAN_POINT('Ctrl Pts',(-0.023662886750181,0.152570277056746,
0.947765395985079));
#15296=CARTESIAN_POINT('Ctrl Pts',(-0.0758165413472122,0.134497114127667,
0.950412785359339));
#15297=CARTESIAN_POINT('Ctrl Pts',(-0.108431221550465,0.0986479012011113,
0.953060174733599));
#15298=CARTESIAN_POINT('Ctrl Pts',(-0.132554242808212,0.0721325001574252,
0.955018281627637));
#15299=CARTESIAN_POINT('Ctrl Pts',(-0.145988218858404,0.0358924841874147,
0.956976388521674));
#15300=CARTESIAN_POINT('Ctrl Pts',(-0.146309694201085,-0.000133223314395004,
0.958934495415711));
#15301=CARTESIAN_POINT('Origin',(0.,0.,0.));
#15302=CARTESIAN_POINT('',(-0.146565171121453,5.44893591410845E-5,1.01606550458429));
#15303=CARTESIAN_POINT('',(-0.146582076026177,3.15354312248815E-5,1.00893449541571));
#15304=CARTESIAN_POINT('',(-0.14635,-1.79227059055215E-17,0.));
#15305=CARTESIAN_POINT('Ctrl Pts',(-0.146565171121453,5.44893591410845E-5,
1.01606550458429));
#15306=CARTESIAN_POINT('Ctrl Pts',(-0.146579596851449,0.00307427920823236,
1.01590062602541));
#15307=CARTESIAN_POINT('Ctrl Pts',(-0.146494352296349,0.00609323927190738,
1.01573574746653));
#15308=CARTESIAN_POINT('Ctrl Pts',(-0.146306854564556,0.00910583530985269,
1.01557086890765));
#15309=CARTESIAN_POINT('Ctrl Pts',(-0.143297482980539,0.0574585317612167,
1.01292453902855));
#15310=CARTESIAN_POINT('Ctrl Pts',(-0.11394685994478,0.104171803331984,
1.01027820914945));
#15311=CARTESIAN_POINT('Ctrl Pts',(-0.0716892273871119,0.127864250695428,
1.00763187927034));
#15312=CARTESIAN_POINT('Ctrl Pts',(-0.0294315948294418,0.151556698058874,
1.00498554939124));
#15313=CARTESIAN_POINT('Ctrl Pts',(0.0257330472501378,0.152228321214993,
1.00233921951214));
#15314=CARTESIAN_POINT('Ctrl Pts',(0.0685549742796134,0.129571707678744,
0.999692889633039));
#15315=CARTESIAN_POINT('Ctrl Pts',(0.111376901309088,0.106915094142495,
0.997046559753937));
#15316=CARTESIAN_POINT('Ctrl Pts',(0.141856113288459,0.0609302439138786,
0.994400229874835));
#15317=CARTESIAN_POINT('Ctrl Pts',(0.146041795372579,0.0126651464112397,
0.991753899995733));
#15318=CARTESIAN_POINT('Ctrl Pts',(0.150227477456699,-0.0355999510913994,
0.989107570116631));
#15319=CARTESIAN_POINT('Ctrl Pts',(0.128119629645567,-0.0861452958680607,
0.986461240237529));
#15320=CARTESIAN_POINT('Ctrl Pts',(0.0898373616998479,-0.115835488396583,
0.983814910358427));
#15321=CARTESIAN_POINT('Ctrl Pts',(0.051555093754129,-0.145525680925106,
0.981168580479325));
#15322=CARTESIAN_POINT('Ctrl Pts',(-0.00290159432617693,-0.154360721205491,
0.978522250600224));
#15323=CARTESIAN_POINT('Ctrl Pts',(-0.0486070196525971,-0.138296672301818,
0.975875920721122));
#15324=CARTESIAN_POINT('Ctrl Pts',(-0.0943124449790173,-0.122232623398145,
0.97322959084202));
#15325=CARTESIAN_POINT('Ctrl Pts',(-0.131266607551552,-0.081269485310415,
0.970583260962917));
#15326=CARTESIAN_POINT('Ctrl Pts',(-0.142555005769704,-0.0341567308046872,
0.967936931083816));
#15327=CARTESIAN_POINT('Ctrl Pts',(-0.145215975052668,-0.0230510282813687,
0.967313122250641));
#15328=CARTESIAN_POINT('Ctrl Pts',(-0.146450780951306,-0.0116036114945705,
0.966689313417466));
#15329=CARTESIAN_POINT('Ctrl Pts',(-0.146345621585321,-0.000133809880645736,
0.966065504584291));
#15330=CARTESIAN_POINT('Ctrl Pts',(-0.146309694201085,-0.000133223314395004,
0.958934495415711));
#15331=CARTESIAN_POINT('Ctrl Pts',(-0.146422858258782,-0.0128148032088542,
0.959623777895933));
#15332=CARTESIAN_POINT('Ctrl Pts',(-0.14491119500038,-0.0254698272036438,
0.960313060376156));
#15333=CARTESIAN_POINT('Ctrl Pts',(-0.141668994059001,-0.037664762585484,
0.961002342856379));
#15334=CARTESIAN_POINT('Ctrl Pts',(-0.129216380554811,-0.0845029505214961,
0.963649732230639));
#15335=CARTESIAN_POINT('Ctrl Pts',(-0.0912354477369537,-0.12455406346949,
0.966297121604899));
#15336=CARTESIAN_POINT('Ctrl Pts',(-0.0451234138007503,-0.1394726343957,
0.968944510979159));
#15337=CARTESIAN_POINT('Ctrl Pts',(0.00098862013545236,-0.154391205321909,
0.97159190035342));
#15338=CARTESIAN_POINT('Ctrl Pts',(0.055231755190001,-0.144177234226336,
0.974239289727679));
#15339=CARTESIAN_POINT('Ctrl Pts',(0.0927598492034174,-0.113509244531313,
0.976886679101939));
#15340=CARTESIAN_POINT('Ctrl Pts',(0.130287943216833,-0.0828412548362905,
0.979534068476199));
#15341=CARTESIAN_POINT('Ctrl Pts',(0.151100996189117,-0.0317192465418168,
0.982181457850459));
#15342=CARTESIAN_POINT('Ctrl Pts',(0.145665560755875,0.0164402745715088,
0.984828847224719));
#15343=CARTESIAN_POINT('Ctrl Pts',(0.140230125322634,0.0645997956848379,
0.987476236598979));
#15344=CARTESIAN_POINT('Ctrl Pts',(0.108546201483865,0.109796829617019,
0.990123625973239));
#15345=CARTESIAN_POINT('Ctrl Pts',(0.0651266538643092,0.131328813193254,
0.992771015347499));
#15346=CARTESIAN_POINT('Ctrl Pts',(0.0217071062447581,0.152860796769488,
0.995418404721759));
#15347=CARTESIAN_POINT('Ctrl Pts',(-0.0334480651555777,0.15072772998978,
0.998065794096019));
#15348=CARTESIAN_POINT('Ctrl Pts',(-0.0750749586823209,0.125906667008376,
1.00071318347028));
#15349=CARTESIAN_POINT('Ctrl Pts',(-0.116701852209067,0.101085604026969,
1.00336057284454));
#15350=CARTESIAN_POINT('Ctrl Pts',(-0.144800467862219,0.053576544843864,
1.0060079622188));
#15351=CARTESIAN_POINT('Ctrl Pts',(-0.146500196332402,0.00514107896046776,
1.00865535159306));
#15352=CARTESIAN_POINT('Ctrl Pts',(-0.146559936783033,0.00343871495990628,
1.00874839953394));
#15353=CARTESIAN_POINT('Ctrl Pts',(-0.146587066279139,0.00173520655478852,
1.00884144747483));
#15354=CARTESIAN_POINT('Ctrl Pts',(-0.146582076026177,3.15354312248815E-5,
1.00893449541571));
#15355=CARTESIAN_POINT('Origin',(0.,0.,0.));
#15356=CARTESIAN_POINT('',(-0.146184049129756,9.96948043307314E-5,1.06606550458429));
#15357=CARTESIAN_POINT('',(-0.146216477546812,0.000114345603752017,1.05893449541571));
#15358=CARTESIAN_POINT('',(-0.14635,-1.79227059055215E-17,0.));
#15359=CARTESIAN_POINT('Ctrl Pts',(-0.146184049129756,9.96948043307314E-5,
1.06606550458429));
#15360=CARTESIAN_POINT('Ctrl Pts',(-0.146294264763128,0.0176817746259609,
1.06511193863336));
#15361=CARTESIAN_POINT('Ctrl Pts',(-0.143360807533043,0.0352283113603788,
1.06415837268242));
#15362=CARTESIAN_POINT('Ctrl Pts',(-0.13721959397524,0.0515693218739058,
1.06320480673148));
#15363=CARTESIAN_POINT('Ctrl Pts',(-0.120176538991979,0.0969187854681546,
1.06055847685238));
#15364=CARTESIAN_POINT('Ctrl Pts',(-0.0784283132238915,0.132983650068601,
1.05791214697328));
#15365=CARTESIAN_POINT('Ctrl Pts',(-0.0310837364199337,0.143256459747686,
1.05526581709418));
#15366=CARTESIAN_POINT('Ctrl Pts',(0.0162608403840241,0.153529269426771,
1.05261948721508));
#15367=CARTESIAN_POINT('Ctrl Pts',(0.0692017682238519,0.138010024184496,
1.04997315733597));
#15368=CARTESIAN_POINT('Ctrl Pts',(0.103507151520239,0.103802126728842,
1.04732682745687));
#15369=CARTESIAN_POINT('Ctrl Pts',(0.137812534816628,0.0695942292731864,
1.04468049757777));
#15370=CARTESIAN_POINT('Ctrl Pts',(0.153482373569574,0.01669767960415,1.04203416769867));
#15371=CARTESIAN_POINT('Ctrl Pts',(0.143344336052008,-0.0306759392859165,
1.03938783781957));
#15372=CARTESIAN_POINT('Ctrl Pts',(0.133206298534443,-0.0780495581759789,
1.03674150794047));
#15373=CARTESIAN_POINT('Ctrl Pts',(0.0972603847463712,-0.119900246287072,
1.03409517806136));
#15374=CARTESIAN_POINT('Ctrl Pts',(0.0519596049571008,-0.137072285243832,
1.03144884818226));
#15375=CARTESIAN_POINT('Ctrl Pts',(0.00665882516783032,-0.154244324200591,
1.02880251830316));
#15376=CARTESIAN_POINT('Ctrl Pts',(-0.0479968206226384,-0.146737714003016,
1.02615618842406));
#15377=CARTESIAN_POINT('Ctrl Pts',(-0.0869905834517384,-0.11798834823825,
1.02350985854496));
#15378=CARTESIAN_POINT('Ctrl Pts',(-0.123554854979944,-0.0910302005802824,
1.02102840722473));
#15379=CARTESIAN_POINT('Ctrl Pts',(-0.146348061346918,-0.0453938791777224,
1.01854695590451));
#15380=CARTESIAN_POINT('Ctrl Pts',(-0.146565171121453,5.44893591410845E-5,
1.01606550458429));
#15381=CARTESIAN_POINT('Ctrl Pts',(-0.146582076026177,3.15354312248815E-5,
1.00893449541571));
#15382=CARTESIAN_POINT('Ctrl Pts',(-0.146445084172466,-0.0467374494427972,
1.01148883684909));
#15383=CARTESIAN_POINT('Ctrl Pts',(-0.122102455869861,-0.0936290599181376,
1.01404317828246));
#15384=CARTESIAN_POINT('Ctrl Pts',(-0.0837162036049941,-0.120334265578335,
1.01659751971584));
#15385=CARTESIAN_POINT('Ctrl Pts',(-0.0439316411201867,-0.14801227165006,
1.0192449090901));
#15386=CARTESIAN_POINT('Ctrl Pts',(0.0109383251366414,-0.154006411209824,
1.02189229846436));
#15387=CARTESIAN_POINT('Ctrl Pts',(0.0557604321169594,-0.135571060438576,
1.02453968783862));
#15388=CARTESIAN_POINT('Ctrl Pts',(0.100582539097277,-0.11713570966733,
1.02718707721288));
#15389=CARTESIAN_POINT('Ctrl Pts',(0.135356786801084,-0.0742708685650716,
1.02983446658714));
#15390=CARTESIAN_POINT('Ctrl Pts',(0.144154783532934,-0.0266108361928598,
1.0324818559614));
#15391=CARTESIAN_POINT('Ctrl Pts',(0.152952780264784,0.0210491961793507,
1.03512924533566));
#15392=CARTESIAN_POINT('Ctrl Pts',(0.135774526024679,0.0735044198215165,
1.03777663470992));
#15393=CARTESIAN_POINT('Ctrl Pts',(0.100488543649143,0.106727647840587,
1.04042402408418));
#15394=CARTESIAN_POINT('Ctrl Pts',(0.0652025612736062,0.139950875859659,
1.04307141345844));
#15395=CARTESIAN_POINT('Ctrl Pts',(0.0118088507626404,0.153942108255635,
1.0457188028327));
#15396=CARTESIAN_POINT('Ctrl Pts',(-0.0352355257975899,0.142292641904202,
1.04836619220696));
#15397=CARTESIAN_POINT('Ctrl Pts',(-0.0822799023578202,0.130643175552769,
1.05101358158122));
#15398=CARTESIAN_POINT('Ctrl Pts',(-0.122974944967313,0.0933530104539243,
1.05366097095548));
#15399=CARTESIAN_POINT('Ctrl Pts',(-0.138680233730631,0.0475029577050484,
1.05630836032974));
#15400=CARTESIAN_POINT('Ctrl Pts',(-0.143873300563147,0.0323423075707214,
1.05718373869173));
#15401=CARTESIAN_POINT('Ctrl Pts',(-0.146334133026589,0.0162457690968458,
1.05805911705372));
#15402=CARTESIAN_POINT('Ctrl Pts',(-0.146216477546812,0.000114345603752017,
1.05893449541571));
#15403=CARTESIAN_POINT('Origin',(0.,0.,0.));
#15404=CARTESIAN_POINT('',(-0.146204073634541,-0.000109175101205505,1.11606550458429));
#15405=CARTESIAN_POINT('',(-0.146170555016798,-9.22629125885076E-5,1.10893449541571));
#15406=CARTESIAN_POINT('',(-0.14635,-1.79227059055215E-17,0.));
#15407=CARTESIAN_POINT('Ctrl Pts',(-0.146204073634541,-0.000109175101205505,
1.11606550458429));
#15408=CARTESIAN_POINT('Ctrl Pts',(-0.145981599624502,0.032003853555373,
1.1143232512413));
#15409=CARTESIAN_POINT('Ctrl Pts',(-0.135565881201595,0.0642480963468658,
1.11258099789831));
#15410=CARTESIAN_POINT('Ctrl Pts',(-0.11609067353381,0.0895073597405865,
1.11083874455532));
#15411=CARTESIAN_POINT('Ctrl Pts',(-0.0865095427755784,0.127873963375947,
1.10819241467622));
#15412=CARTESIAN_POINT('Ctrl Pts',(-0.0360273159486943,0.150125560802435,
1.10554608479712));
#15413=CARTESIAN_POINT('Ctrl Pts',(0.0122494975033169,0.14607724579886,
1.10289975491801));
#15414=CARTESIAN_POINT('Ctrl Pts',(0.0605263109553308,0.142028930795284,
1.10025342503891));
#15415=CARTESIAN_POINT('Ctrl Pts',(0.10659771103247,0.111680703361642,1.09760709515981));
#15416=CARTESIAN_POINT('Ctrl Pts',(0.129376093089052,0.0689234246557527,
1.09496076528071));
#15417=CARTESIAN_POINT('Ctrl Pts',(0.152154475145634,0.0261661459498645,
1.09231443540161));
#15418=CARTESIAN_POINT('Ctrl Pts',(0.151639839181659,-0.0290001840282729,
1.0896681055225));
#15419=CARTESIAN_POINT('Ctrl Pts',(0.128067742174483,-0.0713250681289163,
1.0870217756434));
#15420=CARTESIAN_POINT('Ctrl Pts',(0.104495645167307,-0.11364995222956,
1.0843754457643));
#15421=CARTESIAN_POINT('Ctrl Pts',(0.0578660871169326,-0.143133390452712,
1.0817291158852));
#15422=CARTESIAN_POINT('Ctrl Pts',(0.00952215035475689,-0.146280349267719,
1.0790827860061));
#15423=CARTESIAN_POINT('Ctrl Pts',(-0.0388217864074202,-0.149427308082725,
1.07643645612699));
#15424=CARTESIAN_POINT('Ctrl Pts',(-0.0888801018813974,-0.126237787489585,
1.07379012624789));
#15425=CARTESIAN_POINT('Ctrl Pts',(-0.117740317519168,-0.0873259958989869,
1.07114379636879));
#15426=CARTESIAN_POINT('Ctrl Pts',(-0.136201180005177,-0.0624354946409797,
1.06945103244062));
#15427=CARTESIAN_POINT('Ctrl Pts',(-0.145988395071105,-0.0311118962502767,
1.06775826851246));
#15428=CARTESIAN_POINT('Ctrl Pts',(-0.146184049129756,9.96948043307314E-5,
1.06606550458429));
#15429=CARTESIAN_POINT('Ctrl Pts',(-0.146216477546812,0.000114345603752017,
1.05893449541571));
#15430=CARTESIAN_POINT('Ctrl Pts',(-0.145978309898544,-0.0325401742182177,
1.06070650642798));
#15431=CARTESIAN_POINT('Ctrl Pts',(-0.135174246449945,-0.06533764273189,
1.06247851744025));
#15432=CARTESIAN_POINT('Ctrl Pts',(-0.115079600404687,-0.0908043159161929,
1.06425052845252));
#15433=CARTESIAN_POINT('Ctrl Pts',(-0.0850581433982766,-0.128851596389654,
1.06689791782678));
#15434=CARTESIAN_POINT('Ctrl Pts',(-0.0342996944683099,-0.150536216937668,
1.06954530720104));
#15435=CARTESIAN_POINT('Ctrl Pts',(0.0139457694684962,-0.145925507476389,
1.0721926965753));
#15436=CARTESIAN_POINT('Ctrl Pts',(0.0621912334052997,-0.14131479801511,
1.07484008594956));
#15437=CARTESIAN_POINT('Ctrl Pts',(0.107923712348941,-0.110408758544542,
1.07748747532382));
#15438=CARTESIAN_POINT('Ctrl Pts',(0.1301953818052,-0.0673639426912374,
1.08013486469808));
#15439=CARTESIAN_POINT('Ctrl Pts',(0.15246705126146,-0.024319126837932,
1.08278225407234));
#15440=CARTESIAN_POINT('Ctrl Pts',(0.151277911230334,0.0308644653981125,
1.0854296434466));
#15441=CARTESIAN_POINT('Ctrl Pts',(0.127172648928576,0.0729099141598672,
1.08807703282086));
#15442=CARTESIAN_POINT('Ctrl Pts',(0.103067386626818,0.114955362921624,
1.09072442219512));
#15443=CARTESIAN_POINT('Ctrl Pts',(0.0560460020544268,0.143862668209093,
1.09337181156938));
#15444=CARTESIAN_POINT('Ctrl Pts',(0.00764670469074742,0.146390799320458,
1.09601920094364));
#15445=CARTESIAN_POINT('Ctrl Pts',(-0.0407525926729279,0.148918930431823,
1.0986665903179));
#15446=CARTESIAN_POINT('Ctrl Pts',(-0.0905298028278899,0.125067887367091,
1.10131397969216));
#15447=CARTESIAN_POINT('Ctrl Pts',(-0.11888440661962,0.0857626730052823,
1.10396136906642));
#15448=CARTESIAN_POINT('Ctrl Pts',(-0.136639133674055,0.0611510311732957,
1.10561907784952));
#15449=CARTESIAN_POINT('Ctrl Pts',(-0.145994366384503,0.0304800321277272,
1.10727678663261));
#15450=CARTESIAN_POINT('Ctrl Pts',(-0.146170555016798,-9.22629125885076E-5,
1.10893449541571));
#15451=CARTESIAN_POINT('Origin',(0.,0.,0.));
#15452=CARTESIAN_POINT('',(-0.146577386142569,-3.88073511912723E-5,1.16606550458429));
#15453=CARTESIAN_POINT('',(-0.146552328192774,-6.73160170860698E-5,1.15893449541571));
#15454=CARTESIAN_POINT('',(-0.14635,-1.79227059055215E-17,0.));
#15455=CARTESIAN_POINT('Ctrl Pts',(-0.146577386142569,-3.88073511912723E-5,
1.16606550458429));
#15456=CARTESIAN_POINT('Ctrl Pts',(-0.146413350709018,0.0463056768050285,
1.16353456384924));
#15457=CARTESIAN_POINT('Ctrl Pts',(-0.122574225104448,0.0927954474992645,
1.1610036231142));
#15458=CARTESIAN_POINT('Ctrl Pts',(-0.0847742546295189,0.119590709008994,
1.15847268237915));
#15459=CARTESIAN_POINT('Ctrl Pts',(-0.0452509303920754,0.147607604138013,
1.15582635250005));
#15460=CARTESIAN_POINT('Ctrl Pts',(0.00953524646069181,0.154093252855687,
1.15318002262095));
#15461=CARTESIAN_POINT('Ctrl Pts',(0.0545077808453859,0.136079071706768,
1.15053369274185));
#15462=CARTESIAN_POINT('Ctrl Pts',(0.0994803152300801,0.118064890557849,
1.14788736286275));
#15463=CARTESIAN_POINT('Ctrl Pts',(0.134639207146701,0.0755508795423365,
1.14524103298364));
#15464=CARTESIAN_POINT('Ctrl Pts',(0.14389167861853,0.027996370364851,1.14259470310454));
#15465=CARTESIAN_POINT('Ctrl Pts',(0.15314415009036,-0.0195581388126345,
1.13994837322544));
#15466=CARTESIAN_POINT('Ctrl Pts',(0.136490201117397,-0.0721531461520931,
1.13730204334634));
#15467=CARTESIAN_POINT('Ctrl Pts',(0.101552606157185,-0.105715089329518,
1.13465571346724));
#15468=CARTESIAN_POINT('Ctrl Pts',(0.0666150111969725,-0.139277032506943,
1.13200938358813));
#15469=CARTESIAN_POINT('Ctrl Pts',(0.0133937702495101,-0.153805911522335,
1.12936305370903));
#15470=CARTESIAN_POINT('Ctrl Pts',(-0.033750917386428,-0.142651629870951,
1.12671672382993));
#15471=CARTESIAN_POINT('Ctrl Pts',(-0.0808956050223675,-0.131497348219567,
1.12407039395083));
#15472=CARTESIAN_POINT('Ctrl Pts',(-0.121963739346782,-0.094659905901407,
1.12142406407173));
#15473=CARTESIAN_POINT('Ctrl Pts',(-0.1381577891642,-0.0490003798202082,
1.11877773419262));
#15474=CARTESIAN_POINT('Ctrl Pts',(-0.143690228857438,-0.0334015285560649,
1.11787365765651));
#15475=CARTESIAN_POINT('Ctrl Pts',(-0.146319518115206,-0.0167730178360648,
1.1169695811204));
#15476=CARTESIAN_POINT('Ctrl Pts',(-0.146204073634541,-0.000109175101205505,
1.11606550458429));
#15477=CARTESIAN_POINT('Ctrl Pts',(-0.146170555016798,-9.22629125885076E-5,
1.10893449541571));
#15478=CARTESIAN_POINT('Ctrl Pts',(-0.146275742653821,-0.0183444476975235,
1.10992417600687));
#15479=CARTESIAN_POINT('Ctrl Pts',(-0.143109248288425,-0.0365614514641733,
1.11091385659804));
#15480=CARTESIAN_POINT('Ctrl Pts',(-0.136505188007283,-0.0534328725168923,
1.1119035371892));
#15481=CARTESIAN_POINT('Ctrl Pts',(-0.118839368174718,-0.0985638180183679,
1.11455092656346));
#15482=CARTESIAN_POINT('Ctrl Pts',(-0.0765757310810901,-0.134066323362434,
1.11719831593772));
#15483=CARTESIAN_POINT('Ctrl Pts',(-0.0290731934694857,-0.143678417446031,
1.11984570531198));
#15484=CARTESIAN_POINT('Ctrl Pts',(0.01842934414212,-0.153290511529629,
1.12249309468624));
#15485=CARTESIAN_POINT('Ctrl Pts',(0.071170782271703,-0.137012194352758,
1.1251404840605));
#15486=CARTESIAN_POINT('Ctrl Pts',(0.10499283308901,-0.102299771349957,
1.12778787343476));
#15487=CARTESIAN_POINT('Ctrl Pts',(0.138814883906317,-0.0675873483471558,
1.13043526280902));
#15488=CARTESIAN_POINT('Ctrl Pts',(0.153717547411349,-0.0144408195184256,
1.13308265218328));
#15489=CARTESIAN_POINT('Ctrl Pts',(0.142874638214406,0.0327959749574983,
1.13573004155754));
#15490=CARTESIAN_POINT('Ctrl Pts',(0.132031729017462,0.0800327694334235,
1.1383774309318));
#15491=CARTESIAN_POINT('Ctrl Pts',(0.0954432471185425,0.121359829556542,
1.14102482030606));
#15492=CARTESIAN_POINT('Ctrl Pts',(0.0498685966661331,0.137847238945365,
1.14367220968032));
#15493=CARTESIAN_POINT('Ctrl Pts',(0.00429394621372511,0.154334648334189,
1.14631959905458));
#15494=CARTESIAN_POINT('Ctrl Pts',(-0.0502668727921719,0.145982406988718,
1.14896698842884));
#15495=CARTESIAN_POINT('Ctrl Pts',(-0.0888222026239048,0.116616270474356,
1.1516143778031));
#15496=CARTESIAN_POINT('Ctrl Pts',(-0.124357782404925,0.0895501633622979,
1.1540544170073));
#15497=CARTESIAN_POINT('Ctrl Pts',(-0.146296868742479,0.0446329749882746,
1.15649445621151));
#15498=CARTESIAN_POINT('Ctrl Pts',(-0.146552328192774,-6.73160170860698E-5,
1.15893449541571));
#15499=CARTESIAN_POINT('Origin',(0.,0.,0.));
#15500=CARTESIAN_POINT('',(-0.146318311025392,0.000133437649768732,1.21606550458429));
#15501=CARTESIAN_POINT('',(-0.146373054956946,0.000132657382717961,1.20893449541571));
#15502=CARTESIAN_POINT('',(-0.14635,-1.79227059055215E-17,0.));
#15503=CARTESIAN_POINT('Ctrl Pts',(-0.146318311025392,0.000133437649768732,
1.21606550458429));
#15504=CARTESIAN_POINT('Ctrl Pts',(-0.146429658069886,0.0125190846592594,
1.21539220633629));
#15505=CARTESIAN_POINT('Ctrl Pts',(-0.144988168643405,0.0248791929292086,
1.21471890808829));
#15506=CARTESIAN_POINT('Ctrl Pts',(-0.141892968227885,0.0368102906365087,
1.21404560984029));
#15507=CARTESIAN_POINT('Ctrl Pts',(-0.129727599662405,0.083704249513052,
1.21139927996119));
#15508=CARTESIAN_POINT('Ctrl Pts',(-0.0920156607298113,0.123970842060419,
1.20875295008209));
#15509=CARTESIAN_POINT('Ctrl Pts',(-0.0460184991925076,0.139179415364965,
1.20610662020299));
#15510=CARTESIAN_POINT('Ctrl Pts',(-2.13376552038805E-5,0.15438798866951,
1.20346029032389));
#15511=CARTESIAN_POINT('Ctrl Pts',(0.0542610464868107,0.144538542731236,
1.20081396044478));
#15512=CARTESIAN_POINT('Ctrl Pts',(0.091982751999895,0.114139323915075,
1.19816763056568));
#15513=CARTESIAN_POINT('Ctrl Pts',(0.129704457512977,0.0837401050989159,
1.19552130068658));
#15514=CARTESIAN_POINT('Ctrl Pts',(0.150865484397133,0.0327911134048729,
1.19287497080748));
#15515=CARTESIAN_POINT('Ctrl Pts',(0.145780097726084,-0.0153874961003253,
1.19022864092838));
#15516=CARTESIAN_POINT('Ctrl Pts',(0.140694711055036,-0.063566105605525,
1.18758231104927));
#15517=CARTESIAN_POINT('Ctrl Pts',(0.109362910828785,-0.108974332921877,
1.18493598117017));
#15518=CARTESIAN_POINT('Ctrl Pts',(0.0661257549466402,-0.130828118009858,
1.18228965129107));
#15519=CARTESIAN_POINT('Ctrl Pts',(0.0228885990644955,-0.152681903097838,
1.17964332141197));
#15520=CARTESIAN_POINT('Ctrl Pts',(-0.0322539124735426,-0.150981245957443,
1.17699699153287));
#15521=CARTESIAN_POINT('Ctrl Pts',(-0.0740621845924981,-0.126504564117865,
1.17435066165376));
#15522=CARTESIAN_POINT('Ctrl Pts',(-0.115870456711455,-0.102027882278287,
1.17170433177466));
#15523=CARTESIAN_POINT('Ctrl Pts',(-0.144344489411329,-0.0547751757395235,
1.16905800189556));
#15524=CARTESIAN_POINT('Ctrl Pts',(-0.146451269950206,-0.00637475169995868,
1.16641167201646));
#15525=CARTESIAN_POINT('Ctrl Pts',(-0.146543132875163,-0.00426432565444621,
1.1662962828724));
#15526=CARTESIAN_POINT('Ctrl Pts',(-0.146584864748453,-0.00215171749738942,
1.16618089372835));
#15527=CARTESIAN_POINT('Ctrl Pts',(-0.146577386142569,-3.88073511912723E-5,
1.16606550458429));
#15528=CARTESIAN_POINT('Ctrl Pts',(-0.146552328192774,-6.73160170860698E-5,
1.15893449541571));
#15529=CARTESIAN_POINT('Ctrl Pts',(-0.146574036680232,-0.00386586684592084,
1.15914184558577));
#15530=CARTESIAN_POINT('Ctrl Pts',(-0.1464391612665,-0.00766285139452399,
1.15934919575582));
#15531=CARTESIAN_POINT('Ctrl Pts',(-0.146142739258869,-0.0114471821958193,
1.15955654592588));
#15532=CARTESIAN_POINT('Ctrl Pts',(-0.142358105404532,-0.0597644666683822,
1.16220393530014));
#15533=CARTESIAN_POINT('Ctrl Pts',(-0.112238997038288,-0.106019003930254,
1.1648513246744));
#15534=CARTESIAN_POINT('Ctrl Pts',(-0.0695815129186611,-0.129023839960917,
1.16749871404866));
#15535=CARTESIAN_POINT('Ctrl Pts',(-0.026924028799035,-0.15202867599158,
1.17014610342292));
#15536=CARTESIAN_POINT('Ctrl Pts',(0.0282718310739737,-0.151783810791035,
1.17279349279718));
#15537=CARTESIAN_POINT('Ctrl Pts',(0.0707235276354612,-0.128401405199111,
1.17544088217144));
#15538=CARTESIAN_POINT('Ctrl Pts',(0.11317522419695,-0.105018999607187,
1.1780882715457));
#15539=CARTESIAN_POINT('Ctrl Pts',(0.142882757446916,-0.0584990536238821,
1.18073566091996));
#15540=CARTESIAN_POINT('Ctrl Pts',(0.146238551171451,-0.0101500920973681,
1.18338305029422));
#15541=CARTESIAN_POINT('Ctrl Pts',(0.149594344895986,0.0381988694291446,
1.18603043966848));
#15542=CARTESIAN_POINT('Ctrl Pts',(0.12659839909509,0.0883768464988665,
1.18867782904274));
#15543=CARTESIAN_POINT('Ctrl Pts',(0.0877840381772113,0.117399748124142,
1.191325218417));
#15544=CARTESIAN_POINT('Ctrl Pts',(0.0489696772593311,0.146422649749419,
1.19397260779126));
#15545=CARTESIAN_POINT('Ctrl Pts',(-0.00566309877553352,0.154290475930249,
1.19661999716552));
#15546=CARTESIAN_POINT('Ctrl Pts',(-0.0510896721842483,0.137399358129564,
1.19926738653978));
#15547=CARTESIAN_POINT('Ctrl Pts',(-0.0965162455929618,0.12050824032888,
1.20191477591404));
#15548=CARTESIAN_POINT('Ctrl Pts',(-0.132736616375526,0.0788581785466829,
1.2045621652883));
#15549=CARTESIAN_POINT('Ctrl Pts',(-0.143159994183491,0.0315270405159292,
1.20720955466256));
#15550=CARTESIAN_POINT('Ctrl Pts',(-0.145423823013163,0.021247302336111,
1.20778453491361));
#15551=CARTESIAN_POINT('Ctrl Pts',(-0.146470795531708,0.0106995851133921,
1.20835951516466));
#15552=CARTESIAN_POINT('Ctrl Pts',(-0.146373054956946,0.000132657382717961,
1.20893449541571));
#15553=CARTESIAN_POINT('Origin',(0.,0.,0.));
#15554=CARTESIAN_POINT('',(-0.146120596765396,-4.14129048147555E-5,1.26606550458429));
#15555=CARTESIAN_POINT('',(-0.146109918970638,-1.0198006988139E-5,1.25893449541571));
#15556=CARTESIAN_POINT('',(-0.14635,-1.79227059055215E-17,0.));
#15557=CARTESIAN_POINT('Ctrl Pts',(-0.146120596765396,-4.14129048147555E-5,
1.26606550458429));
#15558=CARTESIAN_POINT('Ctrl Pts',(-0.14605219935785,0.0269443530192317,
1.26460351894424));
#15559=CARTESIAN_POINT('Ctrl Pts',(-0.138898723445843,0.053963836666407,
1.26314153330418));
#15560=CARTESIAN_POINT('Ctrl Pts',(-0.124882896249422,0.0767650581554474,
1.26167954766413));
#15561=CARTESIAN_POINT('Ctrl Pts',(-0.0995129464537159,0.118037388097231,
1.25903321778503));
#15562=CARTESIAN_POINT('Ctrl Pts',(-0.051658938874944,0.145488850208621,
1.25638688790592));
#15563=CARTESIAN_POINT('Ctrl Pts',(-0.00322440565727106,0.146554478394238,
1.25374055802682));
#15564=CARTESIAN_POINT('Ctrl Pts',(0.0452101275604033,0.147620106579856,
1.25109422814772));
#15565=CARTESIAN_POINT('Ctrl Pts',(0.0942251864169787,0.122299900839699,
1.24844789826862));
#15566=CARTESIAN_POINT('Ctrl Pts',(0.121385807331354,0.0821833176976391,
1.24580156838952));
#15567=CARTESIAN_POINT('Ctrl Pts',(0.148546428245729,0.0420667345555804,
1.24315523851041));
#15568=CARTESIAN_POINT('Ctrl Pts',(0.153852611217905,-0.0128462259883804,
1.24050890863131));
#15569=CARTESIAN_POINT('Ctrl Pts',(0.134875632820701,-0.0574210379606392,
1.23786257875221));
#15570=CARTESIAN_POINT('Ctrl Pts',(0.115898654423498,-0.101995849932898,
1.23521624887311));
#15571=CARTESIAN_POINT('Ctrl Pts',(0.0726385146569148,-0.136232513333455,
1.23256991899401));
#15572=CARTESIAN_POINT('Ctrl Pts',(0.0248960600935515,-0.144460368686643,
1.2299235891149));
#15573=CARTESIAN_POINT('Ctrl Pts',(-0.0228463944698117,-0.152688224039831,
1.2272772592358));
#15574=CARTESIAN_POINT('Ctrl Pts',(-0.0750711638299551,-0.134907271345651,
1.2246309293567));
#15575=CARTESIAN_POINT('Ctrl Pts',(-0.107874149410843,-0.0992561323957017,
1.2219845994776));
#15576=CARTESIAN_POINT('Ctrl Pts',(-0.132331163880887,-0.072675612185966,
1.2200115678465));
#15577=CARTESIAN_POINT('Ctrl Pts',(-0.145992019903337,-0.0361614337449312,
1.21803853621539));
#15578=CARTESIAN_POINT('Ctrl Pts',(-0.146318311025392,0.000133437649768732,
1.21606550458429));
#15579=CARTESIAN_POINT('Ctrl Pts',(-0.146373054956946,0.000132657382717961,
1.20893449541571));
#15580=CARTESIAN_POINT('Ctrl Pts',(-0.146020767276673,-0.0379538636644633,
1.21100690453892));
#15581=CARTESIAN_POINT('Ctrl Pts',(-0.130797424420382,-0.0762899498869128,
1.21307931366213));
#15582=CARTESIAN_POINT('Ctrl Pts',(-0.104081054125652,-0.103227285106232,
1.21515172278534));
#15583=CARTESIAN_POINT('Ctrl Pts',(-0.0699523514264828,-0.137638258418326,
1.2177991121596));
#15584=CARTESIAN_POINT('Ctrl Pts',(-0.0170685611947798,-0.153447990763203,
1.22044650153386));
#15585=CARTESIAN_POINT('Ctrl Pts',(0.0303468241642401,-0.143414812629152,
1.22309389090812));
#15586=CARTESIAN_POINT('Ctrl Pts',(0.0777622095232573,-0.133381634495101,
1.22574128028238));
#15587=CARTESIAN_POINT('Ctrl Pts',(0.119709190009594,-0.0975055458821257,
1.22838866965664));
#15588=CARTESIAN_POINT('Ctrl Pts',(0.136973893871985,-0.052219638220276,
1.2310360590309));
#15589=CARTESIAN_POINT('Ctrl Pts',(0.154238597734379,-0.00693373055842239,
1.23368344840516));
#15590=CARTESIAN_POINT('Ctrl Pts',(0.146821024972825,0.0477619961523044,
1.23633083777942));
#15591=CARTESIAN_POINT('Ctrl Pts',(0.118118804930222,0.0868140895256425,
1.23897822715368));
#15592=CARTESIAN_POINT('Ctrl Pts',(0.0894165848876198,0.125866182898978,
1.24162561652794));
#15593=CARTESIAN_POINT('Ctrl Pts',(0.0394297175639698,0.149274642934924,
1.2442730059022));
#15594=CARTESIAN_POINT('Ctrl Pts',(-0.00894524413350711,0.146317192515786,
1.24692039527646));
#15595=CARTESIAN_POINT('Ctrl Pts',(-0.0573202058309854,0.143359742096648,
1.24956778465072));
#15596=CARTESIAN_POINT('Ctrl Pts',(-0.104083261902292,0.114036381222425,
1.25221517402498));
#15597=CARTESIAN_POINT('Ctrl Pts',(-0.127814530591109,0.0717787154251623,
1.25486256339924));
#15598=CARTESIAN_POINT('Ctrl Pts',(-0.139981499518435,0.0501133037087236,
1.2562198740714));
#15599=CARTESIAN_POINT('Ctrl Pts',(-0.146094355379323,0.0250479932723348,
1.25757718474355));
#15600=CARTESIAN_POINT('Ctrl Pts',(-0.146109918970638,-1.0198006988139E-5,
1.25893449541571));
#15601=CARTESIAN_POINT('Origin',(0.,0.,0.));
#15602=CARTESIAN_POINT('',(-0.146470135615938,-0.000111966546850736,1.31606550458429));
#15603=CARTESIAN_POINT('',(-0.146410535958061,-0.000127756381200432,1.30893449541571));
#15604=CARTESIAN_POINT('',(-0.14635,-1.79227059055215E-17,0.));
#15605=CARTESIAN_POINT('Ctrl Pts',(-0.146470135615938,-0.000111966546850736,
1.31606550458429));
#15606=CARTESIAN_POINT('Ctrl Pts',(-0.146120207411574,0.0411799307449602,
1.31381483155218));
#15607=CARTESIAN_POINT('Ctrl Pts',(-0.127827491572984,0.0827431563937987,
1.31156415852007));
#15608=CARTESIAN_POINT('Ctrl Pts',(-0.0969137672218927,0.10998333351997,
1.30931348548796));
#15609=CARTESIAN_POINT('Ctrl Pts',(-0.0605655677022408,0.142012194937238,
1.30666715560886));
#15610=CARTESIAN_POINT('Ctrl Pts',(-0.00676890401288169,0.154239532672684,
1.30402082572976));
#15611=CARTESIAN_POINT('Ctrl Pts',(0.0398526445220406,0.14106870189023,
1.30137449585066));
#15612=CARTESIAN_POINT('Ctrl Pts',(0.0864741930569617,0.127897871107775,
1.29872816597155));
#15613=CARTESIAN_POINT('Ctrl Pts',(0.125920626437448,0.0893288718074177,
1.29608183609245));
#15614=CARTESIAN_POINT('Ctrl Pts',(0.14013669149516,0.0430153417578024,
1.29343550621335));
#15615=CARTESIAN_POINT('Ctrl Pts',(0.154352756552873,-0.00329818829181684,
1.29078917633425));
#15616=CARTESIAN_POINT('Ctrl Pts',(0.143338453287813,-0.0573562490906975,
1.28814284645515));
#15617=CARTESIAN_POINT('Ctrl Pts',(0.112135201594409,-0.0944156157243562,
1.28549651657604));
#15618=CARTESIAN_POINT('Ctrl Pts',(0.0809319499010078,-0.131474982358013,
1.28285018669694));
#15619=CARTESIAN_POINT('Ctrl Pts',(0.0295397497792676,-0.151535654826449,
1.28020385681784));
#15620=CARTESIAN_POINT('Ctrl Pts',(-0.0185183802362589,-0.1454155477333,
1.27755752693874));
#15621=CARTESIAN_POINT('Ctrl Pts',(-0.066576510251784,-0.139295440640151,
1.27491119705964));
#15622=CARTESIAN_POINT('Ctrl Pts',(-0.111300570161094,-0.106994553985419,
1.27226486718053));
#15623=CARTESIAN_POINT('Ctrl Pts',(-0.13221965410943,-0.0632975117719662,
1.26961853730143));
#15624=CARTESIAN_POINT('Ctrl Pts',(-0.141581826511298,-0.0437412423069929,
1.26843419306239));
#15625=CARTESIAN_POINT('Ctrl Pts',(-0.146176005022067,-0.0219023912433209,
1.26724984882334));
#15626=CARTESIAN_POINT('Ctrl Pts',(-0.146120596765396,-4.14129048147555E-5,
1.26606550458429));
#15627=CARTESIAN_POINT('Ctrl Pts',(-0.146109918970638,-1.0198006988139E-5,
1.25893449541571));
#15628=CARTESIAN_POINT('Ctrl Pts',(-0.146124711647138,-0.0238271763493914,
1.26022457411781));
#15629=CARTESIAN_POINT('Ctrl Pts',(-0.140631289159497,-0.0476377233371588,
1.26151465281992));
#15630=CARTESIAN_POINT('Ctrl Pts',(-0.129592576141605,-0.0685164391025303,
1.26280473152202));
#15631=CARTESIAN_POINT('Ctrl Pts',(-0.106939871696956,-0.111361957112663,
1.26545212089628));
#15632=CARTESIAN_POINT('Ctrl Pts',(-0.0609349815013302,-0.141861022412626,
1.26809951027054));
#15633=CARTESIAN_POINT('Ctrl Pts',(-0.0126505083952331,-0.146043496451057,
1.2707468996448));
#15634=CARTESIAN_POINT('Ctrl Pts',(0.0356339647108625,-0.150225970489488,
1.27339428901906));
#15635=CARTESIAN_POINT('Ctrl Pts',(0.0861980207274291,-0.128091853266388,
1.27604167839332));
#15636=CARTESIAN_POINT('Ctrl Pts',(0.11588072467734,-0.0897797074320025,
1.27868906776758));
#15637=CARTESIAN_POINT('Ctrl Pts',(0.145563428627253,-0.0514675615976161,
1.28133645714184));
#15638=CARTESIAN_POINT('Ctrl Pts',(0.154364780510509,0.00302261284805656,
1.2839838465161));
#15639=CARTESIAN_POINT('Ctrl Pts',(0.138253309066183,0.0487315170146188,
1.28663123589036));
#15640=CARTESIAN_POINT('Ctrl Pts',(0.122141837621857,0.0944404211811797,
1.28927862526462));
#15641=CARTESIAN_POINT('Ctrl Pts',(0.0811175428499519,0.131368055068631,
1.29192601463888));
#15642=CARTESIAN_POINT('Ctrl Pts',(0.0339716590485425,0.142599665496764,
1.29457340401314));
#15643=CARTESIAN_POINT('Ctrl Pts',(-0.013174224752867,0.153831275924897,
1.2972207933874));
#15644=CARTESIAN_POINT('Ctrl Pts',(-0.0664416975837803,0.139366862893713,
1.29986818276166));
#15645=CARTESIAN_POINT('Ctrl Pts',(-0.101431520699135,0.105831870563862,
1.30251557213592));
#15646=CARTESIAN_POINT('Ctrl Pts',(-0.129710573305276,0.0787286237393239,
1.30465521322918));
#15647=CARTESIAN_POINT('Ctrl Pts',(-0.146050663974784,0.0391684733249047,
1.30679485432245));
#15648=CARTESIAN_POINT('Ctrl Pts',(-0.146410535958061,-0.000127756381200432,
1.30893449541571));
#15649=CARTESIAN_POINT('Origin',(0.,0.,0.));
#15650=CARTESIAN_POINT('',(-0.146471469669193,0.000111495080380188,1.36606550458429));
#15651=CARTESIAN_POINT('',(-0.146526884620975,8.5711493927648E-5,1.35893449541571));
#15652=CARTESIAN_POINT('',(-0.14635,-1.79227059055215E-17,0.));
#15653=CARTESIAN_POINT('Ctrl Pts',(-0.146471469669193,0.000111495080380188,
1.36606550458429));
#15654=CARTESIAN_POINT('Ctrl Pts',(-0.146532402405025,0.0073220458586883,
1.36567247403923));
#15655=CARTESIAN_POINT('Ctrl Pts',(-0.146045973070864,0.0145243451116175,
1.36527944349416));
#15656=CARTESIAN_POINT('Ctrl Pts',(-0.144983764805735,0.0216407019395156,
1.3648864129491));
#15657=CARTESIAN_POINT('Ctrl Pts',(-0.137831767320671,0.0695561322809842,
1.36224008307));
#15658=CARTESIAN_POINT('Ctrl Pts',(-0.104576727819841,0.113575347233418,
1.3595937531909));
#15659=CARTESIAN_POINT('Ctrl Pts',(-0.060440002550743,0.133550058215342,
1.3569474233118));
#15660=CARTESIAN_POINT('Ctrl Pts',(-0.0163032772816473,0.153524769197265,
1.35430109343269));
#15661=CARTESIAN_POINT('Ctrl Pts',(0.0387151337557165,0.149454976208681,
1.35165476355359));
#15662=CARTESIAN_POINT('Ctrl Pts',(0.0794324390145508,0.123203488242689,
1.34900843367449));
#15663=CARTESIAN_POINT('Ctrl Pts',(0.120149744273387,0.0969520002766962,
1.34636210379539));
#15664=CARTESIAN_POINT('Ctrl Pts',(0.146565943753694,0.048518817333291,
1.34371577391629));
#15665=CARTESIAN_POINT('Ctrl Pts',(0.14658992694451,7.25688577880009E-5,
1.34106944403718));
#15666=CARTESIAN_POINT('Ctrl Pts',(0.146613910135327,-0.0483736796177136,
1.33842311415808));
#15667=CARTESIAN_POINT('Ctrl Pts',(0.120245677036657,-0.0968329936253116,
1.33577678427898));
#15668=CARTESIAN_POINT('Ctrl Pts',(0.0795543829983497,-0.123124782547022,
1.33313045439988));
#15669=CARTESIAN_POINT('Ctrl Pts',(0.0388630889600415,-0.149416571468734,
1.33048412452078));
#15670=CARTESIAN_POINT('Ctrl Pts',(-0.0161512660179049,-0.153540835304554,
1.32783779464168));
#15671=CARTESIAN_POINT('Ctrl Pts',(-0.0603077462478081,-0.133609833714981,
1.32519146476257));
#15672=CARTESIAN_POINT('Ctrl Pts',(-0.10446422647771,-0.113678832125408,
1.32254513488347));
#15673=CARTESIAN_POINT('Ctrl Pts',(-0.137762831959571,-0.0696925651104417,
1.31989880500437));
#15674=CARTESIAN_POINT('Ctrl Pts',(-0.144962267025529,-0.0217842390534145,
1.31725247512527));
#15675=CARTESIAN_POINT('Ctrl Pts',(-0.146038665626028,-0.0146213916011371,
1.31685681827827));
#15676=CARTESIAN_POINT('Ctrl Pts',(-0.146531651210624,-0.00737087161912708,
1.31646116143128));
#15677=CARTESIAN_POINT('Ctrl Pts',(-0.146470135615938,-0.000111966546850736,
1.31606550458429));
#15678=CARTESIAN_POINT('Ctrl Pts',(-0.146410535958061,-0.000127756381200432,
1.30893449541571));
#15679=CARTESIAN_POINT('Ctrl Pts',(-0.146495935505426,-0.00945296197092968,
1.30944224369671));
#15680=CARTESIAN_POINT('Ctrl Pts',(-0.145681427739287,-0.018763305174839,
1.3099499919777));
#15681=CARTESIAN_POINT('Ctrl Pts',(-0.143913007029536,-0.0278887903271487,
1.3104577402587));
#15682=CARTESIAN_POINT('Ctrl Pts',(-0.134692496844786,-0.0754688872597875,
1.31310512963296));
#15683=CARTESIAN_POINT('Ctrl Pts',(-0.0995393030754929,-0.118023509496548,
1.31575251900722));
#15684=CARTESIAN_POINT('Ctrl Pts',(-0.0545553941775042,-0.136060454153345,
1.31839990838148));
#15685=CARTESIAN_POINT('Ctrl Pts',(-0.00957148527951295,-0.154097398810142,
1.32104729775574));
#15686=CARTESIAN_POINT('Ctrl Pts',(0.0452431387471776,-0.14761666588697,
1.32369468713));
#15687=CARTESIAN_POINT('Ctrl Pts',(0.0847805644327026,-0.119586763955155,
1.32634207650426));
#15688=CARTESIAN_POINT('Ctrl Pts',(0.124317990118227,-0.09155686202334,
1.32898946587852));
#15689=CARTESIAN_POINT('Ctrl Pts',(0.148578217462589,-0.041977791082884,
1.33163685525278));
#15690=CARTESIAN_POINT('Ctrl Pts',(0.146448816178573,0.00644068764408242,
1.33428424462704));
#15691=CARTESIAN_POINT('Ctrl Pts',(0.144319414894557,0.0548591663710502,
1.3369316340013));
#15692=CARTESIAN_POINT('Ctrl Pts',(0.115800384982161,0.102117052884526,
1.33957902337556));
#15693=CARTESIAN_POINT('Ctrl Pts',(0.0739549070570988,0.126567807678519,
1.34222641274982));
#15694=CARTESIAN_POINT('Ctrl Pts',(0.0321094291320376,0.151018562472512,
1.34487380212408));
#15695=CARTESIAN_POINT('Ctrl Pts',(-0.0230624968056921,0.152662185547021,
1.34752119149834));
#15696=CARTESIAN_POINT('Ctrl Pts',(-0.0662892946253695,0.1307458130856,
1.3501685808726));
#15697=CARTESIAN_POINT('Ctrl Pts',(-0.109516092445046,0.10882944062418,
1.35281597024686));
#15698=CARTESIAN_POINT('Ctrl Pts',(-0.140797762146673,0.0633530726268328,
1.35546335962112));
#15699=CARTESIAN_POINT('Ctrl Pts',(-0.145805692234247,0.0151472216574969,
1.35811074899538));
#15700=CARTESIAN_POINT('Ctrl Pts',(-0.146325105122407,0.0101474034011793,
1.35838533113549));
#15701=CARTESIAN_POINT('Ctrl Pts',(-0.146561879835735,0.00511822289583405,
1.3586599132756));
#15702=CARTESIAN_POINT('Ctrl Pts',(-0.146526884620975,8.5711493927648E-5,
1.35893449541571));
#15703=CARTESIAN_POINT('Origin',(0.,0.,0.));
#15704=CARTESIAN_POINT('',(-0.146120987371435,4.2191387702159E-5,1.41606550458429));
#15705=CARTESIAN_POINT('',(-0.146148882937928,7.6306569664006E-5,1.40893449541571));
#15706=CARTESIAN_POINT('',(-0.14635,-1.79227059055215E-17,0.));
#15707=CARTESIAN_POINT('Ctrl Pts',(-0.146120987371435,4.2191387702159E-5,
1.41606550458429));
#15708=CARTESIAN_POINT('Ctrl Pts',(-0.146177309023295,0.021854523983563,
1.41488378664717));
#15709=CARTESIAN_POINT('Ctrl Pts',(-0.141604359564088,0.0436444172696427,
1.41370206871005));
#15710=CARTESIAN_POINT('Ctrl Pts',(-0.132282279973341,0.0631665524487371,
1.41252035077294));
#15711=CARTESIAN_POINT('Ctrl Pts',(-0.1114064880593,0.106884268839086,1.40987402089383));
#15712=CARTESIAN_POINT('Ctrl Pts',(-0.0667143915920224,0.139229456738304,
1.40722769101473));
#15713=CARTESIAN_POINT('Ctrl Pts',(-0.0186623352932378,0.145397151366753,
1.40458136113563));
#15714=CARTESIAN_POINT('Ctrl Pts',(0.0293897210055454,0.151564845995202,
1.40193503125653));
#15715=CARTESIAN_POINT('Ctrl Pts',(0.0808017371358351,0.131555047352884,
1.39928870137743));
#15716=CARTESIAN_POINT('Ctrl Pts',(0.112041660826149,0.0945265884816804,
1.39664237149832));
#15717=CARTESIAN_POINT('Ctrl Pts',(0.143281584516463,0.0574981296104763,
1.39399604161922));
#15718=CARTESIAN_POINT('Ctrl Pts',(0.154349415766802,0.00345101051038574,
1.39134971174012));
#15719=CARTESIAN_POINT('Ctrl Pts',(0.140179214932283,-0.0428765696854336,
1.38870338186102));
#15720=CARTESIAN_POINT('Ctrl Pts',(0.126009014097764,-0.089204149881253,
1.38605705198192));
#15721=CARTESIAN_POINT('Ctrl Pts',(0.0866007811783877,-0.127812191172801,
1.38341072210282));
#15722=CARTESIAN_POINT('Ctrl Pts',(0.0399922944706322,-0.14102917638501,
1.38076439222371));
#15723=CARTESIAN_POINT('Ctrl Pts',(-0.00661619223712474,-0.15424616159722,
1.37811806234461));
#15724=CARTESIAN_POINT('Ctrl Pts',(-0.060424932733261,-0.142072090730089,
1.37547173246551));
#15725=CARTESIAN_POINT('Ctrl Pts',(-0.0968048252466797,-0.110079232431271,
1.37282540258641));
#15726=CARTESIAN_POINT('Ctrl Pts',(-0.127781608685608,-0.08283792481198,
1.37057210325237));
#15727=CARTESIAN_POINT('Ctrl Pts',(-0.146122133733866,-0.0412276055847571,
1.36831880391833));
#15728=CARTESIAN_POINT('Ctrl Pts',(-0.146471469669193,0.000111495080380188,
1.36606550458429));
#15729=CARTESIAN_POINT('Ctrl Pts',(-0.146526884620975,8.5711493927648E-5,
1.35893449541571));
#15730=CARTESIAN_POINT('Ctrl Pts',(-0.146224472749943,-0.0434028397118431,
1.36130730264986));
#15731=CARTESIAN_POINT('Ctrl Pts',(-0.125627402569456,-0.0871401285467012,
1.36368010988401));
#15732=CARTESIAN_POINT('Ctrl Pts',(-0.0917490966422633,-0.114327780902106,
1.36605291711816));
#15733=CARTESIAN_POINT('Ctrl Pts',(-0.0539503804891888,-0.144661598551044,
1.36870030649242));
#15734=CARTESIAN_POINT('Ctrl Pts',(0.00038124229047478,-0.154393899907594,
1.37134769586668));
#15735=CARTESIAN_POINT('Ctrl Pts',(0.0463590973565905,-0.139066790892088,
1.37399508524094));
#15736=CARTESIAN_POINT('Ctrl Pts',(0.0923369524227062,-0.123739681876581,
1.3766424746152));
#15737=CARTESIAN_POINT('Ctrl Pts',(0.129961039775272,-0.083353162489017,
1.37928986398946));
#15738=CARTESIAN_POINT('Ctrl Pts',(0.141997595260484,-0.0364063334065561,
1.38193725336372));
#15739=CARTESIAN_POINT('Ctrl Pts',(0.154034150745695,0.0105404956759021,
1.38458464273798));
#15740=CARTESIAN_POINT('Ctrl Pts',(0.140483174363557,0.0640476344532581,
1.38723203211224));
#15741=CARTESIAN_POINT('Ctrl Pts',(0.10755170844225,0.0996060653705087,
1.3898794214865));
#15742=CARTESIAN_POINT('Ctrl Pts',(0.0746202425209409,0.135164496287762,
1.39252681086076));
#15743=CARTESIAN_POINT('Ctrl Pts',(0.0223082870604623,0.152774219344908,
1.39517420023502));
#15744=CARTESIAN_POINT('Ctrl Pts',(-0.025422593472234,0.144369075867769,
1.39782158960928));
#15745=CARTESIAN_POINT('Ctrl Pts',(-0.073153474004929,0.135963932390631,
1.40046897898354));
#15746=CARTESIAN_POINT('Ctrl Pts',(-0.11630327960984,0.101543922379208,
1.4031163683578));
#15747=CARTESIAN_POINT('Ctrl Pts',(-0.135107186188192,0.0568751802851974,
1.40576375773206));
#15748=CARTESIAN_POINT('Ctrl Pts',(-0.142614236437708,0.0390421576584788,
1.40682067029328));
#15749=CARTESIAN_POINT('Ctrl Pts',(-0.14624095998336,0.0195756595648056,
1.40787758285449));
#15750=CARTESIAN_POINT('Ctrl Pts',(-0.146148882937928,7.6306569664006E-5,
1.40893449541571));
#15751=CARTESIAN_POINT('Origin',(0.,0.,0.));
#15752=CARTESIAN_POINT('',(-0.14631473222987,-0.000131398079681141,1.46606550458429));
#15753=CARTESIAN_POINT('',(-0.146248097568756,-0.000123763188177425,1.45893449541571));
#15754=CARTESIAN_POINT('',(-0.14635,-1.79227059055215E-17,0.));
#15755=CARTESIAN_POINT('Ctrl Pts',(-0.14631473222987,-0.000131398079681141,
1.46606550458429));
#15756=CARTESIAN_POINT('Ctrl Pts',(-0.145989697979493,0.0361157155227289,
1.46409509925512));
#15757=CARTESIAN_POINT('Ctrl Pts',(-0.132370868650209,0.0725796635271419,
1.46212469392594));
#15758=CARTESIAN_POINT('Ctrl Pts',(-0.107973319296019,0.0991484059484618,
1.46015428859677));
#15759=CARTESIAN_POINT('Ctrl Pts',(-0.0752064754000165,0.134831245351468,
1.45750795871767));
#15760=CARTESIAN_POINT('Ctrl Pts',(-0.0229974942306327,0.152665588379184,
1.45486162883857));
#15761=CARTESIAN_POINT('Ctrl Pts',(0.0247535192036911,0.144485406820094,
1.45221529895946));
#15762=CARTESIAN_POINT('Ctrl Pts',(0.0725045326380122,0.136305225261004,
1.44956896908036));
#15763=CARTESIAN_POINT('Ctrl Pts',(0.115797578337275,0.102110519115111,
1.44692263920126));
#15764=CARTESIAN_POINT('Ctrl Pts',(0.134818450998255,0.0575543070937695,
1.44427630932216));
#15765=CARTESIAN_POINT('Ctrl Pts',(0.153839323659235,0.0129980950724284,
1.44162997944306));
#15766=CARTESIAN_POINT('Ctrl Pts',(0.148588023281934,-0.0419196228243577,
1.43898364956396));
#15767=CARTESIAN_POINT('Ctrl Pts',(0.121467255745355,-0.082062966762292,
1.43633731968485));
#15768=CARTESIAN_POINT('Ctrl Pts',(0.0943464882087764,-0.122206310700226,
1.43369098980575));
#15769=CARTESIAN_POINT('Ctrl Pts',(0.0453562535129183,-0.147575280679306,
1.43104465992665));
#15770=CARTESIAN_POINT('Ctrl Pts',(-0.00307937473935208,-0.146557666176543,
1.42839833004755));
#15771=CARTESIAN_POINT('Ctrl Pts',(-0.0515150029916225,-0.14554005167378,
1.42575200016845));
#15772=CARTESIAN_POINT('Ctrl Pts',(-0.0993960248003067,-0.118135852689175,
1.42310567028934));
#15773=CARTESIAN_POINT('Ctrl Pts',(-0.124806792024246,-0.0768886307561326,
1.42045934041024));
#15774=CARTESIAN_POINT('Ctrl Pts',(-0.138870387581649,-0.0540603453281256,
1.41899472846826));
#15775=CARTESIAN_POINT('Ctrl Pts',(-0.146051182757901,-0.0269918425378075,
1.41753011652627));
#15776=CARTESIAN_POINT('Ctrl Pts',(-0.146120987371435,4.2191387702159E-5,
1.41606550458429));
#15777=CARTESIAN_POINT('Ctrl Pts',(-0.146148882937928,7.6306569664006E-5,
1.40893449541571));
#15778=CARTESIAN_POINT('Ctrl Pts',(-0.146010322369016,-0.0292669616874671,
1.41052497222875));
#15779=CARTESIAN_POINT('Ctrl Pts',(-0.137450455640384,-0.0586846305953837,
1.4121154490418));
#15780=CARTESIAN_POINT('Ctrl Pts',(-0.121019719714466,-0.0827222215753489,
1.41370592585484));
#15781=CARTESIAN_POINT('Ctrl Pts',(-0.0936703391105966,-0.122733407165291,
1.4163533152291));
#15782=CARTESIAN_POINT('Ctrl Pts',(-0.0445135703510636,-0.147838304168576,
1.41900070460336));
#15783=CARTESIAN_POINT('Ctrl Pts',(0.00393424939099551,-0.146537573651384,
1.42164809397762));
#15784=CARTESIAN_POINT('Ctrl Pts',(0.0523820691330518,-0.145236843134192,
1.42429548335188));
#15785=CARTESIAN_POINT('Ctrl Pts',(0.100120939857634,-0.117530485096527,
1.42694287272614));
#15786=CARTESIAN_POINT('Ctrl Pts',(0.125284029446909,-0.0761094471358441,
1.4295902621004));
#15787=CARTESIAN_POINT('Ctrl Pts',(0.150447119036187,-0.0346884091751576,
1.43223765147466));
#15788=CARTESIAN_POINT('Ctrl Pts',(0.153034427490153,0.020447308708549,
1.43488504084892));
#15789=CARTESIAN_POINT('Ctrl Pts',(0.13186079120536,0.0640427391611241,
1.43753243022318));
#15790=CARTESIAN_POINT('Ctrl Pts',(0.110687154920568,0.107638169613697,
1.44017981959744));
#15791=CARTESIAN_POINT('Ctrl Pts',(0.0657525738970213,0.139693312635139,
1.4428272089717));
#15792=CARTESIAN_POINT('Ctrl Pts',(0.0176394768514684,0.145525221357757,
1.44547459834596));
#15793=CARTESIAN_POINT('Ctrl Pts',(-0.0304736201940859,0.151357130080375,
1.44812198772022));
#15794=CARTESIAN_POINT('Ctrl Pts',(-0.0817652332616461,0.130965804504167,
1.45076937709448));
#15795=CARTESIAN_POINT('Ctrl Pts',(-0.112741325423428,0.0936916042199666,
1.45341676646874));
#15796=CARTESIAN_POINT('Ctrl Pts',(-0.134261605244105,0.0677957870194472,
1.45525600945106));
#15797=CARTESIAN_POINT('Ctrl Pts',(-0.145976367207401,0.0337512577971725,
1.45709525243339));
#15798=CARTESIAN_POINT('Ctrl Pts',(-0.146248097568756,-0.000123763188177425,
1.45893449541571));
#15799=CARTESIAN_POINT('Origin',(0.,0.,-0.0924367114736175));
#15800=CARTESIAN_POINT('',(-0.117746618301147,-0.000105742458702955,1.48256328852638));
#15801=CARTESIAN_POINT('',(-0.117971241274414,-5.28325160115065E-6,1.49243671147361));
#15802=CARTESIAN_POINT('',(-0.117775,2.85464118895969E-14,-0.0924367114736175));
#15803=CARTESIAN_POINT('',(-0.117668597464313,0.00500517689812599,1.532225));
#15804=CARTESIAN_POINT('Ctrl Pts',(-0.117746618301147,-0.000105742458702949,
1.48256328852638));
#15805=CARTESIAN_POINT('Ctrl Pts',(-0.117836347163251,-0.0101121102621826,
1.48323921307631));
#15806=CARTESIAN_POINT('Ctrl Pts',(-0.112089674709738,-0.0591937430214443,
1.48656146750534));
#15807=CARTESIAN_POINT('Ctrl Pts',(-0.0435804807853106,-0.132222740314769,
1.49253005181348));
#15808=CARTESIAN_POINT('Ctrl Pts',(0.0874774386997331,-0.108286040948335,
1.50046904145078));
#15809=CARTESIAN_POINT('Ctrl Pts',(0.138385550162814,0.0147146982980264,
1.50840803108809));
#15810=CARTESIAN_POINT('Ctrl Pts',(0.0627460642121078,0.124368470664037,
1.51634702072539));
#15811=CARTESIAN_POINT('Ctrl Pts',(-0.0706026869052757,0.119928391791904,
1.5242860103627));
#15812=CARTESIAN_POINT('Ctrl Pts',(-0.116004137797729,0.0441355889673283,
1.5295786701209));
#15813=CARTESIAN_POINT('Ctrl Pts',(-0.117668597464313,0.00500517689812487,
1.532225));
#15814=CARTESIAN_POINT('',(-0.0334019664627544,0.1129391839063,1.53222500000001));
#15815=CARTESIAN_POINT('Origin',(0.,0.,1.532225));
#15816=CARTESIAN_POINT('Ctrl Pts',(-0.117971276761593,-5.28420699491729E-6,
1.49243671147361));
#15817=CARTESIAN_POINT('Ctrl Pts',(-0.117971582784674,-0.000385634193345565,
1.49246252744444));
#15818=CARTESIAN_POINT('Ctrl Pts',(-0.117794795258817,-0.0397700451254522,
1.49513573278954));
#15819=CARTESIAN_POINT('Ctrl Pts',(-0.0742871760264013,-0.117748889605885,
1.50045632750888));
#15820=CARTESIAN_POINT('Ctrl Pts',(0.0586284551779338,-0.126233948370975,
1.50839849563167));
#15821=CARTESIAN_POINT('Ctrl Pts',(0.137995068118234,-0.019163470063063,
1.51634066375444));
#15822=CARTESIAN_POINT('Ctrl Pts',(0.0906261803825392,0.105639137646141,
1.52428283187723));
#15823=CARTESIAN_POINT('Ctrl Pts',(0.00417072711528833,0.124051375507138,
1.52957761062575));
#15824=CARTESIAN_POINT('Ctrl Pts',(-0.0334019664627544,0.1129391839063,
1.53222500000001));
#15825=CARTESIAN_POINT('Origin',(0.,0.,-0.0924367114736175));
#15826=CARTESIAN_POINT('',(-0.117590702341447,3.3953472435133E-5,1.43256328852638));
#15827=CARTESIAN_POINT('',(-0.117692994131604,-9.95982882293356E-5,1.44243671147361));
#15828=CARTESIAN_POINT('',(-0.117775,2.85464118895969E-14,-0.0924367114736175));
#15829=CARTESIAN_POINT('Ctrl Pts',(-0.117590702341447,3.39534724351446E-5,
1.43256328852638));
#15830=CARTESIAN_POINT('Ctrl Pts',(-0.117534527156218,-0.0217216553118358,
1.43402790046837));
#15831=CARTESIAN_POINT('Ctrl Pts',(-0.101314495966545,-0.0828641818343832,
1.43813884228945));
#15832=CARTESIAN_POINT('Ctrl Pts',(-0.00292444232197888,-0.139176693688359,
1.44489611398964));
#15833=CARTESIAN_POINT('Ctrl Pts',(0.115350068603298,-0.0779297424218237,
1.45283510362695));
#15834=CARTESIAN_POINT('Ctrl Pts',(0.128028003046829,0.0546551750765237,
1.46077409326425));
#15835=CARTESIAN_POINT('Ctrl Pts',(0.0235079116789307,0.137209630484779,
1.46871308290156));
#15836=CARTESIAN_POINT('Ctrl Pts',(-0.0918059616614023,0.0978189523496558,
1.47597614798894));
#15837=CARTESIAN_POINT('Ctrl Pts',(-0.117485047349053,0.0290640819657798,
1.48059288319721));
#15838=CARTESIAN_POINT('Ctrl Pts',(-0.117746618301147,-0.000105742458702949,
1.48256328852638));
#15839=CARTESIAN_POINT('Ctrl Pts',(-0.117692994131604,-9.9598288229346E-5,
1.44243671147361));
#15840=CARTESIAN_POINT('Ctrl Pts',(-0.117789077779518,-0.0120777797952868,
1.44324485786555));
#15841=CARTESIAN_POINT('Ctrl Pts',(-0.110597905189529,-0.0631824179582176,
1.44670039363175));
#15842=CARTESIAN_POINT('Ctrl Pts',(-0.0368790902657646,-0.134252921254984,
1.45280331877221));
#15843=CARTESIAN_POINT('Ctrl Pts',(0.0928396680879532,-0.103751556080299,
1.46074548689499));
#15844=CARTESIAN_POINT('Ctrl Pts',(0.137511141307062,0.0217950526079239,
1.46868765501776));
#15845=CARTESIAN_POINT('Ctrl Pts',(0.0562018483347667,0.127378648737854,
1.47662982314055));
#15846=CARTESIAN_POINT('Ctrl Pts',(-0.0761502833827582,0.1162998103107,
1.48454617529249));
#15847=CARTESIAN_POINT('Ctrl Pts',(-0.117940200573233,0.0386186906477724,
1.48981513807018));
#15848=CARTESIAN_POINT('Ctrl Pts',(-0.117971276761593,-5.28420699491729E-6,
1.49243671147361));
#15849=CARTESIAN_POINT('Origin',(0.,0.,-0.0924367114736175));
#15850=CARTESIAN_POINT('',(-0.117872752581409,8.97255421561373E-5,1.38256328852638));
#15851=CARTESIAN_POINT('',(-0.117613151267609,6.14076272390171E-5,1.39243671147361));
#15852=CARTESIAN_POINT('',(-0.117775,2.85464118895969E-14,-0.0924367114736175));
#15853=CARTESIAN_POINT('Ctrl Pts',(-0.117872752581409,8.97255421561322E-5,
1.38256328852638));
#15854=CARTESIAN_POINT('Ctrl Pts',(-0.117591624875346,-0.0331778698171688,
1.38481658786042));
#15855=CARTESIAN_POINT('Ctrl Pts',(-0.0854981695600773,-0.105990339321694,
1.38971621707357));
#15856=CARTESIAN_POINT('Ctrl Pts',(0.0379781508110965,-0.133926497290667,
1.39726217616581));
#15857=CARTESIAN_POINT('Ctrl Pts',(0.133119345865688,-0.0407171622080862,
1.40520116580311));
#15858=CARTESIAN_POINT('Ctrl Pts',(0.106398871137127,0.0897659150453452,
1.41314015544042));
#15859=CARTESIAN_POINT('Ctrl Pts',(-0.0177224175491345,0.138074504763813,
1.42107914507772));
#15860=CARTESIAN_POINT('Ctrl Pts',(-0.105714817800915,0.0743914165933911,
1.42755352277305));
#15861=CARTESIAN_POINT('Ctrl Pts',(-0.11763602712824,0.0175874039095825,
1.43138157058926));
#15862=CARTESIAN_POINT('Ctrl Pts',(-0.117590702341447,3.39534724351446E-5,
1.43256328852638));
#15863=CARTESIAN_POINT('Ctrl Pts',(-0.117613151267609,6.1407627239024E-5,
1.39243671147361));
#15864=CARTESIAN_POINT('Ctrl Pts',(-0.117501644803633,-0.0235525549213426,
1.39402718828666));
#15865=CARTESIAN_POINT('Ctrl Pts',(-0.0991469449676741,-0.0866320980727062,
1.39826505447396));
#15866=CARTESIAN_POINT('Ctrl Pts',(0.00373660876362508,-0.139175849115243,
1.40515031003553));
#15867=CARTESIAN_POINT('Ctrl Pts',(0.118990018389619,-0.0722858665142316,
1.41309247815831));
#15868=CARTESIAN_POINT('Ctrl Pts',(0.125236419206141,0.0608253567263532,
1.42103464628109));
#15869=CARTESIAN_POINT('Ctrl Pts',(0.0167532566496359,0.13821437898841,
1.42897681440387));
#15870=CARTESIAN_POINT('Ctrl Pts',(-0.0944771051913143,0.0939940009069027,
1.43611083613471));
#15871=CARTESIAN_POINT('Ctrl Pts',(-0.117474319425011,0.0271612872365273,
1.44059746849129));
#15872=CARTESIAN_POINT('Ctrl Pts',(-0.117692994131604,-9.9598288229346E-5,
1.44243671147361));
#15873=CARTESIAN_POINT('Origin',(0.,0.,-0.0924367114736175));
#15874=CARTESIAN_POINT('',(-0.117871679003533,-9.01049542302267E-5,1.33256328852638));
#15875=CARTESIAN_POINT('',(-0.117917347702326,6.89762296073142E-5,1.34243671147361));
#15876=CARTESIAN_POINT('',(-0.117775,2.85464118895969E-14,-0.0924367114736175));
#15877=CARTESIAN_POINT('Ctrl Pts',(-0.117871679003533,-9.01049542302501E-5,
1.33256328852638));
#15878=CARTESIAN_POINT('Ctrl Pts',(-0.117921183610054,-0.00593170075121234,
1.33295894537338));
#15879=CARTESIAN_POINT('Ctrl Pts',(-0.114870949065289,-0.0507926200311143,
1.33600093209947));
#15880=CARTESIAN_POINT('Ctrl Pts',(-0.0572704544775333,-0.126880813469472,
1.34168924870467));
#15881=CARTESIAN_POINT('Ctrl Pts',(0.0755477687720905,-0.116923823242002,
1.34962823834197));
#15882=CARTESIAN_POINT('Ctrl Pts',(0.13920718769651,6.89141801743488E-5,
1.35756722797928));
#15883=CARTESIAN_POINT('Ctrl Pts',(0.0754319660950179,0.116998564767658,
1.36550621761658));
#15884=CARTESIAN_POINT('Ctrl Pts',(-0.0573960494825499,0.126824048933643,
1.37344520725389));
#15885=CARTESIAN_POINT('Ctrl Pts',(-0.11489462347839,0.0507140179075799,
1.37913089755716));
#15886=CARTESIAN_POINT('Ctrl Pts',(-0.117921788132912,0.00589240827474643,
1.38217025798132));
#15887=CARTESIAN_POINT('Ctrl Pts',(-0.117872752581409,8.97255421561322E-5,
1.38256328852638));
#15888=CARTESIAN_POINT('Ctrl Pts',(-0.117917347702326,6.89762296073276E-5,
1.34243671147361));
#15889=CARTESIAN_POINT('Ctrl Pts',(-0.117673982084908,-0.0349283870656527,
1.34480951870776));
#15890=CARTESIAN_POINT('Ctrl Pts',(-0.0826049238592893,-0.109396528181867,
1.34982971531618));
#15891=CARTESIAN_POINT('Ctrl Pts',(0.0440301174146577,-0.132080378229483,
1.35749730129884));
#15892=CARTESIAN_POINT('Ctrl Pts',(0.13486394497766,-0.0345773583278084,
1.36543946942163));
#15893=CARTESIAN_POINT('Ctrl Pts',(0.102148545386143,0.0946020732301706,
1.3733816375444));
#15894=CARTESIAN_POINT('Ctrl Pts',(-0.0241454188302812,0.137116288461919,
1.38132380566719));
#15895=CARTESIAN_POINT('Ctrl Pts',(-0.107458038693719,0.07065895059964,
1.38767549697692));
#15896=CARTESIAN_POINT('Ctrl Pts',(-0.117687250167678,0.015753490298928,
1.3913797989124));
#15897=CARTESIAN_POINT('Ctrl Pts',(-0.117613151267609,6.1407627239024E-5,
1.39243671147361));
#15898=CARTESIAN_POINT('Origin',(0.,0.,-0.0924367114736175));
#15899=CARTESIAN_POINT('',(-0.117590388001671,-3.33269891443968E-5,1.28256328852638));
#15900=CARTESIAN_POINT('',(-0.117823716245033,-0.000102811805890834,1.29243671147362));
#15901=CARTESIAN_POINT('',(-0.117775,2.85464118895969E-14,-0.0924367114736175));
#15902=CARTESIAN_POINT('Ctrl Pts',(-0.117590388001671,-3.33269891444124E-5,
1.28256328852638));
#15903=CARTESIAN_POINT('Ctrl Pts',(-0.117634977734708,-0.017625925033684,
1.28374763276543));
#15904=CARTESIAN_POINT('Ctrl Pts',(-0.105676786131388,-0.0744702911817869,
1.28757830688358));
#15905=CARTESIAN_POINT('Ctrl Pts',(-0.0175857351491984,-0.138091953858251,
1.29405531088083));
#15906=CARTESIAN_POINT('Ctrl Pts',(0.106487712804436,-0.089660542174548,
1.30199430051814));
#15907=CARTESIAN_POINT('Ctrl Pts',(0.133078957772855,0.0408489510387311,
1.30993329015544));
#15908=CARTESIAN_POINT('Ctrl Pts',(0.0378455373822902,0.133964029124136,
1.31787227979275));
#15909=CARTESIAN_POINT('Ctrl Pts',(-0.0855601048685178,0.105915403748908,
1.32541561258306));
#15910=CARTESIAN_POINT('Ctrl Pts',(-0.117590074669608,0.0331395035428114,
1.33031261549427));
#15911=CARTESIAN_POINT('Ctrl Pts',(-0.117871679003533,-9.01049542302501E-5,
1.33256328852638));
#15912=CARTESIAN_POINT('Ctrl Pts',(-0.117823716245033,-0.000102811805890825,
1.29243671147362));
#15913=CARTESIAN_POINT('Ctrl Pts',(-0.117892441435953,-0.00760726064997237,
1.29294445975461));
#15914=CARTESIAN_POINT('Ctrl Pts',(-0.113819337750002,-0.0541654333254181,
1.29609959740987));
#15915=CARTESIAN_POINT('Ctrl Pts',(-0.0518146499729274,-0.129225073214149,
1.30190212443939));
#15916=CARTESIAN_POINT('Ctrl Pts',(0.0805213734929343,-0.11357898534207,
1.30984429256217));
#15917=CARTESIAN_POINT('Ctrl Pts',(0.1390915465469,0.0061171215252809,1.31778646068495));
#15918=CARTESIAN_POINT('Ctrl Pts',(0.0702395735793815,0.120209316621791,
1.32572862880773));
#15919=CARTESIAN_POINT('Ctrl Pts',(-0.0629590648350173,0.124177428154433,
1.33367079693051));
#15920=CARTESIAN_POINT('Ctrl Pts',(-0.115917830154768,0.0471875384414626,
1.33924015781913));
#15921=CARTESIAN_POINT('Ctrl Pts',(-0.117945510062545,0.00411888419242175,
1.3421621293335));
#15922=CARTESIAN_POINT('Ctrl Pts',(-0.117917347702326,6.89762296073276E-5,
1.34243671147361));
#15923=CARTESIAN_POINT('Origin',(0.,0.,-0.0924367114736175));
#15924=CARTESIAN_POINT('',(-0.11774949833287,0.000107383800510985,1.23256328852638));
#15925=CARTESIAN_POINT('',(-0.117581795058195,-8.20683476789735E-6,1.24243671147361));
#15926=CARTESIAN_POINT('',(-0.117775,2.85464118895969E-14,-0.0924367114736175));
#15927=CARTESIAN_POINT('Ctrl Pts',(-0.11774949833287,0.000107383800510997,
1.23256328852638));
#15928=CARTESIAN_POINT('Ctrl Pts',(-0.1174869159147,-0.0291008736543001,
1.23453632015749));
#15929=CARTESIAN_POINT('Ctrl Pts',(-0.0917482398636095,-0.0978979247776974,
1.23915568166769));
#15930=CARTESIAN_POINT('Ctrl Pts',(0.0236422145726536,-0.137184880695923,
1.246421373057));
#15931=CARTESIAN_POINT('Ctrl Pts',(0.128082862902196,-0.0545291301253663,
1.2543603626943));
#15932=CARTESIAN_POINT('Ctrl Pts',(0.115272428336817,0.0780443019497631,
1.26229935233161));
#15933=CARTESIAN_POINT('Ctrl Pts',(-0.00306201423577413,0.139173524314926,
1.27023834196891));
#15934=CARTESIAN_POINT('Ctrl Pts',(-0.101358337705897,0.08278581645186,
1.27699298736717));
#15935=CARTESIAN_POINT('Ctrl Pts',(-0.117535345263889,0.02168343817453,
1.28110130288633));
#15936=CARTESIAN_POINT('Ctrl Pts',(-0.117590388001671,-3.33269891444124E-5,
1.28256328852638));
#15937=CARTESIAN_POINT('Ctrl Pts',(-0.117581795058195,-8.20683476789562E-6,
1.24243671147361));
#15938=CARTESIAN_POINT('Ctrl Pts',(-0.117593699448189,-0.0191748937105988,
1.24372679017572));
#15939=CARTESIAN_POINT('Ctrl Pts',(-0.104100832827715,-0.0776580224685839,
1.24766425825208));
#15940=CARTESIAN_POINT('Ctrl Pts',(-0.0120149744006178,-0.138706589206355,
1.25424911570271));
#15941=CARTESIAN_POINT('Ctrl Pts',(0.110059129405696,-0.0852693704304675,
1.26219128382548));
#15942=CARTESIAN_POINT('Ctrl Pts',(0.13130776387206,0.0462833517151888,
1.27013345194827));
#15943=CARTESIAN_POINT('Ctrl Pts',(0.0322649968732001,0.135435768819968,
1.27807562007105));
#15944=CARTESIAN_POINT('Ctrl Pts',(-0.0881142830049797,0.102747609761224,
1.28551003991283));
#15945=CARTESIAN_POINT('Ctrl Pts',(-0.117534109666069,0.0315207854174475,
1.29029707038035));
#15946=CARTESIAN_POINT('Ctrl Pts',(-0.117823716245033,-0.000102811805890825,
1.29243671147362));
#15947=CARTESIAN_POINT('Origin',(0.,0.,-0.0924367114736175));
#15948=CARTESIAN_POINT('',(-0.117957988745754,-3.12301727557783E-5,1.18256328852638));
#15949=CARTESIAN_POINT('',(-0.117793553451004,0.000106755881474893,1.19243671147362));
#15950=CARTESIAN_POINT('',(-0.117775,2.85464118895969E-14,-0.0924367114736175));
#15951=CARTESIAN_POINT('Ctrl Pts',(-0.117957988745754,-3.12301727557569E-5,
1.18256328852638));
#15952=CARTESIAN_POINT('Ctrl Pts',(-0.117964007145535,-0.00173159226684161,
1.18267867767044));
#15953=CARTESIAN_POINT('Ctrl Pts',(-0.117160216762375,-0.0424221720604921,
1.1854403966936));
#15954=CARTESIAN_POINT('Ctrl Pts',(-0.0703321751825429,-0.12013338809653,
1.19084844559586));
#15955=CARTESIAN_POINT('Ctrl Pts',(0.0627954496153871,-0.124239193932754,
1.19878743523316));
#15956=CARTESIAN_POINT('Ctrl Pts',(0.138438143943654,-0.0146125323915816,
1.20672642487047));
#15957=CARTESIAN_POINT('Ctrl Pts',(0.0873502052771435,0.108390901091839,
1.21466541450777));
#15958=CARTESIAN_POINT('Ctrl Pts',(-0.043700859820065,0.132169893139269,
1.22260440414508));
#15959=CARTESIAN_POINT('Ctrl Pts',(-0.112119660921406,0.0591163174148552,
1.22857036215128));
#15960=CARTESIAN_POINT('Ctrl Pts',(-0.117839104743291,0.0100747194789664,
1.23188999027838));
#15961=CARTESIAN_POINT('Ctrl Pts',(-0.11774949833287,0.000107383800510997,
1.23256328852638));
#15962=CARTESIAN_POINT('Ctrl Pts',(-0.117793553451004,0.000106755881474891,
1.19243671147362));
#15963=CARTESIAN_POINT('Ctrl Pts',(-0.117510050331475,-0.0305433296418112,
1.19450912059683));
#15964=CARTESIAN_POINT('Ctrl Pts',(-0.0896091397727994,-0.100804620014092,
1.19922891909429));
#15965=CARTESIAN_POINT('Ctrl Pts',(0.0288222657999454,-0.136209964735594,
1.20659610696603));
#15966=CARTESIAN_POINT('Ctrl Pts',(0.130092623711363,-0.0495962373069701,
1.21453827508881));
#15967=CARTESIAN_POINT('Ctrl Pts',(0.112184773380136,0.082452738709893,
1.22248044321158));
#15968=CARTESIAN_POINT('Ctrl Pts',(-0.00849585454694533,0.138966535376798,
1.23042261133437));
#15969=CARTESIAN_POINT('Ctrl Pts',(-0.103054997843392,0.079672038485689,
1.23707470075504));
#15970=CARTESIAN_POINT('Ctrl Pts',(-0.11756927027536,0.0201573447738481,
1.24107940080146));
#15971=CARTESIAN_POINT('Ctrl Pts',(-0.117581795058195,-8.20683476789562E-6,
1.24243671147361));
#15972=CARTESIAN_POINT('Origin',(0.,0.,-0.0924367114736175));
#15973=CARTESIAN_POINT('',(-0.117657565919426,-8.78585414499747E-5,1.13256328852638));
#15974=CARTESIAN_POINT('',(-0.117937823388479,-5.4172489969917E-5,1.14243671147362));
#15975=CARTESIAN_POINT('',(-0.117775,2.85464118895969E-14,-0.0924367114736175));
#15976=CARTESIAN_POINT('Ctrl Pts',(-0.117657565919426,-8.78585414499974E-5,
1.13256328852638));
#15977=CARTESIAN_POINT('Ctrl Pts',(-0.11775046973706,-0.0134980674796043,
1.13346736506249));
#15978=CARTESIAN_POINT('Ctrl Pts',(-0.109441032251172,-0.0660497484721492,
1.13701777147771));
#15979=CARTESIAN_POINT('Ctrl Pts',(-0.0320511128216771,-0.13546723577438,
1.14321450777202));
#15980=CARTESIAN_POINT('Ctrl Pts',(0.0964380908528195,-0.100390938007982,
1.15115349740933));
#15981=CARTESIAN_POINT('Ctrl Pts',(0.136644831685568,0.0265863832644056,
1.15909248704664));
#15982=CARTESIAN_POINT('Ctrl Pts',(0.0517625939920979,0.129225692742072,
1.16703147668394));
#15983=CARTESIAN_POINT('Ctrl Pts',(-0.0785823129332351,0.113795317289389,
1.17485507717719));
#15984=CARTESIAN_POINT('Ctrl Pts',(-0.117825981412732,0.0372644419932696,
1.18003234779134));
#15985=CARTESIAN_POINT('Ctrl Pts',(-0.117957988745754,-3.12301727557569E-5,
1.18256328852638));
#15986=CARTESIAN_POINT('Ctrl Pts',(-0.117937823388479,-5.41724899699178E-5,
1.14243671147362));
#15987=CARTESIAN_POINT('Ctrl Pts',(-0.117955293269658,-0.0031110520517566,
1.14264406164367));
#15988=CARTESIAN_POINT('Ctrl Pts',(-0.116460933142332,-0.0451799670343263,
1.14549880118799));
#15989=CARTESIAN_POINT('Ctrl Pts',(-0.0660858892268601,-0.122541963197144,
1.15100093010657));
#15990=CARTESIAN_POINT('Ctrl Pts',(0.0671705316110708,-0.121950798202395,
1.15894309822935));
#15991=CARTESIAN_POINT('Ctrl Pts',(0.138891844802359,-0.00964017357273747,
1.16688526635212));
#15992=CARTESIAN_POINT('Ctrl Pts',(0.0833739592533277,0.111501840422208,
1.17482743447491));
#15993=CARTESIAN_POINT('Ctrl Pts',(-0.0485230383040216,0.130496713571114,
1.18276960259768));
#15994=CARTESIAN_POINT('Ctrl Pts',(-0.113150295826959,0.0561813708375219,
1.18863936159726));
#15995=CARTESIAN_POINT('Ctrl Pts',(-0.117872210070015,0.00861047923971886,
1.19186173122257));
#15996=CARTESIAN_POINT('Ctrl Pts',(-0.117793553451004,0.000106755881474891,
1.19243671147362));
#15997=CARTESIAN_POINT('Origin',(0.,0.,-0.0924367114736175));
#15998=CARTESIAN_POINT('',(-0.117641451221435,8.0229283111194E-5,1.08256328852638));
#15999=CARTESIAN_POINT('',(-0.117630591849015,-7.42484764288953E-5,1.09243671147362));
#16000=CARTESIAN_POINT('',(-0.117775,2.85464118895969E-14,-0.0924367114736175));
#16001=CARTESIAN_POINT('Ctrl Pts',(-0.117641451221435,8.02292831111745E-5,
1.08256328852638));
#16002=CARTESIAN_POINT('Ctrl Pts',(-0.117483998834985,-0.0250372639622414,
1.08425605245455));
#16003=CARTESIAN_POINT('Ctrl Pts',(-0.0972946570053161,-0.0896524615425008,
1.08859514626182));
#16004=CARTESIAN_POINT('Ctrl Pts',(0.00904258428980543,-0.13891320121148,
1.09558056994819));
#16005=CARTESIAN_POINT('Ctrl Pts',(0.121617839487272,-0.067732908692211,
1.1035195595855));
#16006=CARTESIAN_POINT('Ctrl Pts',(0.122860297649024,0.0654522196953821,
1.1114585492228));
#16007=CARTESIAN_POINT('Ctrl Pts',(0.0116325734791967,0.138720326685422,
1.11939753886011));
#16008=CARTESIAN_POINT('Ctrl Pts',(-0.096364912740844,0.0911171059582243,
1.1264324519613));
#16009=CARTESIAN_POINT('Ctrl Pts',(-0.117478530206868,0.0257550656131636,
1.13082103518339));
#16010=CARTESIAN_POINT('Ctrl Pts',(-0.117657565919426,-8.78585414499974E-5,
1.13256328852638));
#16011=CARTESIAN_POINT('Ctrl Pts',(-0.117630591849015,-7.42484764288814E-5,
1.09243671147362));
#16012=CARTESIAN_POINT('Ctrl Pts',(-0.117715241483118,-0.0147626739157663,
1.09342639206478));
#16013=CARTESIAN_POINT('Ctrl Pts',(-0.108350501834675,-0.0686384992808382,
1.0970634620302));
#16014=CARTESIAN_POINT('Ctrl Pts',(-0.0276126195379174,-0.136460326620484,
1.10334792136989));
#16015=CARTESIAN_POINT('Ctrl Pts',(0.0997182217817603,-0.0971604536002107,
1.11129008949267));
#16016=CARTESIAN_POINT('Ctrl Pts',(0.135696927507188,0.0311483765905046,
1.11923225761545));
#16017=CARTESIAN_POINT('Ctrl Pts',(0.0473633069609982,0.130922093830007,
1.12717442573822));
#16018=CARTESIAN_POINT('Ctrl Pts',(-0.0809210029008042,0.111284164335459,
1.13490924369095));
#16019=CARTESIAN_POINT('Ctrl Pts',(-0.117732242679493,0.0359183370635313,
1.13999667226941));
#16020=CARTESIAN_POINT('Ctrl Pts',(-0.117937823388479,-5.41724899699178E-5,
1.14243671147362));
#16021=CARTESIAN_POINT('Origin',(0.,0.,-0.0924367114736175));
#16022=CARTESIAN_POINT('',(-0.117948158721073,4.38502512853227E-5,1.03256328852638));
#16023=CARTESIAN_POINT('',(-0.117667547954054,9.20194976846214E-5,1.04243671147362));
#16024=CARTESIAN_POINT('',(-0.117775,2.85464118895969E-14,-0.0924367114736175));
#16025=CARTESIAN_POINT('Ctrl Pts',(-0.117948158721073,4.38502512853157E-5,
1.03256328852638));
#16026=CARTESIAN_POINT('Ctrl Pts',(-0.117773439871091,-0.0365306738650768,
1.03504473984661));
#16027=CARTESIAN_POINT('Ctrl Pts',(-0.0798690478914953,-0.112422454385097,
1.04017252104593));
#16028=CARTESIAN_POINT('Ctrl Pts',(0.0493427524230464,-0.130168884856471,
1.04794663212436));
#16029=CARTESIAN_POINT('Ctrl Pts',(0.136125055048066,-0.0291310004912345,
1.05588562176166));
#16030=CARTESIAN_POINT('Ctrl Pts',(0.0982941990358779,0.0985743183458784,
1.06382461139897));
#16031=CARTESIAN_POINT('Ctrl Pts',(-0.0295182596522469,0.136041604476578,
1.07176360103627));
#16032=CARTESIAN_POINT('Ctrl Pts',(-0.108818061611988,0.067537217334308,
1.07800982674541));
#16033=CARTESIAN_POINT('Ctrl Pts',(-0.11773014713001,0.0142293884972668,
1.08160972257545));
#16034=CARTESIAN_POINT('Ctrl Pts',(-0.117641451221435,8.02292831111745E-5,
1.08256328852638));
#16035=CARTESIAN_POINT('Ctrl Pts',(-0.117667547954054,9.20194976846197E-5,
1.04243671147362));
#16036=CARTESIAN_POINT('Ctrl Pts',(-0.117475882803567,-0.0261866690710452,
1.04420872248589));
#16037=CARTESIAN_POINT('Ctrl Pts',(-0.0957916308421219,-0.0920126959480487,
1.04862812287242));
#16038=CARTESIAN_POINT('Ctrl Pts',(0.0132451643780021,-0.13859452774087,
1.05569491263321));
#16039=CARTESIAN_POINT('Ctrl Pts',(0.123654649330263,-0.0639797248987874,
1.06363708075599));
#16040=CARTESIAN_POINT('Ctrl Pts',(0.120783771971213,0.0692470788374567,
1.07157924887876));
#16041=CARTESIAN_POINT('Ctrl Pts',(0.00726255089817806,0.139036444335888,
1.07952141700155));
#16042=CARTESIAN_POINT('Ctrl Pts',(-0.0979368667310299,0.0886295245336828,
1.08647390453316));
#16043=CARTESIAN_POINT('Ctrl Pts',(-0.117488804242801,0.0245287720112504,
1.09077900269052));
#16044=CARTESIAN_POINT('Ctrl Pts',(-0.117630591849015,-7.42484764288814E-5,
1.09243671147362));
#16045=CARTESIAN_POINT('Origin',(0.,0.,-0.0924367114736175));
#16046=CARTESIAN_POINT('',(-0.117771476475648,-0.000107683352847938,0.982563288526384));
#16047=CARTESIAN_POINT('',(-0.11796176292438,2.53781033017321E-5,0.992436711473616));
#16048=CARTESIAN_POINT('',(-0.117775,2.85464118895969E-14,-0.0924367114736175));
#16049=CARTESIAN_POINT('Ctrl Pts',(-0.117771476475648,-0.000107683352847945,
0.982563288526384));
#16050=CARTESIAN_POINT('Ctrl Pts',(-0.117856103358663,-0.00933799346614349,
0.983187097359559));
#16051=CARTESIAN_POINT('Ctrl Pts',(-0.112646870919438,-0.057630810124202,
0.986457236071836));
#16052=CARTESIAN_POINT('Ctrl Pts',(-0.0461590140787468,-0.131331607851033,
0.992373704663214));
#16053=CARTESIAN_POINT('Ctrl Pts',(0.0853128637208732,-0.110001641284132,
1.00031269430052));
#16054=CARTESIAN_POINT('Ctrl Pts',(0.138686661656432,0.0120272889735618,
1.00825168393783));
#16055=CARTESIAN_POINT('Ctrl Pts',(0.0651023256631918,0.123046060459907,
1.01619067357513));
#16056=CARTESIAN_POINT('Ctrl Pts',(-0.0680787277209358,0.121424596492465,
1.02412966321244));
#16057=CARTESIAN_POINT('Ctrl Pts',(-0.116790117880403,0.0438975063746073,
1.02958720152952));
#16058=CARTESIAN_POINT('Ctrl Pts',(-0.11795976781127,0.00247402277930658,
1.0323984099675));
#16059=CARTESIAN_POINT('Ctrl Pts',(-0.117948158721073,4.38502512853157E-5,
1.03256328852638));
#16060=CARTESIAN_POINT('Ctrl Pts',(-0.11796176292438,2.53781033017319E-5,
0.992436711473616));
#16061=CARTESIAN_POINT('Ctrl Pts',(-0.117851518882229,-0.0376119105440478,
0.994991052906992));
#16062=CARTESIAN_POINT('Ctrl Pts',(-0.077958511321084,-0.114458475672252,
1.00019278371463));
#16063=CARTESIAN_POINT('Ctrl Pts',(0.0529591494285269,-0.128760265574912,
1.00804190389653));
#16064=CARTESIAN_POINT('Ctrl Pts',(0.136912761112491,-0.0252739657289669,
1.0159840720193));
#16065=CARTESIAN_POINT('Ctrl Pts',(0.0954402180350474,0.101365883217864,
1.02392624014209));
#16066=CARTESIAN_POINT('Ctrl Pts',(-0.0334653697086341,0.135144169424284,
1.03186840826486));
#16067=CARTESIAN_POINT('Ctrl Pts',(-0.109792739119276,0.0652029671457737,
1.03803856537538));
#16068=CARTESIAN_POINT('Ctrl Pts',(-0.117762231070763,0.0130737646421874,
1.04156133311163));
#16069=CARTESIAN_POINT('Ctrl Pts',(-0.117667547954054,9.20194976846197E-5,
1.04243671147362));
#16070=CARTESIAN_POINT('Origin',(0.,0.,-0.0924367114736175));
#16071=CARTESIAN_POINT('',(-0.117585265278523,2.16484251076657E-5,0.932563288526384));
#16072=CARTESIAN_POINT('',(-0.117742563953077,-0.000107211314308964,0.942436711473616));
#16073=CARTESIAN_POINT('',(-0.117775,2.85464118895969E-14,-0.0924367114736175));
#16074=CARTESIAN_POINT('Ctrl Pts',(-0.117585265278523,2.16484251076635E-5,
0.932563288526384));
#16075=CARTESIAN_POINT('Ctrl Pts',(-0.117550805757046,-0.0209622679161363,
0.933975784751614));
#16076=CARTESIAN_POINT('Ctrl Pts',(-0.102172791552808,-0.0813069697478888,
0.938034610855947));
#16077=CARTESIAN_POINT('Ctrl Pts',(-0.00565790085648466,-0.139092177922979,
0.944739766839381));
#16078=CARTESIAN_POINT('Ctrl Pts',(0.113796373024222,-0.0801812402497705,
0.952678756476687));
#16079=CARTESIAN_POINT('Ctrl Pts',(0.129077866376032,0.0521301276928276,
0.960617746113992));
#16080=CARTESIAN_POINT('Ctrl Pts',(0.026197419344502,0.13671993644362,0.968556735751298));
#16081=CARTESIAN_POINT('Ctrl Pts',(-0.0906967139502387,0.0993396518733501,
0.975871916555428));
#16082=CARTESIAN_POINT('Ctrl Pts',(-0.117497098103867,0.02981894716558,
0.980540767480457));
#16083=CARTESIAN_POINT('Ctrl Pts',(-0.117771476475648,-0.000107683352847945,
0.982563288526384));
#16084=CARTESIAN_POINT('Ctrl Pts',(-0.117742563953077,-0.000107211314308957,
0.942436711473616));
#16085=CARTESIAN_POINT('Ctrl Pts',(-0.117833632602859,-0.0103126986533654,
0.943125993953839));
#16086=CARTESIAN_POINT('Ctrl Pts',(-0.111944766202914,-0.0596118697348184,
0.946462665808322));
#16087=CARTESIAN_POINT('Ctrl Pts',(-0.0428565117498991,-0.132465832952297,
0.952446727037066));
#16088=CARTESIAN_POINT('Ctrl Pts',(0.0880997963686447,-0.107806787258123,
0.960388895159846));
#16089=CARTESIAN_POINT('Ctrl Pts',(0.138347640177547,0.0156143509765511,
0.968331063282625));
#16090=CARTESIAN_POINT('Ctrl Pts',(0.061854832590724,0.124731139593481,
0.976273231405407));
#16091=CARTESIAN_POINT('Ctrl Pts',(-0.0713033562375951,0.119581390225944,
0.984215399528185));
#16092=CARTESIAN_POINT('Ctrl Pts',(-0.117322772537986,0.0417718924351975,
0.989603226217589));
#16093=CARTESIAN_POINT('Ctrl Pts',(-0.11796577882491,0.00139640554830399,
0.992343663532733));
#16094=CARTESIAN_POINT('Ctrl Pts',(-0.11796176292438,2.53781033017319E-5,
0.992436711473616));
#16095=CARTESIAN_POINT('Origin',(0.,0.,-0.0924367114736175));
#16096=CARTESIAN_POINT('',(-0.117850913371472,9.6525574830472E-5,0.882563288526384));
#16097=CARTESIAN_POINT('',(-0.117591231449503,3.54948526558943E-5,0.892436711473616));
#16098=CARTESIAN_POINT('',(-0.117775,2.85464118895969E-14,-0.0924367114736175));
#16099=CARTESIAN_POINT('Ctrl Pts',(-0.117850913371472,9.65255748304767E-5,
0.882563288526384));
#16100=CARTESIAN_POINT('Ctrl Pts',(-0.117563006813672,-0.0324172738354332,
0.884764472143669));
#16101=CARTESIAN_POINT('Ctrl Pts',(-0.0867151192651892,-0.104499852648429,
0.889611985640057));
#16102=CARTESIAN_POINT('Ctrl Pts',(0.0353397195745277,-0.134646760160997,
0.897105829015547));
#16103=CARTESIAN_POINT('Ctrl Pts',(0.132293719443212,-0.0433245611326863,
0.905044818652852));
#16104=CARTESIAN_POINT('Ctrl Pts',(0.108141885842356,0.0876583043865096,
0.912983808290157));
#16105=CARTESIAN_POINT('Ctrl Pts',(-0.0150064327997127,0.138395999855801,
0.920922797927463));
#16106=CARTESIAN_POINT('Ctrl Pts',(-0.104951114476159,0.0759553573435841,
0.927449291339539));
#16107=CARTESIAN_POINT('Ctrl Pts',(-0.117615366114572,0.01835136974357,
0.931329454872513));
#16108=CARTESIAN_POINT('Ctrl Pts',(-0.117585265278523,2.16484251076635E-5,
0.932563288526384));
#16109=CARTESIAN_POINT('Ctrl Pts',(-0.117591231449503,3.54948526559117E-5,
0.892436711473616));
#16110=CARTESIAN_POINT('Ctrl Pts',(-0.117532234588281,-0.0218238662162972,
0.893908324374946));
#16111=CARTESIAN_POINT('Ctrl Pts',(-0.101194437785642,-0.0830895288483654,
0.898027326650536));
#16112=CARTESIAN_POINT('Ctrl Pts',(-0.00250162451743248,-0.139203517821528,
0.904793718300386));
#16113=CARTESIAN_POINT('Ctrl Pts',(0.115632500949424,-0.0775435504945224,
0.912735886423165));
#16114=CARTESIAN_POINT('Ctrl Pts',(0.127835376168433,0.0551542754370876,
0.920678054545947));
#16115=CARTESIAN_POINT('Ctrl Pts',(0.0229279137899797,0.137325118854324,
0.928620222668725));
#16116=CARTESIAN_POINT('Ctrl Pts',(-0.0920562790907298,0.0974788594069619,
0.935873108311283));
#16117=CARTESIAN_POINT('Ctrl Pts',(-0.117483857027998,0.0288844367965532,
0.94047860457958));
#16118=CARTESIAN_POINT('Ctrl Pts',(-0.117742563953077,-0.000107211314308957,
0.942436711473616));
#16119=CARTESIAN_POINT('Origin',(0.,0.,-0.0924367114736175));
#16120=CARTESIAN_POINT('',(-0.11789232318732,-8.18790992476613E-5,0.832563288526384));
#16121=CARTESIAN_POINT('',(-0.117872825429845,8.99519344067963E-5,0.842436711473616));
#16122=CARTESIAN_POINT('',(-0.117775,2.85464118895969E-14,-0.0924367114736175));
#16123=CARTESIAN_POINT('Ctrl Pts',(-0.11789232318732,-8.18790992476734E-5,
0.832563288526384));
#16124=CARTESIAN_POINT('Ctrl Pts',(-0.117932494517479,-0.00515170743829337,
0.832906829656623));
#16125=CARTESIAN_POINT('Ctrl Pts',(-0.115332713682068,-0.0492334187378749,
0.835896700665964));
#16126=CARTESIAN_POINT('Ctrl Pts',(-0.059752088941783,-0.125731196083361,
0.841532901554406));
#16127=CARTESIAN_POINT('Ctrl Pts',(0.0732361146625898,-0.118385460722959,
0.849471891191712));
#16128=CARTESIAN_POINT('Ctrl Pts',(0.139181674492094,-0.00266594955618734,
0.857410880829018));
#16129=CARTESIAN_POINT('Ctrl Pts',(0.077715950067195,0.115494055719818,
0.865349870466323));
#16130=CARTESIAN_POINT('Ctrl Pts',(-0.0548934004223171,0.127927168308903,
0.87328886010363));
#16131=CARTESIAN_POINT('Ctrl Pts',(-0.114416768398411,0.0522742940766184,
0.879026666123649));
#16132=CARTESIAN_POINT('Ctrl Pts',(-0.117909136832228,0.0066718045071592,
0.882118142264567));
#16133=CARTESIAN_POINT('Ctrl Pts',(-0.117850913371472,9.65255748304767E-5,
0.882563288526384));
#16134=CARTESIAN_POINT('Ctrl Pts',(-0.117872825429845,8.99519344067998E-5,
0.842436711473616));
#16135=CARTESIAN_POINT('Ctrl Pts',(-0.117591169542271,-0.0331870933343037,
0.844690654796053));
#16136=CARTESIAN_POINT('Ctrl Pts',(-0.0854771005934613,-0.106025606004136,
0.84959198749275));
#16137=CARTESIAN_POINT('Ctrl Pts',(0.0380692928980519,-0.133920149482284,
0.857140709563706));
#16138=CARTESIAN_POINT('Ctrl Pts',(0.133179650076608,-0.0405839661022353,
0.865082877686486));
#16139=CARTESIAN_POINT('Ctrl Pts',(0.106283765719693,0.0899312995767124,
0.873025045809266));
#16140=CARTESIAN_POINT('Ctrl Pts',(-0.0179789669825735,0.138060255849953,
0.880967213932046));
#16141=CARTESIAN_POINT('Ctrl Pts',(-0.105798194743126,0.0742290978659706,
0.887437769153496));
#16142=CARTESIAN_POINT('Ctrl Pts',(-0.117638368248411,0.0175004969839459,
0.891260935000686));
#16143=CARTESIAN_POINT('Ctrl Pts',(-0.117591231449503,3.54948526559117E-5,
0.892436711473616));
#16144=CARTESIAN_POINT('Origin',(0.,0.,-0.0924367114736175));
#16145=CARTESIAN_POINT('',(-0.117598114366551,-4.51832715892789E-5,0.782563288526384));
#16146=CARTESIAN_POINT('',(-0.117874685330111,-8.92836445515327E-5,0.792436711473617));
#16147=CARTESIAN_POINT('',(-0.117775,2.85464118895969E-14,-0.0924367114736175));
#16148=CARTESIAN_POINT('Ctrl Pts',(-0.117598114366551,-4.518327158929E-5,
0.782563288526384));
#16149=CARTESIAN_POINT('Ctrl Pts',(-0.117656123976761,-0.0168608793038394,
0.783695517048678));
#16150=CARTESIAN_POINT('Ctrl Pts',(-0.106420815930739,-0.0729055463807818,
0.787474075450074));
#16151=CARTESIAN_POINT('Ctrl Pts',(-0.0202952816069424,-0.137719814645367,
0.793898963730571));
#16152=CARTESIAN_POINT('Ctrl Pts',(0.104705698854998,-0.0917352845351548,
0.801837953367879));
#16153=CARTESIAN_POINT('Ctrl Pts',(0.133855787965376,0.0382266115373486,
0.809776943005182));
#16154=CARTESIAN_POINT('Ctrl Pts',(0.0404700769297216,0.133194664588195,
0.81771593264249));
#16155=CARTESIAN_POINT('Ctrl Pts',(-0.0843190215395119,0.107398870964955,
0.825311381149555));
#16156=CARTESIAN_POINT('Ctrl Pts',(-0.117623050954756,0.0339016606582783,
0.830260499777521));
#16157=CARTESIAN_POINT('Ctrl Pts',(-0.11789232318732,-8.18790992476734E-5,
0.832563288526384));
#16158=CARTESIAN_POINT('Ctrl Pts',(-0.117874685330111,-8.9283644551537E-5,
0.792436711473617));
#16159=CARTESIAN_POINT('Ctrl Pts',(-0.11792303416021,-0.00583050672374999,
0.7928255958429));
#16160=CARTESIAN_POINT('Ctrl Pts',(-0.114931453360353,-0.0506053896743902,
0.795861869586443));
#16161=CARTESIAN_POINT('Ctrl Pts',(-0.0575513573065257,-0.126774282767806,
0.801545532704245));
#16162=CARTESIAN_POINT('Ctrl Pts',(0.0753527000357912,-0.117071978271622,
0.809487700827026));
#16163=CARTESIAN_POINT('Ctrl Pts',(0.139225942868322,-0.000119714417332432,
0.817429868949805));
#16164=CARTESIAN_POINT('Ctrl Pts',(0.0755539188089132,0.116942220141962,
0.825372037072586));
#16165=CARTESIAN_POINT('Ctrl Pts',(-0.0573332568284509,0.12687306712048,
0.833314205195366));
#16166=CARTESIAN_POINT('Ctrl Pts',(-0.114890414736801,0.0507419104293215,
0.839002429995709));
#16167=CARTESIAN_POINT('Ctrl Pts',(-0.117921990994851,0.00589875908008548,
0.842043265421793));
#16168=CARTESIAN_POINT('Ctrl Pts',(-0.117872825429845,8.99519344067998E-5,
0.842436711473616));
#16169=CARTESIAN_POINT('Origin',(0.,0.,-0.0924367114736175));
#16170=CARTESIAN_POINT('',(-0.11772691567491,0.000105512987197037,0.732563288526384));
#16171=CARTESIAN_POINT('',(-0.117591850253004,-3.65476421498312E-5,0.742436711473616));
#16172=CARTESIAN_POINT('',(-0.117775,2.85464118895969E-14,-0.0924367114736175));
#16173=CARTESIAN_POINT('Ctrl Pts',(-0.11772691567491,0.000105512987197042,
0.732563288526384));
#16174=CARTESIAN_POINT('Ctrl Pts',(-0.117479624464894,-0.0283451130369189,
0.734484204440733));
#16175=CARTESIAN_POINT('Ctrl Pts',(-0.0928318426870313,-0.096374559506161,
0.739051450234184));
#16176=CARTESIAN_POINT('Ctrl Pts',(0.0209425314183671,-0.137622876656644,
0.746265025906738));
#16177=CARTESIAN_POINT('Ctrl Pts',(0.126986869252672,-0.0570349089493802,
0.754204015544043));
#16178=CARTESIAN_POINT('Ctrl Pts',(0.11678343126468,0.0757646090434518,
0.762143005181349));
#16179=CARTESIAN_POINT('Ctrl Pts',(-0.000327234354877375,0.139206819944772,
0.770081994818654));
#16180=CARTESIAN_POINT('Ctrl Pts',(-0.100479183608201,0.0843410365921374,
0.776888755933667));
#16181=CARTESIAN_POINT('Ctrl Pts',(-0.117520539541507,0.0224420334666934,
0.781049187169576));
#16182=CARTESIAN_POINT('Ctrl Pts',(-0.117598114366551,-4.518327158929E-5,
0.782563288526384));
#16183=CARTESIAN_POINT('Ctrl Pts',(-0.117591850253004,-3.65476421498364E-5,
0.742436711473616));
#16184=CARTESIAN_POINT('Ctrl Pts',(-0.117640211257931,-0.0174335619022046,
0.743607926264006));
#16185=CARTESIAN_POINT('Ctrl Pts',(-0.105863856762799,-0.0740921523660566,
0.747426530428656));
#16186=CARTESIAN_POINT('Ctrl Pts',(-0.0182163644075178,-0.138029133036789,
0.753892523967566));
#16187=CARTESIAN_POINT('Ctrl Pts',(0.106128952536144,-0.0901139441634624,
0.761834692090347));
#16188=CARTESIAN_POINT('Ctrl Pts',(0.133249245915149,0.0403548753208232,
0.769776860213125));
#16189=CARTESIAN_POINT('Ctrl Pts',(0.0382995408207276,0.133854483197375,
0.777719028335907));
#16190=CARTESIAN_POINT('Ctrl Pts',(-0.0853693283863186,0.106155717082476,
0.785272312089402));
#16191=CARTESIAN_POINT('Ctrl Pts',(-0.117593892160246,0.0332537408718532,
0.79017820646864));
#16192=CARTESIAN_POINT('Ctrl Pts',(-0.117874685330111,-8.9283644551537E-5,
0.792436711473617));
#16193=CARTESIAN_POINT('Origin',(0.,0.,-0.0924367114736175));
#16194=CARTESIAN_POINT('',(-0.117964947617991,-1.73329198795185E-5,0.682563288526384));
#16195=CARTESIAN_POINT('',(-0.117740574064672,0.000107068518266168,0.692436711473616));
#16196=CARTESIAN_POINT('',(-0.117775,2.85464118895969E-14,-0.0924367114736175));
#16197=CARTESIAN_POINT('Ctrl Pts',(-0.117964947617991,-1.73329198795367E-5,
0.682563288526384));
#16198=CARTESIAN_POINT('Ctrl Pts',(-0.117966864156947,-0.000949576032666658,
0.682626561953687));
#16199=CARTESIAN_POINT('Ctrl Pts',(-0.117534558560489,-0.0408698671952461,
0.685336165260092));
#16200=CARTESIAN_POINT('Ctrl Pts',(-0.0726787294560835,-0.118728463672822,
0.690692098445597));
#16201=CARTESIAN_POINT('Ctrl Pts',(0.0603425395611779,-0.125448888878168,
0.698631088082904));
#16202=CARTESIAN_POINT('Ctrl Pts',(0.138124349154501,-0.0173294538893964,
0.706570077720209));
#16203=CARTESIAN_POINT('Ctrl Pts',(0.0894627833767505,0.106653908470079,
0.714509067357515));
#16204=CARTESIAN_POINT('Ctrl Pts',(-0.0410958292974484,0.133002927094911,
0.72244805699482));
#16205=CARTESIAN_POINT('Ctrl Pts',(-0.111546724107196,0.0606813038481789,
0.728466130717777));
#16206=CARTESIAN_POINT('Ctrl Pts',(-0.117820302634623,0.0108495967181263,
0.731837874561632));
#16207=CARTESIAN_POINT('Ctrl Pts',(-0.11772691567491,0.000105512987197042,
0.732563288526384));
#16208=CARTESIAN_POINT('Ctrl Pts',(-0.117740574064672,0.000107068518266165,
0.692436711473616));
#16209=CARTESIAN_POINT('Ctrl Pts',(-0.117483171888848,-0.0288182833237499,
0.694390256685113));
#16210=CARTESIAN_POINT('Ctrl Pts',(-0.0921515028359353,-0.0973455904149804,
0.698991191270869));
#16211=CARTESIAN_POINT('Ctrl Pts',(0.022691720100341,-0.137364345221032,
0.706239515230886));
#16212=CARTESIAN_POINT('Ctrl Pts',(0.127740337615313,-0.0553740340325759,
0.714181683353665));
#16213=CARTESIAN_POINT('Ctrl Pts',(0.115765682611161,0.077344581120379,
0.722123851476446));
#16214=CARTESIAN_POINT('Ctrl Pts',(-0.00226223072526165,0.139207614056346,
0.730066019599226));
#16215=CARTESIAN_POINT('Ctrl Pts',(-0.101117998472899,0.083225715609228,
0.736836972931616));
#16216=CARTESIAN_POINT('Ctrl Pts',(-0.117530897055598,0.0218902846491045,
0.740960536889746));
#16217=CARTESIAN_POINT('Ctrl Pts',(-0.117591850253004,-3.65476421498364E-5,
0.742436711473616));
#16218=CARTESIAN_POINT('Origin',(0.,0.,-0.0924367114736175));
#16219=CARTESIAN_POINT('',(-0.117676160015555,-9.46906955630148E-5,0.632563288526383));
#16220=CARTESIAN_POINT('',(-0.117962383120995,-2.41598447144192E-5,0.642436711473616));
#16221=CARTESIAN_POINT('',(-0.117775,2.85464118895969E-14,-0.0924367114736175));
#16222=CARTESIAN_POINT('Ctrl Pts',(-0.117676160015555,-9.46906955630045E-5,
0.632563288526383));
#16223=CARTESIAN_POINT('Ctrl Pts',(-0.117771520970562,-0.0127268345011372,
0.633415249345741));
#16224=CARTESIAN_POINT('Ctrl Pts',(-0.110078248258936,-0.064483421762156,
0.636913540044201));
#16225=CARTESIAN_POINT('Ctrl Pts',(-0.0347063025259737,-0.134811417789573,
0.643058160621763));
#16226=CARTESIAN_POINT('Ctrl Pts',(0.0944472082050275,-0.102266175560326,
0.65099715025907));
#16227=CARTESIAN_POINT('Ctrl Pts',(0.137140772714236,0.0238967416356601,
0.658936139896373));
#16228=CARTESIAN_POINT('Ctrl Pts',(0.054291358674537,0.128183829614862,
0.666875129533682));
#16229=CARTESIAN_POINT('Ctrl Pts',(-0.0772016597727435,0.11523146575827,
0.674750845743682));
#16230=CARTESIAN_POINT('Ctrl Pts',(-0.117886707375211,0.0380402955314478,
0.679980232074585));
#16231=CARTESIAN_POINT('Ctrl Pts',(-0.117964947617991,-1.73329198795367E-5,
0.682563288526384));
#16232=CARTESIAN_POINT('Ctrl Pts',(-0.117962383120995,-2.41598447144253E-5,
0.642436711473616));
#16233=CARTESIAN_POINT('Ctrl Pts',(-0.117966033213387,-0.0013279541977536,
0.642525197731959));
#16234=CARTESIAN_POINT('Ctrl Pts',(-0.117355585052125,-0.0416360146359673,
0.645261073364563));
#16235=CARTESIAN_POINT('Ctrl Pts',(-0.0715088964667609,-0.119458592094588,
0.650644338371427));
#16236=CARTESIAN_POINT('Ctrl Pts',(0.0616402393688536,-0.124837327709565,
0.658586506494205));
#16237=CARTESIAN_POINT('Ctrl Pts',(0.138320583400205,-0.0158522461166236,
0.666528674616987));
#16238=CARTESIAN_POINT('Ctrl Pts',(0.0882850628235238,0.107655121482266,
0.674470842739765));
#16239=CARTESIAN_POINT('Ctrl Pts',(-0.0426286451686149,0.132539337972556,
0.682413010862546));
#16240=CARTESIAN_POINT('Ctrl Pts',(-0.111894847147975,0.059748848130285,
0.68840163377383));
#16241=CARTESIAN_POINT('Ctrl Pts',(-0.117831996057943,0.0103805377030848,
0.691742867310853));
#16242=CARTESIAN_POINT('Ctrl Pts',(-0.117740574064672,0.000107068518266165,
0.692436711473616));
#16243=CARTESIAN_POINT('Origin',(0.,0.,-0.0924367114736175));
#16244=CARTESIAN_POINT('',(-0.117626285855324,7.11112359239178E-5,0.582563288526384));
#16245=CARTESIAN_POINT('',(-0.11766919235599,-9.26074537421634E-5,0.592436711473616));
#16246=CARTESIAN_POINT('',(-0.117775,2.85464118895969E-14,-0.0924367114736175));
#16247=CARTESIAN_POINT('Ctrl Pts',(-0.117626285855324,7.11112359239024E-5,
0.582563288526383));
#16248=CARTESIAN_POINT('Ctrl Pts',(-0.117492102008102,-0.0242809575267813,
0.584203936737797));
#16249=CARTESIAN_POINT('Ctrl Pts',(-0.0982512120079041,-0.0881067492982899,
0.588490914828312));
#16250=CARTESIAN_POINT('Ctrl Pts',(0.00631176444456456,-0.139064040754811,
0.595424222797929));
#16251=CARTESIAN_POINT('Ctrl Pts',(0.120263693490807,-0.0701091280034811,
0.603363212435234));
#16252=CARTESIAN_POINT('Ctrl Pts',(0.124122453355413,0.0630258865426945,
0.611302202072541));
#16253=CARTESIAN_POINT('Ctrl Pts',(0.0143556138404206,0.138465021405133,
0.619241191709845));
#16254=CARTESIAN_POINT('Ctrl Pts',(-0.0953630726970595,0.0926558297308384,
0.626328220527794));
#16255=CARTESIAN_POINT('Ctrl Pts',(-0.117475314221613,0.0265106736450616,
0.630768919466639));
#16256=CARTESIAN_POINT('Ctrl Pts',(-0.117676160015555,-9.46906955630045E-5,
0.632563288526383));
#16257=CARTESIAN_POINT('Ctrl Pts',(-0.11766919235599,-9.26074537421669E-5,
0.592436711473616));
#16258=CARTESIAN_POINT('Ctrl Pts',(-0.117764072896019,-0.0130062487266101,
0.593307528153066));
#16259=CARTESIAN_POINT('Ctrl Pts',(-0.109848366281979,-0.0650658641993071,
0.596825734206776));
#16260=CARTESIAN_POINT('Ctrl Pts',(-0.0336977294021144,-0.135086418755761,
0.602991329634746));
#16261=CARTESIAN_POINT('Ctrl Pts',(0.0952657566843092,-0.101529863106778,
0.610933497757526));
#16262=CARTESIAN_POINT('Ctrl Pts',(0.136956022624868,0.025038477707157,
0.618875665880307));
#16263=CARTESIAN_POINT('Ctrl Pts',(0.0531805018142573,0.128669000640787,
0.626817834003085));
#16264=CARTESIAN_POINT('Ctrl Pts',(-0.0778376600742765,0.114584191752874,
0.634671515867523));
#16265=CARTESIAN_POINT('Ctrl Pts',(-0.117856827377429,0.0376798124439797,
0.639877808357699));
#16266=CARTESIAN_POINT('Ctrl Pts',(-0.117962383120995,-2.41598447144253E-5,
0.642436711473616));
#16267=CARTESIAN_POINT('Origin',(0.,0.,-0.0924367114736175));
#16268=CARTESIAN_POINT('',(-0.117934829819181,5.63106208242181E-5,0.532563288526383));
#16269=CARTESIAN_POINT('',(-0.117629301205424,7.34277634442948E-5,0.542436711473615));
#16270=CARTESIAN_POINT('',(-0.117775,2.85464118895969E-14,-0.0924367114736175));
#16271=CARTESIAN_POINT('Ctrl Pts',(-0.117934829819181,5.63106208242166E-5,
0.532563288526383));
#16272=CARTESIAN_POINT('Ctrl Pts',(-0.117723349859012,-0.0357608023914865,
0.534992624129852));
#16273=CARTESIAN_POINT('Ctrl Pts',(-0.0811985738067347,-0.110967619805887,
0.540068289612422));
#16274=CARTESIAN_POINT('Ctrl Pts',(0.0467759446245483,-0.131113145053959,
0.547790284974095));
#16275=CARTESIAN_POINT('Ctrl Pts',(0.135526478334676,-0.031799677225719,
0.555729274611401));
#16276=CARTESIAN_POINT('Ctrl Pts',(0.100211809365564,0.0966242157284558,
0.563668264248707));
#16277=CARTESIAN_POINT('Ctrl Pts',(-0.0268399031138932,0.136595261273209,
0.571607253886012));
#16278=CARTESIAN_POINT('Ctrl Pts',(-0.108142973925314,0.0691035501437442,
0.577905595311905));
#16279=CARTESIAN_POINT('Ctrl Pts',(-0.117708537635025,0.0149983997031143,
0.581557606858695));
#16280=CARTESIAN_POINT('Ctrl Pts',(-0.117626285855324,7.11112359239024E-5,
0.582563288526383));
#16281=CARTESIAN_POINT('Ctrl Pts',(-0.117629301205424,7.34277634442983E-5,
0.542436711473615));
#16282=CARTESIAN_POINT('Ctrl Pts',(-0.11748956090956,-0.0244625652698295,
0.544089858574172));
#16283=CARTESIAN_POINT('Ctrl Pts',(-0.0980201725405651,-0.0884941619373469,
0.548390395048989));
#16284=CARTESIAN_POINT('Ctrl Pts',(0.00702343738442799,-0.139048728244533,
0.555338320898066));
#16285=CARTESIAN_POINT('Ctrl Pts',(0.12066450826877,-0.0694546898587181,
0.563280489020846));
#16286=CARTESIAN_POINT('Ctrl Pts',(0.123764493242992,0.063766979789076,
0.571222657143626));
#16287=CARTESIAN_POINT('Ctrl Pts',(0.0134834875971477,0.13857154491934,
0.579164825266405));
#16288=CARTESIAN_POINT('Ctrl Pts',(-0.0957036897026042,0.092147346049863,
0.586236176709736));
#16289=CARTESIAN_POINT('Ctrl Pts',(-0.117475624432153,0.0262528025703711,
0.590660138778806));
#16290=CARTESIAN_POINT('Ctrl Pts',(-0.11766919235599,-9.26074537421669E-5,
0.592436711473616));
#16291=CARTESIAN_POINT('Origin',(0.,0.,-0.0924367114736175));
#16292=CARTESIAN_POINT('',(-0.117794891956694,-0.000106411733115368,0.482563288526384));
#16293=CARTESIAN_POINT('',(-0.117936566864074,5.52347650140707E-5,0.492436711473616));
#16294=CARTESIAN_POINT('',(-0.117775,2.85464118895969E-14,-0.0924367114736175));
#16295=CARTESIAN_POINT('Ctrl Pts',(-0.117794891956694,-0.000106411733115381,
0.482563288526384));
#16296=CARTESIAN_POINT('Ctrl Pts',(-0.117872998614688,-0.00856127641466401,
0.483134981642805));
#16297=CARTESIAN_POINT('Ctrl Pts',(-0.113184542395844,-0.0560672187853419,
0.486353004638329));
#16298=CARTESIAN_POINT('Ctrl Pts',(-0.0487302328423073,-0.130399425645183,
0.492217357512954));
#16299=CARTESIAN_POINT('Ctrl Pts',(0.0831353173341669,-0.111656458896056,
0.50015634715026));
#16300=CARTESIAN_POINT('Ctrl Pts',(0.13889618212661,0.00930034365552528,
0.508095336787567));
#16301=CARTESIAN_POINT('Ctrl Pts',(0.0675071113591811,0.12174331898465,
0.516034326424871));
#16302=CARTESIAN_POINT('Ctrl Pts',(-0.0656800932930844,0.122738629397884,
0.523973316062178));
#16303=CARTESIAN_POINT('Ctrl Pts',(-0.116384786286051,0.04545243224792,
0.529482970096015));
#16304=CARTESIAN_POINT('Ctrl Pts',(-0.117953719733239,0.00325558390455253,
0.53234629425075));
#16305=CARTESIAN_POINT('Ctrl Pts',(-0.117934829819181,5.63106208242166E-5,
0.532563288526383));
#16306=CARTESIAN_POINT('Ctrl Pts',(-0.117936566864074,5.52347650140663E-5,
0.492436711473616));
#16307=CARTESIAN_POINT('Ctrl Pts',(-0.117728017843002,-0.0358510361847084,
0.494872188995279));
#16308=CARTESIAN_POINT('Ctrl Pts',(-0.0810366231971402,-0.111156550628637,
0.499955055891203));
#16309=CARTESIAN_POINT('Ctrl Pts',(0.0471380885036503,-0.131003351527116,
0.507685312161385));
#16310=CARTESIAN_POINT('Ctrl Pts',(0.135643160584381,-0.031381690295376,
0.515627480284167));
#16311=CARTESIAN_POINT('Ctrl Pts',(0.0998851624184703,0.0969888232104648,
0.523569648406945));
#16312=CARTESIAN_POINT('Ctrl Pts',(-0.0273779061153799,0.136507610615132,
0.531511816529727));
#16313=CARTESIAN_POINT('Ctrl Pts',(-0.108290992649607,0.0687756007668377,
0.537800837551949));
#16314=CARTESIAN_POINT('Ctrl Pts',(-0.117713344367368,0.0148299618267192,
0.541442469199912));
#16315=CARTESIAN_POINT('Ctrl Pts',(-0.117629301205424,7.34277634442983E-5,
0.542436711473615));
#16316=CARTESIAN_POINT('Origin',(0.,0.,-0.0924367114736175));
#16317=CARTESIAN_POINT('',(-0.117582256074849,9.06819982020624E-6,0.432563288526383));
#16318=CARTESIAN_POINT('',(-0.11779560903417,-0.000106574656651148,0.442436711473616));
#16319=CARTESIAN_POINT('',(-0.117775,2.85464118895969E-14,-0.0924367114736175));
#16320=CARTESIAN_POINT('Ctrl Pts',(-0.117582256074849,9.06819982019261E-6,
0.432563288526383));
#16321=CARTESIAN_POINT('Ctrl Pts',(-0.117568373935691,-0.020201912089319,
0.43392366903486));
#16322=CARTESIAN_POINT('Ctrl Pts',(-0.10300922874285,-0.0797477867736473,
0.437930379422439));
#16323=CARTESIAN_POINT('Ctrl Pts',(-0.00838939967687663,-0.138954178686792,
0.44458341968912));
#16324=CARTESIAN_POINT('Ctrl Pts',(0.11219917790857,-0.0824013973067221,
0.452522409326426));
#16325=CARTESIAN_POINT('Ctrl Pts',(0.13007709763057,0.0495842159710775,
0.460461398963732));
#16326=CARTESIAN_POINT('Ctrl Pts',(0.0288783492374893,0.136178877755608,
0.468400388601037));
#16327=CARTESIAN_POINT('Ctrl Pts',(-0.0895654556576369,0.100852400902523,
0.475767685121922));
#16328=CARTESIAN_POINT('Ctrl Pts',(-0.117511448025972,0.0305757367622385,
0.480488651763704));
#16329=CARTESIAN_POINT('Ctrl Pts',(-0.117794891956694,-0.000106411733115381,
0.482563288526384));
#16330=CARTESIAN_POINT('Ctrl Pts',(-0.11779560903417,-0.000106574656651151,
0.442436711473616));
#16331=CARTESIAN_POINT('Ctrl Pts',(-0.117873644338608,-0.00854245500997505,
0.443007130042126));
#16332=CARTESIAN_POINT('Ctrl Pts',(-0.113196618671047,-0.056044542179559,
0.446224937984896));
#16333=CARTESIAN_POINT('Ctrl Pts',(-0.0487473834415776,-0.130413074907061,
0.452090135301926));
#16334=CARTESIAN_POINT('Ctrl Pts',(0.0831820848081396,-0.111645054821459,
0.460032303424706));
#16335=CARTESIAN_POINT('Ctrl Pts',(0.138908217753341,0.00940130521287039,
0.467974471547486));
#16336=CARTESIAN_POINT('Ctrl Pts',(0.0673801526530663,0.121835103839429,
0.475916639670265));
#16337=CARTESIAN_POINT('Ctrl Pts',(-0.0658750545035054,0.12265543075329,
0.483858807793047));
#16338=CARTESIAN_POINT('Ctrl Pts',(-0.116424939330292,0.0453161125527027,
0.489365498394162));
#16339=CARTESIAN_POINT('Ctrl Pts',(-0.11795471279604,0.00317945345687678,
0.492224799621019));
#16340=CARTESIAN_POINT('Ctrl Pts',(-0.117936566864074,5.52347650140663E-5,
0.492436711473616));
#16341=CARTESIAN_POINT('Origin',(0.,0.,-0.0924367114736175));
#16342=CARTESIAN_POINT('',(-0.117828183671793,0.000101754196006455,0.382563288526383));
#16343=CARTESIAN_POINT('',(-0.117581664177921,7.09484545444172E-6,0.392436711473616));
#16344=CARTESIAN_POINT('',(-0.117775,2.85464118895969E-14,-0.0924367114736175));
#16345=CARTESIAN_POINT('Ctrl Pts',(-0.117828183671793,0.000101754196006446,
0.382563288526384));
#16346=CARTESIAN_POINT('Ctrl Pts',(-0.117538790254565,-0.0316580736410773,
0.384712356426916));
#16347=CARTESIAN_POINT('Ctrl Pts',(-0.0879068326507716,-0.103002379129266,
0.38950775420655));
#16348=CARTESIAN_POINT('Ctrl Pts',(0.0326876424682324,-0.135315053971568,
0.396949481865287));
#16349=CARTESIAN_POINT('Ctrl Pts',(0.13141703692502,-0.0459152284901983,
0.404888471502591));
#16350=CARTESIAN_POINT('Ctrl Pts',(0.109843140674695,0.0855168418978295,
0.412827461139898));
#16351=CARTESIAN_POINT('Ctrl Pts',(-0.0122846228212416,0.13866410438033,
0.420766450777203));
#16352=CARTESIAN_POINT('Ctrl Pts',(-0.104166535924894,0.0775181589932739,
0.427345059906032));
#16353=CARTESIAN_POINT('Ctrl Pts',(-0.117595378674006,0.0191142356295008,
0.431277339155758));
#16354=CARTESIAN_POINT('Ctrl Pts',(-0.117582256074849,9.06819982019261E-6,
0.432563288526383));
#16355=CARTESIAN_POINT('Ctrl Pts',(-0.117581664177921,7.09484545444172E-6,
0.392436711473616));
#16356=CARTESIAN_POINT('Ctrl Pts',(-0.117570873504463,-0.0200907396801347,
0.393789460463232));
#16357=CARTESIAN_POINT('Ctrl Pts',(-0.10312708440739,-0.079535468422451,
0.397789598827109));
#16358=CARTESIAN_POINT('Ctrl Pts',(-0.00873482453528946,-0.138951719454826,
0.404437126565246));
#16359=CARTESIAN_POINT('Ctrl Pts',(0.112042812448737,-0.0826455423945668,
0.412379294688026));
#16360=CARTESIAN_POINT('Ctrl Pts',(0.130177722634257,0.049372441998279,
0.420321462810806));
#16361=CARTESIAN_POINT('Ctrl Pts',(0.0290564652212241,0.136160197297018,
0.428263630933586));
#16362=CARTESIAN_POINT('Ctrl Pts',(-0.0895090212855029,0.100936776489487,
0.435635380487856));
#16363=CARTESIAN_POINT('Ctrl Pts',(-0.117511471984497,0.0306096014671689,
0.440359740667866));
#16364=CARTESIAN_POINT('Ctrl Pts',(-0.11779560903417,-0.000106574656651151,
0.442436711473616));
#16365=CARTESIAN_POINT('Origin',(0.,0.,-0.0924367114736175));
#16366=CARTESIAN_POINT('',(-0.117911328466355,-7.22474488887591E-5,0.332563288526384));
#16367=CARTESIAN_POINT('',(-0.117821685414254,0.000103165543095151,0.342436711473616));
#16368=CARTESIAN_POINT('',(-0.117775,2.85464118895969E-14,-0.0924367114736175));
#16369=CARTESIAN_POINT('Ctrl Pts',(-0.117911328466355,-7.22474488887752E-5,
0.332563288526384));
#16370=CARTESIAN_POINT('Ctrl Pts',(-0.117942332027964,-0.00437115939612809,
0.332854713939869));
#16371=CARTESIAN_POINT('Ctrl Pts',(-0.115777752883067,-0.0476754067323583,
0.335792469232457));
#16372=CARTESIAN_POINT('Ctrl Pts',(-0.0622106591311991,-0.12453304658572,
0.341376554404146));
#16373=CARTESIAN_POINT('Ctrl Pts',(0.0708961914151981,-0.119801401679107,
0.349315544041452));
#16374=CARTESIAN_POINT('Ctrl Pts',(0.1391024375543,-0.00539978406154301,
0.357254533678757));
#16375=CARTESIAN_POINT('Ctrl Pts',(0.0799699354250877,0.113944965792994,
0.365193523316063));
#16376=CARTESIAN_POINT('Ctrl Pts',(-0.0523695618881846,0.128980908622551,
0.373132512953369));
#16377=CARTESIAN_POINT('Ctrl Pts',(-0.113921748517257,0.0538356345748906,
0.378922434690143));
#16378=CARTESIAN_POINT('Ctrl Pts',(-0.117895144954496,0.00745050051778832,
0.382066026547814));
#16379=CARTESIAN_POINT('Ctrl Pts',(-0.117828183671793,0.000101754196006446,
0.382563288526384));
#16380=CARTESIAN_POINT('Ctrl Pts',(-0.117821685414254,0.000103165543095145,
0.342436711473616));
#16381=CARTESIAN_POINT('Ctrl Pts',(-0.117532262555972,-0.0314544122979593,
0.344571790884339));
#16382=CARTESIAN_POINT('Ctrl Pts',(-0.0882170202347594,-0.102616110661261,
0.349354259669323));
#16383=CARTESIAN_POINT('Ctrl Pts',(0.0320320385160992,-0.135491055083419,
0.356784117828566));
#16384=CARTESIAN_POINT('Ctrl Pts',(0.131227975626944,-0.0465090949381858,
0.364726285951346));
#16385=CARTESIAN_POINT('Ctrl Pts',(0.110205605501345,0.0850799742312894,
0.372668454074126));
#16386=CARTESIAN_POINT('Ctrl Pts',(-0.0117764211155082,0.138727046407055,
0.380610622196906));
#16387=CARTESIAN_POINT('Ctrl Pts',(-0.10403099481448,0.0777947493501838,
0.387200041330069));
#16388=CARTESIAN_POINT('Ctrl Pts',(-0.117591991327853,0.019241607989002,
0.391142071088973));
#16389=CARTESIAN_POINT('Ctrl Pts',(-0.117581664177921,7.09484545444172E-6,
0.392436711473616));
#16390=CARTESIAN_POINT('Origin',(0.,0.,-0.0924367114736175));
#16391=CARTESIAN_POINT('',(-0.117608153246896,-5.64262068778628E-5,0.282563288526383));
#16392=CARTESIAN_POINT('',(-0.117918861549493,-6.80329776671096E-5,0.292436711473615));
#16393=CARTESIAN_POINT('',(-0.117775,2.85464118895969E-14,-0.0924367114736175));
#16394=CARTESIAN_POINT('Ctrl Pts',(-0.117608153246896,-5.64262068778604E-5,
0.282563288526383));
#16395=CARTESIAN_POINT('Ctrl Pts',(-0.117677606263852,-0.0160946837114709,
0.283643401331924));
#16396=CARTESIAN_POINT('Ctrl Pts',(-0.107144424846824,-0.0713401098021974,
0.287369844016567));
#16397=CARTESIAN_POINT('Ctrl Pts',(-0.0229969941138309,-0.137294515779738,
0.293742616580312));
#16398=CARTESIAN_POINT('Ctrl Pts',(0.102883268653204,-0.0937746172089793,
0.301681606217617));
#16399=CARTESIAN_POINT('Ctrl Pts',(0.134580950019115,0.0355895166223291,
0.309620595854923));
#16400=CARTESIAN_POINT('Ctrl Pts',(0.0430789950773988,0.13237388709478,
0.317559585492229));
#16401=CARTESIAN_POINT('Ctrl Pts',(-0.0830523456774332,0.10887452531409,
0.325207149716049));
#16402=CARTESIAN_POINT('Ctrl Pts',(-0.11766079978112,0.0346657214219864,
0.330208384060767));
#16403=CARTESIAN_POINT('Ctrl Pts',(-0.117911328466355,-7.22474488887752E-5,
0.332563288526384));
#16404=CARTESIAN_POINT('Ctrl Pts',(-0.117918861549493,-6.80329776671157E-5,
0.292436711473616));
#16405=CARTESIAN_POINT('Ctrl Pts',(-0.117946256357307,-0.00405052459867665,
0.292706731931186));
#16406=CARTESIAN_POINT('Ctrl Pts',(-0.11595553950755,-0.0470512577090033,
0.295624141763016));
#16407=CARTESIAN_POINT('Ctrl Pts',(-0.0631725212350128,-0.124068972994571,
0.301188940969106));
#16408=CARTESIAN_POINT('Ctrl Pts',(0.0700327441786229,-0.12032993078169,
0.309131109091886));
#16409=CARTESIAN_POINT('Ctrl Pts',(0.139080821187468,-0.00635631000930847,
0.317073277214666));
#16410=CARTESIAN_POINT('Ctrl Pts',(0.0807165776729536,0.11344034374014,
0.325015445337446));
#16411=CARTESIAN_POINT('Ctrl Pts',(-0.0515923433190751,0.129313988454311,
0.332957613460226));
#16412=CARTESIAN_POINT('Ctrl Pts',(-0.113774867115171,0.0543021652640841,
0.338764702172283));
#16413=CARTESIAN_POINT('Ctrl Pts',(-0.117891132111753,0.00767537174388221,
0.341924401510079));
#16414=CARTESIAN_POINT('Ctrl Pts',(-0.117821685414254,0.000103165543095145,
0.342436711473616));
#16415=CARTESIAN_POINT('Origin',(0.,0.,-0.0924367114736175));
#16416=CARTESIAN_POINT('',(-0.117705188630573,0.000102098618198066,0.232563288526383));
#16417=CARTESIAN_POINT('',(-0.1176142238744,-6.23262858038681E-5,0.242436711473616));
#16418=CARTESIAN_POINT('',(-0.117775,2.85464118895969E-14,-0.0924367114736175));
#16419=CARTESIAN_POINT('Ctrl Pts',(-0.117705188630573,0.000102098618198071,
0.232563288526383));
#16420=CARTESIAN_POINT('Ctrl Pts',(-0.117475649963863,-0.0275896003179174,
0.234432088723979));
#16421=CARTESIAN_POINT('Ctrl Pts',(-0.0938913217252411,-0.0948462909608301,
0.238947218800678));
#16422=CARTESIAN_POINT('Ctrl Pts',(0.0182347644767634,-0.138007750384372,
0.246108678756477));
#16423=CARTESIAN_POINT('Ctrl Pts',(0.125841858853055,-0.0595186723796334,
0.254047668393783));
#16424=CARTESIAN_POINT('Ctrl Pts',(0.118249355954961,0.073455671106145,
0.261986658031089));
#16425=CARTESIAN_POINT('Ctrl Pts',(0.00240767183786234,0.139186381940956,
0.269925647668394));
#16426=CARTESIAN_POINT('Ctrl Pts',(-0.0995777503027144,0.0858938305448248,
0.27678452450016));
#16427=CARTESIAN_POINT('Ctrl Pts',(-0.117507442931816,0.0231998416616275,
0.280997071452822));
#16428=CARTESIAN_POINT('Ctrl Pts',(-0.117608153246896,-5.64262068778604E-5,
0.282563288526383));
#16429=CARTESIAN_POINT('Ctrl Pts',(-0.1176142238744,-6.2326285803882E-5,
0.242436711473616));
#16430=CARTESIAN_POINT('Ctrl Pts',(-0.117689148257971,-0.0156863246439697,
0.243489062352292));
#16431=CARTESIAN_POINT('Ctrl Pts',(-0.107519643382358,-0.0705218816827611,
0.247188802605229));
#16432=CARTESIAN_POINT('Ctrl Pts',(-0.024381182195918,-0.137074561658528,
0.253535932232426));
#16433=CARTESIAN_POINT('Ctrl Pts',(0.101985705091022,-0.094777599970642,
0.261478100355206));
#16434=CARTESIAN_POINT('Ctrl Pts',(0.134923209124943,0.0343453801629359,
0.269420268477986));
#16435=CARTESIAN_POINT('Ctrl Pts',(0.0442571924125319,0.132004463632409,
0.277362436600766));
#16436=CARTESIAN_POINT('Ctrl Pts',(-0.0824920331482911,0.109525057495754,
0.285034584265976));
#16437=CARTESIAN_POINT('Ctrl Pts',(-0.117677666622401,0.0349954280503056,
0.290059342556926));
#16438=CARTESIAN_POINT('Ctrl Pts',(-0.117918861549493,-6.80329776671157E-5,
0.292436711473616));
#16439=CARTESIAN_POINT('Origin',(0.,0.,-0.0924367114736175));
#16440=CARTESIAN_POINT('',(-0.117967994073432,-3.0724305424694E-6,0.182563288526383));
#16441=CARTESIAN_POINT('',(-0.117691121003631,9.91971943564221E-5,0.192436711473615));
#16442=CARTESIAN_POINT('',(-0.117775,2.85464118895969E-14,-0.0924367114736175));
#16443=CARTESIAN_POINT('Ctrl Pts',(-0.117967994073432,-3.07243054247449E-6,
0.182563288526383));
#16444=CARTESIAN_POINT('Ctrl Pts',(-0.117968057042159,-0.000167453844217198,
0.182574446236933));
#16445=CARTESIAN_POINT('Ctrl Pts',(-0.117893299674953,-0.0393189363008842,
0.185231933826584));
#16446=CARTESIAN_POINT('Ctrl Pts',(-0.0749972298318695,-0.11727771015962,
0.190535751295337));
#16447=CARTESIAN_POINT('Ctrl Pts',(0.0578663373665801,-0.126610160769685,
0.198474740932643));
#16448=CARTESIAN_POINT('Ctrl Pts',(0.13775723856723,-0.0200396862227523,
0.206413730569949));
#16449=CARTESIAN_POINT('Ctrl Pts',(0.091540828968026,0.104875747581476,
0.214352720207254));
#16450=CARTESIAN_POINT('Ctrl Pts',(-0.0384749358425138,0.133784622116252,
0.22229170984456));
#16451=CARTESIAN_POINT('Ctrl Pts',(-0.110955338697302,0.0622468391270206,
0.22836189928427));
#16452=CARTESIAN_POINT('Ctrl Pts',(-0.11780069007939,0.0116234575531164,
0.231785758844877));
#16453=CARTESIAN_POINT('Ctrl Pts',(-0.117705188630573,0.000102098618198071,
0.232563288526383));
#16454=CARTESIAN_POINT('Ctrl Pts',(-0.117691121003631,9.91971943564221E-5,
0.192436711473615));
#16455=CARTESIAN_POINT('Ctrl Pts',(-0.117474218986382,-0.0270951350261672,
0.194271392773399));
#16456=CARTESIAN_POINT('Ctrl Pts',(-0.0945676524372527,-0.0938598508209937,
0.198753463447442));
#16457=CARTESIAN_POINT('Ctrl Pts',(0.0165156171993534,-0.138242945169174,
0.205882923495746));
#16458=CARTESIAN_POINT('Ctrl Pts',(0.125131592687617,-0.061040658666823,
0.213825091618526));
#16459=CARTESIAN_POINT('Ctrl Pts',(0.119114174013628,0.0720811421096423,
0.221767259741306));
#16460=CARTESIAN_POINT('Ctrl Pts',(0.0039759348809324,0.139169211541763,
0.229709427864086));
#16461=CARTESIAN_POINT('Ctrl Pts',(-0.0990660356104632,0.0867677816679632,
0.236599245108189));
#16462=CARTESIAN_POINT('Ctrl Pts',(-0.117500661679058,0.0236188235484957,
0.240841672978032));
#16463=CARTESIAN_POINT('Ctrl Pts',(-0.1176142238744,-6.2326285803882E-5,
0.242436711473616));
#16464=CARTESIAN_POINT('Origin',(0.,0.,-0.0924367114736175));
#16465=CARTESIAN_POINT('',(-0.117696212882312,-0.000100181105204699,0.132563288526383));
#16466=CARTESIAN_POINT('',(-0.117967699956222,8.3697257429456E-6,0.142436711473616));
#16467=CARTESIAN_POINT('',(-0.117775,2.85464118895969E-14,-0.0924367114736175));
#16468=CARTESIAN_POINT('Ctrl Pts',(-0.117696212882312,-0.000100181105204706,
0.132563288526383));
#16469=CARTESIAN_POINT('Ctrl Pts',(-0.117792074781153,-0.0119544960022407,
0.133363133628988));
#16470=CARTESIAN_POINT('Ctrl Pts',(-0.110696412003459,-0.0629173266909915,
0.136809308610694));
#16471=CARTESIAN_POINT('Ctrl Pts',(-0.0373480950846616,-0.134103559412242,
0.142901813471503));
#16472=CARTESIAN_POINT('Ctrl Pts',(0.0924198687735613,-0.104101940294199,
0.150840803108809));
#16473=CARTESIAN_POINT('Ctrl Pts',(0.137583777756591,0.0211978768359354,
0.158779792746114));
#16474=CARTESIAN_POINT('Ctrl Pts',(0.0567991668878991,0.127092487218924,
0.16671878238342));
#16475=CARTESIAN_POINT('Ctrl Pts',(-0.0757945745091616,0.116657324056303,
0.174646614310176));
#16476=CARTESIAN_POINT('Ctrl Pts',(-0.117953122434976,0.0388197061692436,
0.179928116357831));
#16477=CARTESIAN_POINT('Ctrl Pts',(-0.117967994073432,-3.07243054247449E-6,
0.182563288526383));
#16478=CARTESIAN_POINT('Ctrl Pts',(-0.117967699956222,8.3697257429579E-6,
0.142436711473616));
#16479=CARTESIAN_POINT('Ctrl Pts',(-0.117928252023989,-0.038547130539091,
0.145053723194506));
#16480=CARTESIAN_POINT('Ctrl Pts',(-0.0762804946418446,-0.116178754198862,
0.150318124289656));
#16481=CARTESIAN_POINT('Ctrl Pts',(0.0559861945572589,-0.127473226882309,
0.158229914759066));
#16482=CARTESIAN_POINT('Ctrl Pts',(0.137471621702818,-0.0220324926503626,
0.166172082881846));
#16483=CARTESIAN_POINT('Ctrl Pts',(0.0930189202108026,0.103592267873211,
0.174114251004626));
#16484=CARTESIAN_POINT('Ctrl Pts',(-0.0366486683060043,0.134315868829211,
0.182056419127406));
#16485=CARTESIAN_POINT('Ctrl Pts',(-0.110544190454925,0.0633195416932908,
0.188163905950403));
#16486=CARTESIAN_POINT('Ctrl Pts',(-0.11778720200735,0.0121454601492482,
0.191624003399139));
#16487=CARTESIAN_POINT('Ctrl Pts',(-0.117691121003631,9.91971943564221E-5,
0.192436711473615));
#16488=CARTESIAN_POINT('Origin',(0.,0.,-0.0924367114736175));
#16489=CARTESIAN_POINT('',(-0.117613109409711,6.11591708146705E-5,0.0825632885263832));
#16490=CARTESIAN_POINT('',(-0.117715749944134,-0.000104199409386274,0.0924367114736155));
#16491=CARTESIAN_POINT('',(-0.117775,2.85464118895969E-14,-0.0924367114736175));
#16492=CARTESIAN_POINT('Ctrl Pts',(-0.117613109409711,6.11591708146765E-5,
0.0825632885263832));
#16493=CARTESIAN_POINT('Ctrl Pts',(-0.117502393620717,-0.0235240259785673,
0.0841518210210431));
#16494=CARTESIAN_POINT('Ctrl Pts',(-0.0991849320095013,-0.0865581493706475,
0.088386683394805));
#16495=CARTESIAN_POINT('Ctrl Pts',(0.00357853460314598,-0.139161043603659,
0.0952678756476685));
#16496=CARTESIAN_POINT('Ctrl Pts',(0.118863112008681,-0.0724583686054966,
0.103206865284975));
#16497=CARTESIAN_POINT('Ctrl Pts',(0.125336705278751,0.0605752693714656,
0.11114585492228));
#16498=CARTESIAN_POINT('Ctrl Pts',(0.0170731091066207,0.138156245709763,
0.119084844559586));
#16499=CARTESIAN_POINT('Ctrl Pts',(-0.094337657277608,0.0941904991302726,
0.126223989094287));
#16500=CARTESIAN_POINT('Ctrl Pts',(-0.11747491061231,0.0272661325996615,
0.130716803749886));
#16501=CARTESIAN_POINT('Ctrl Pts',(-0.117696212882312,-0.000100181105204706,
0.132563288526383));
#16502=CARTESIAN_POINT('Ctrl Pts',(-0.117715749944134,-0.000104199409386274,
0.0924367114736155));
#16503=CARTESIAN_POINT('Ctrl Pts',(-0.117810584636384,-0.011244028442556,
0.0931886642413524));
#16504=CARTESIAN_POINT('Ctrl Pts',(-0.111246641208053,-0.0614941526881817,
0.0965880063833492));
#16505=CARTESIAN_POINT('Ctrl Pts',(-0.0397151780004399,-0.133441281507892,
0.102634737899606));
#16506=CARTESIAN_POINT('Ctrl Pts',(0.0906220264938673,-0.105695447092796,
0.110576906022386));
#16507=CARTESIAN_POINT('Ctrl Pts',(0.137940159127448,0.0188783162799928,
0.118519074145166));
#16508=CARTESIAN_POINT('Ctrl Pts',(0.0588909273047484,0.126157580947307,
0.126461242267946));
#16509=CARTESIAN_POINT('Ctrl Pts',(-0.074108440039672,0.117863552156501,
0.134403410390726));
#16510=CARTESIAN_POINT('Ctrl Pts',(-0.117763087033452,0.0399060678969832,
0.139728566792616));
#16511=CARTESIAN_POINT('Ctrl Pts',(-0.117968157858494,0.000455912857932787,
0.142406333820246));
#16512=CARTESIAN_POINT('Ctrl Pts',(-0.117967699956222,8.3697257429579E-6,
0.142436711473616));
#16513=CARTESIAN_POINT('Origin',(0.,0.,-0.0924367114736175));
#16514=CARTESIAN_POINT('',(-0.117917485785546,7.60014832213593E-5,0.0325632885263832));
#16515=CARTESIAN_POINT('',(-0.117600989619072,5.04992496179954E-5,0.0424367114736154));
#16516=CARTESIAN_POINT('',(-0.117775,2.85464118895969E-14,-0.0924367114736175));
#16517=CARTESIAN_POINT('Ctrl Pts',(-0.117917485785546,7.60014832213644E-5,
0.0325632885263832));
#16518=CARTESIAN_POINT('Ctrl Pts',(-0.117676727567847,-0.0349830640657269,
0.0349405084130983));
#16519=CARTESIAN_POINT('Ctrl Pts',(-0.0825043195215805,-0.109517225708346,
0.0399640581789154));
#16520=CARTESIAN_POINT('Ctrl Pts',(0.0441923146003338,-0.131999388615902,
0.0476339378238343));
#16521=CARTESIAN_POINT('Ctrl Pts',(0.134874939024977,-0.034459980695041,
0.0555729274611401));
#16522=CARTESIAN_POINT('Ctrl Pts',(0.102091080224759,0.094638871230671,
0.0635119170984456));
#16523=CARTESIAN_POINT('Ctrl Pts',(-0.0241513666277066,0.137095110112719,
0.0714509067357516));
#16524=CARTESIAN_POINT('Ctrl Pts',(-0.107448046275642,0.0706698818446754,
0.0778013638783972));
#16525=CARTESIAN_POINT('Ctrl Pts',(-0.117686834607281,0.0157664388843013,
0.0815054911419412));
#16526=CARTESIAN_POINT('Ctrl Pts',(-0.117613109409711,6.11591708146765E-5,
0.0825632885263832));
#16527=CARTESIAN_POINT('Ctrl Pts',(-0.117600989619072,5.04992496179954E-5,
0.0424367114736154));
#16528=CARTESIAN_POINT('Ctrl Pts',(-0.117514779739531,-0.0227353060542692,
0.043970994662459));
#16529=CARTESIAN_POINT('Ctrl Pts',(-0.100129952091853,-0.0849605109884783,
0.0481526672255625));
#16530=CARTESIAN_POINT('Ctrl Pts',(0.000787973702835166,-0.139222729671589,
0.054981729162926));
#16531=CARTESIAN_POINT('Ctrl Pts',(0.117431922513572,-0.0747907597173192,
0.0629238972857061));
#16532=CARTESIAN_POINT('Ctrl Pts',(0.126496838785129,0.0581591461343325,
0.070866065408486));
#16533=CARTESIAN_POINT('Ctrl Pts',(0.0196773008918215,0.137828289815661,
0.0788082335312661));
#16534=CARTESIAN_POINT('Ctrl Pts',(-0.0933482651079043,0.0956446566614129,
0.085998448886309));
#16535=CARTESIAN_POINT('Ctrl Pts',(-0.11747670148927,0.0279758085988667,
0.0905412748670923));
#16536=CARTESIAN_POINT('Ctrl Pts',(-0.117715749944134,-0.000104199409386274,
0.0924367114736155));
#16537=CARTESIAN_POINT('Origin',(0.,0.,1.55));
#16538=CARTESIAN_POINT('',(-0.143211704627722,-5.70397197726547E-6,1.50700023576178));
#16539=CARTESIAN_POINT('Ctrl Pts',(-0.0334019664626774,0.112939183906323,
1.532225));
#16540=CARTESIAN_POINT('Ctrl Pts',(-0.0250606930336426,0.115799676338094,
1.53184761307169));
#16541=CARTESIAN_POINT('Ctrl Pts',(-0.0164287086124659,0.117635554524944,
1.53147359869818));
#16542=CARTESIAN_POINT('Ctrl Pts',(-0.00767226928320402,0.118510614220874,
1.53110056493424));
#16543=CARTESIAN_POINT('Ctrl Pts',(-0.0042150196872779,0.118856108509867,
1.53095328237096));
#16544=CARTESIAN_POINT('Ctrl Pts',(-0.000736351480830917,0.119051293525916,
1.53080607672538));
#16545=CARTESIAN_POINT('Ctrl Pts',(0.00274830211697625,0.119097943881266,
1.53065904037218));
#16546=CARTESIAN_POINT('Ctrl Pts',(0.00972321854123044,0.119191319684798,
1.53036473098213));
#16547=CARTESIAN_POINT('Ctrl Pts',(0.0166907125456733,0.118690968429664,
1.53007241075126));
#16548=CARTESIAN_POINT('Ctrl Pts',(0.0235721318645625,0.11762150546261,
1.52978094357425));
#16549=CARTESIAN_POINT('Ctrl Pts',(0.0273478463565568,0.117034709826966,
1.52962102062912));
#16550=CARTESIAN_POINT('Ctrl Pts',(0.0310977188904398,0.116276259986281,
1.52946135449799));
#16551=CARTESIAN_POINT('Ctrl Pts',(0.0348087249896146,0.115347945392283,
1.52930175751644));
#16552=CARTESIAN_POINT('Ctrl Pts',(0.0378768737129624,0.114580442682688,
1.52916980751093));
#16553=CARTESIAN_POINT('Ctrl Pts',(0.0409182562642153,0.113696477767379,
1.52903790896105));
#16554=CARTESIAN_POINT('Ctrl Pts',(0.0439120268522727,0.112701821307647,
1.52890655030309));
#16555=CARTESIAN_POINT('Ctrl Pts',(0.0504861734289241,0.110517613410832,
1.52861809430882));
#16556=CARTESIAN_POINT('Ctrl Pts',(0.0568477403450367,0.107796947733889,
1.528331525126));
#16557=CARTESIAN_POINT('Ctrl Pts',(0.0629211062797432,0.10455513280498,
1.52804576869741));
#16558=CARTESIAN_POINT('Ctrl Pts',(0.0667529140263229,0.102509807084265,
1.52786547926507));
#16559=CARTESIAN_POINT('Ctrl Pts',(0.0704699809867569,0.100256700264741,
1.52768551335768));
#16560=CARTESIAN_POINT('Ctrl Pts',(0.0740519796445933,0.0977963961590643,
1.52750560123222));
#16561=CARTESIAN_POINT('Ctrl Pts',(0.0761474027326905,0.0963571499395001,
1.52740035495562));
#16562=CARTESIAN_POINT('Ctrl Pts',(0.0781972522873126,0.0948464165467323,
1.52729509152825));
#16563=CARTESIAN_POINT('Ctrl Pts',(0.0801950758490376,0.0932655888959708,
1.52718986717129));
#16564=CARTESIAN_POINT('Ctrl Pts',(0.0872135629190184,0.0877120362002772,
1.52682020700562));
#16565=CARTESIAN_POINT('Ctrl Pts',(0.0935342345834078,0.0813437113039547,
1.52645409167081));
#16566=CARTESIAN_POINT('Ctrl Pts',(0.0991216768718319,0.0743433873765979,
1.52608928877518));
#16567=CARTESIAN_POINT('Ctrl Pts',(0.101857856375295,0.0709153174549959,
1.52591064420861));
#16568=CARTESIAN_POINT('Ctrl Pts',(0.104417791592617,0.0673349702414553,
1.52573231437502));
#16569=CARTESIAN_POINT('Ctrl Pts',(0.106794530290299,0.0636205708890664,
1.52555403711528));
#16570=CARTESIAN_POINT('Ctrl Pts',(0.108394385735532,0.0611202951812291,
1.52543403324399));
#16571=CARTESIAN_POINT('Ctrl Pts',(0.109912312880749,0.0585571637778213,
1.52531395827658));
#16572=CARTESIAN_POINT('Ctrl Pts',(0.111341951189028,0.0559432008961949,
1.5251940432238));
#16573=CARTESIAN_POINT('Ctrl Pts',(0.115894033640165,0.0476201345006791,
1.52481222412716));
#16574=CARTESIAN_POINT('Ctrl Pts',(0.119530893641226,0.0388304356906876,
1.52443409356659));
#16575=CARTESIAN_POINT('Ctrl Pts',(0.122195159250079,0.0297595052710396,
1.52405718851832));
#16576=CARTESIAN_POINT('Ctrl Pts',(0.123464283518865,0.0254385629829291,
1.52387764960816));
#16577=CARTESIAN_POINT('Ctrl Pts',(0.124512110981915,0.0210533134598664,
1.52369838877875));
#16578=CARTESIAN_POINT('Ctrl Pts',(0.12532867129748,0.0166220814218575,
1.52351913980531));
#16579=CARTESIAN_POINT('Ctrl Pts',(0.126067828800149,0.012610891624201,
1.52335688207487));
#16580=CARTESIAN_POINT('Ctrl Pts',(0.12661735951473,0.00855739899605222,
1.52319445303817));
#16581=CARTESIAN_POINT('Ctrl Pts',(0.126966826155483,0.00450415768051923,
1.52303280899981));
#16582=CARTESIAN_POINT('Ctrl Pts',(0.127602972227412,-0.00287409603749457,
1.52273856283131));
#16583=CARTESIAN_POINT('Ctrl Pts',(0.12758177643555,-0.010267620141741,
1.52244625042084));
#16584=CARTESIAN_POINT('Ctrl Pts',(0.126865581413421,-0.0175939782534482,
1.52215473434257));
#16585=CARTESIAN_POINT('Ctrl Pts',(0.126426462283551,-0.0220859726121444,
1.52197599770985));
#16586=CARTESIAN_POINT('Ctrl Pts',(0.12572570473317,-0.0265528301690258,
1.52179756043894));
#16587=CARTESIAN_POINT('Ctrl Pts',(0.124776542651163,-0.0309793260681717,
1.52161916036391));
#16588=CARTESIAN_POINT('Ctrl Pts',(0.124151644840291,-0.0338935887106027,
1.52150170748789));
#16589=CARTESIAN_POINT('Ctrl Pts',(0.123418330834614,-0.0367926408403149,
1.52138417707714));
#16590=CARTESIAN_POINT('Ctrl Pts',(0.122581975874549,-0.0396644408336013,
1.52126680258073));
#16591=CARTESIAN_POINT('Ctrl Pts',(0.120074191833131,-0.0482754427851461,
1.52091485884509));
#16592=CARTESIAN_POINT('Ctrl Pts',(0.116656903439717,-0.0566007293654626,
1.52056600333313));
#16593=CARTESIAN_POINT('Ctrl Pts',(0.112443760417108,-0.0645262187619275,
1.52021830866717));
#16594=CARTESIAN_POINT('Ctrl Pts',(0.109356904590302,-0.0703330102694749,
1.51996356219884));
#16595=CARTESIAN_POINT('Ctrl Pts',(0.105841781173658,-0.0759253337267248,
1.51970943888381));
#16596=CARTESIAN_POINT('Ctrl Pts',(0.101930367117466,-0.0812537151913617,
1.51945518067311));
#16597=CARTESIAN_POINT('Ctrl Pts',(0.100130771446666,-0.0837052409256295,
1.51933819945644));
#16598=CARTESIAN_POINT('Ctrl Pts',(0.0982476276828181,-0.0860996963839449,
1.51922123442864));
#16599=CARTESIAN_POINT('Ctrl Pts',(0.0962924325256194,-0.0884227179472683,
1.51910469697823));
#16600=CARTESIAN_POINT('Ctrl Pts',(0.0906946176521128,-0.0950736369671782,
1.51877104482549));
#16601=CARTESIAN_POINT('Ctrl Pts',(0.0844921899154374,-0.101162815315101,
1.51843983772287));
#16602=CARTESIAN_POINT('Ctrl Pts',(0.0777644521522082,-0.106582693579069,
1.51810941878));
#16603=CARTESIAN_POINT('Ctrl Pts',(0.0731067700043679,-0.110334931124879,
1.5178806663426));
#16604=CARTESIAN_POINT('Ctrl Pts',(0.0681966627772886,-0.113766151308436,
1.51765229166508));
#16605=CARTESIAN_POINT('Ctrl Pts',(0.0630541948599911,-0.116833686038022,
1.5174237449583));
#16606=CARTESIAN_POINT('Ctrl Pts',(0.0607686815400033,-0.118197018118406,
1.51732216988754));
#16607=CARTESIAN_POINT('Ctrl Pts',(0.0584414404741937,-0.119485783651375,
1.51722075040181));
#16608=CARTESIAN_POINT('Ctrl Pts',(0.0560784264268894,-0.12069488199044,
1.51711960151386));
#16609=CARTESIAN_POINT('Ctrl Pts',(0.0475595529450054,-0.125053787850271,
1.51675495087613));
#16610=CARTESIAN_POINT('Ctrl Pts',(0.038563113830939,-0.128389854466075,
1.51639315730301));
#16611=CARTESIAN_POINT('Ctrl Pts',(0.0292711048986314,-0.130741856378471,
1.51603205677802));
#16612=CARTESIAN_POINT('Ctrl Pts',(0.0254547302664753,-0.13170786066222,
1.51588374709674));
#16613=CARTESIAN_POINT('Ctrl Pts',(0.0215881861914954,-0.132507324978224,
1.51573555432397));
#16614=CARTESIAN_POINT('Ctrl Pts',(0.0176832233642019,-0.13314066674995,
1.51558732853105));
#16615=CARTESIAN_POINT('Ctrl Pts',(0.0144414794405867,-0.133666441752394,
1.51546427740745));
#16616=CARTESIAN_POINT('Ctrl Pts',(0.0111713231872828,-0.134077605234841,
1.5153411329761));
#16617=CARTESIAN_POINT('Ctrl Pts',(0.00789687394913892,-0.134372952697723,
1.51521845803943));
#16618=CARTESIAN_POINT('Ctrl Pts',(-0.00208492598009478,-0.135273287095873,
1.51484449692866));
#16619=CARTESIAN_POINT('Ctrl Pts',(-0.0121386692885745,-0.135107999768821,
1.51447364169918));
#16620=CARTESIAN_POINT('Ctrl Pts',(-0.0220717676774029,-0.133899092645375,
1.51410356562093));
#16621=CARTESIAN_POINT('Ctrl Pts',(-0.0271373055616968,-0.133282591671289,
1.51391483957382));
#16622=CARTESIAN_POINT('Ctrl Pts',(-0.0321716696217597,-0.132393849601707,
1.51372631615657));
#16623=CARTESIAN_POINT('Ctrl Pts',(-0.0371491047637803,-0.131230566976147,
1.51353768678866));
#16624=CARTESIAN_POINT('Ctrl Pts',(-0.0401763453142056,-0.130523066780721,
1.51342296375255));
#16625=CARTESIAN_POINT('Ctrl Pts',(-0.0431793745847511,-0.129714439573166,
1.51330831773957));
#16626=CARTESIAN_POINT('Ctrl Pts',(-0.0461427198170546,-0.128807808452418,
1.51319405707679));
#16627=CARTESIAN_POINT('Ctrl Pts',(-0.0557912886485991,-0.125855842991896,
1.51282202756853));
#16628=CARTESIAN_POINT('Ctrl Pts',(-0.0650506639775802,-0.121862017750276,
1.51245293010828));
#16629=CARTESIAN_POINT('Ctrl Pts',(-0.0737251756215706,-0.116823260910032,
1.51208446868514));
#16630=CARTESIAN_POINT('Ctrl Pts',(-0.0774533877539874,-0.114657657224767,
1.51192610791459));
#16631=CARTESIAN_POINT('Ctrl Pts',(-0.0810733781510443,-0.112298364258586,
1.51176786463208));
#16632=CARTESIAN_POINT('Ctrl Pts',(-0.0845783705992567,-0.109758519633299,
1.51160955655689));
#16633=CARTESIAN_POINT('Ctrl Pts',(-0.0871260289206952,-0.107912394030924,
1.51149448786814));
#16634=CARTESIAN_POINT('Ctrl Pts',(-0.0896122610481647,-0.105970921032248,
1.51137940572563));
#16635=CARTESIAN_POINT('Ctrl Pts',(-0.0920243025666997,-0.10394826075131,
1.51126473391974));
#16636=CARTESIAN_POINT('Ctrl Pts',(-0.0995315444015674,-0.0976529296958118,
1.51090782920982));
#16637=CARTESIAN_POINT('Ctrl Pts',(-0.106349817996106,-0.090554906599088,
1.51055366538392));
#16638=CARTESIAN_POINT('Ctrl Pts',(-0.112409916721278,-0.0828189535999138,
1.51020021897155));
#16639=CARTESIAN_POINT('Ctrl Pts',(-0.11567060314877,-0.0786565598680515,
1.51001004419521));
#16640=CARTESIAN_POINT('Ctrl Pts',(-0.118711357121208,-0.0743087544864998,
1.50982007711492));
#16641=CARTESIAN_POINT('Ctrl Pts',(-0.121517490738653,-0.0697974244982526,
1.50963000253165));
#16642=CARTESIAN_POINT('Ctrl Pts',(-0.123184827969132,-0.0671169005197731,
1.50951706477726));
#16643=CARTESIAN_POINT('Ctrl Pts',(-0.124768226583796,-0.064379797453554,
1.50940414472167));
#16644=CARTESIAN_POINT('Ctrl Pts',(-0.12625918933752,-0.0616017405091787,
1.50929161182319));
#16645=CARTESIAN_POINT('Ctrl Pts',(-0.131254477666307,-0.0522942005345653,
1.50891458411209));
#16646=CARTESIAN_POINT('Ctrl Pts',(-0.135235816373665,-0.0424980109473837,
1.50854057440173));
#16647=CARTESIAN_POINT('Ctrl Pts',(-0.138100316247284,-0.0323932585971084,
1.50816719719795));
#16648=CARTESIAN_POINT('Ctrl Pts',(-0.139428601593765,-0.027707625827389,
1.5079940600046));
#16649=CARTESIAN_POINT('Ctrl Pts',(-0.140516076092011,-0.0229552175461711,
1.50782105881478));
#16650=CARTESIAN_POINT('Ctrl Pts',(-0.14134846970832,-0.01815262603916,
1.50764795577689));
#16651=CARTESIAN_POINT('Ctrl Pts',(-0.141840021659925,-0.0153165600461233,
1.5075457335416));
#16652=CARTESIAN_POINT('Ctrl Pts',(-0.142241997144177,-0.0124651428186592,
1.50744355431084));
#16653=CARTESIAN_POINT('Ctrl Pts',(-0.142550993842162,-0.00961078035088443,
1.50734168592779));
#16654=CARTESIAN_POINT('Ctrl Pts',(-0.142847161918882,-0.00687492249914849,
1.50724404681617));
#16655=CARTESIAN_POINT('Ctrl Pts',(-0.143058332724879,-0.00413406598225375,
1.5071466105924));
#16656=CARTESIAN_POINT('Ctrl Pts',(-0.143182669649515,-0.00139134585336764,
1.50704933585643));
#16657=CARTESIAN_POINT('Ctrl Pts',(-0.143203595382121,-0.00092974984559876,
1.50703296465278));
#16658=CARTESIAN_POINT('Ctrl Pts',(-0.143222061023464,-0.000468100854706259,
1.50701659802318));
#16659=CARTESIAN_POINT('Ctrl Pts',(-0.143238079070951,-6.41379011939899E-6,
1.50700023577028));
#16660=CARTESIAN_POINT('',(-0.00156744678985144,0.146109855568756,1.50365));
#16661=CARTESIAN_POINT('Ctrl Pts',(-0.00156962371672063,0.146072546381438,
1.50365));
#16662=CARTESIAN_POINT('Ctrl Pts',(-0.011711474284147,0.144648739717271,
1.50495065132295));
#16663=CARTESIAN_POINT('Ctrl Pts',(-0.0216501921041044,0.142222471223284,
1.50626105010813));
#16664=CARTESIAN_POINT('Ctrl Pts',(-0.0312062965385204,0.138804788898175,
1.50759029209282));
#16665=CARTESIAN_POINT('Ctrl Pts',(-0.0379863325344082,0.136379950477271,
1.50853338648503));
#16666=CARTESIAN_POINT('Ctrl Pts',(-0.0445735484268955,0.133455002060128,
1.5094859663039));
#16667=CARTESIAN_POINT('Ctrl Pts',(-0.0508923708069948,0.130021662144985,
1.51045128011208));
#16668=CARTESIAN_POINT('Ctrl Pts',(-0.053607485163773,0.128546401418451,
1.51086606268101));
#16669=CARTESIAN_POINT('Ctrl Pts',(-0.0562647183424556,0.126981576978965,
1.51128195276517));
#16670=CARTESIAN_POINT('Ctrl Pts',(-0.0588579379029418,0.125328026221608,
1.51169910067666));
#16671=CARTESIAN_POINT('Ctrl Pts',(-0.0624505046767585,0.123037247762191,
1.51227700458785));
#16672=CARTESIAN_POINT('Ctrl Pts',(-0.0659209207101175,0.120575889029892,
1.51285741907924));
#16673=CARTESIAN_POINT('Ctrl Pts',(-0.0692542752175272,0.117943487410649,
1.51344114883776));
#16674=CARTESIAN_POINT('Ctrl Pts',(-0.0735613784355843,0.114542101371374,
1.51419539934302));
#16675=CARTESIAN_POINT('Ctrl Pts',(-0.0776398170223455,0.110855132244726,
1.51495518495604));
#16676=CARTESIAN_POINT('Ctrl Pts',(-0.0814741368103916,0.106911749311875,
1.51572224163114));
#16677=CARTESIAN_POINT('Ctrl Pts',(-0.0845038784997064,0.103795829845314,
1.51632834224744));
#16678=CARTESIAN_POINT('Ctrl Pts',(-0.087381117690253,0.10051973853988,
1.51693898261853));
#16679=CARTESIAN_POINT('Ctrl Pts',(-0.0900959757046659,0.0970973798321736,
1.51755501917095));
#16680=CARTESIAN_POINT('Ctrl Pts',(-0.0920052356275281,0.0946905606587243,
1.51798825505079));
#16681=CARTESIAN_POINT('Ctrl Pts',(-0.093830595110286,0.092215607777745,
1.51842338946406));
#16682=CARTESIAN_POINT('Ctrl Pts',(-0.0955653742165971,0.0896840982544811,
1.51885969689116));
#16683=CARTESIAN_POINT('Ctrl Pts',(-0.0997851775729162,0.0835262696618028,
1.51992100293214));
#16684=CARTESIAN_POINT('Ctrl Pts',(-0.103479134251024,0.0770231540939269,
1.52099120961793));
#16685=CARTESIAN_POINT('Ctrl Pts',(-0.106606394578922,0.0702509006766953,
1.52207541818308));
#16686=CARTESIAN_POINT('Ctrl Pts',(-0.108879606303698,0.0653281362576702,
1.52286353153598));
#16687=CARTESIAN_POINT('Ctrl Pts',(-0.110852991156964,0.0602629640702717,
1.52365904329275));
#16688=CARTESIAN_POINT('Ctrl Pts',(-0.112503888351057,0.0550849881514033,
1.524463912762));
#16689=CARTESIAN_POINT('Ctrl Pts',(-0.113450017754745,0.0521174894567802,
1.52492518356294));
#16690=CARTESIAN_POINT('Ctrl Pts',(-0.114289979676541,0.0491121240008169,
1.52538965304266));
#16691=CARTESIAN_POINT('Ctrl Pts',(-0.115015874151616,0.0460903162170444,
1.52585530945224));
#16692=CARTESIAN_POINT('Ctrl Pts',(-0.117053612444637,0.0376074669234184,
1.52716250482259));
#16693=CARTESIAN_POINT('Ctrl Pts',(-0.118206139871793,0.0289652499882669,
1.52848357355921));
#16694=CARTESIAN_POINT('Ctrl Pts',(-0.11838625730212,0.0202925750432425,
1.52982832573377));
#16695=CARTESIAN_POINT('Ctrl Pts',(-0.118492077855379,0.015197303257165,
1.53061837930521));
#16696=CARTESIAN_POINT('Ctrl Pts',(-0.118261361656021,0.0100916471271278,
1.53141660760476));
#16697=CARTESIAN_POINT('Ctrl Pts',(-0.11766859746431,0.00500517689818842,
1.532225));
#16698=CARTESIAN_POINT('',(-0.115079981391543,0.0902137050004572,1.50365));
#16699=CARTESIAN_POINT('Origin',(0.,0.,1.50365));
#16700=CARTESIAN_POINT('Ctrl Pts',(-0.143238079070951,-6.41379011939899E-6,
1.50700023577028));
#16701=CARTESIAN_POINT('Ctrl Pts',(-0.143514357617001,0.00795674345750163,
1.50671802038504));
#16702=CARTESIAN_POINT('Ctrl Pts',(-0.14306421847979,0.0159310909218757,
1.50643710681857));
#16703=CARTESIAN_POINT('Ctrl Pts',(-0.141940608246003,0.023841490005315,
1.50615648267927));
#16704=CARTESIAN_POINT('Ctrl Pts',(-0.141317731836386,0.0282266413964,1.50600091791928));
#16705=CARTESIAN_POINT('Ctrl Pts',(-0.14048752132733,0.0325921818867556,
1.50584544210227));
#16706=CARTESIAN_POINT('Ctrl Pts',(-0.139456452513291,0.0369250818702156,
1.5056898827608));
#16707=CARTESIAN_POINT('Ctrl Pts',(-0.138790989895207,0.0397215809279161,
1.50558948313156));
#16708=CARTESIAN_POINT('Ctrl Pts',(-0.138042009924554,0.0425029011667524,
1.50548910366784));
#16709=CARTESIAN_POINT('Ctrl Pts',(-0.137214434473447,0.0452564915355094,
1.50538902890071));
#16710=CARTESIAN_POINT('Ctrl Pts',(-0.134176751889031,0.0553637675507716,
1.50502169637912));
#16711=CARTESIAN_POINT('Ctrl Pts',(-0.130076454936343,0.0651325632434767,
1.50465723703036));
#16712=CARTESIAN_POINT('Ctrl Pts',(-0.125018127980614,0.0743940890034878,
1.50429344851366));
#16713=CARTESIAN_POINT('Ctrl Pts',(-0.122034683484208,0.0798566160996726,
1.50407888293545));
#16714=CARTESIAN_POINT('Ctrl Pts',(-0.118716925567465,0.0851425936725427,
1.50386455072235));
#16715=CARTESIAN_POINT('Ctrl Pts',(-0.115078604842436,0.0902138214954005,
1.50365));
#16716=CARTESIAN_POINT('',(-0.05,-6.12323399573677E-18,1.6));
#16717=CARTESIAN_POINT('',(-0.1,-1.22464679914735E-17,1.55));
#16718=CARTESIAN_POINT('Origin',(0.,0.,1.6));
#16719=CARTESIAN_POINT('Ctrl Pts',(0.0850780204044575,-0.11908002747757,
-0.0164977839420936));
#16720=CARTESIAN_POINT('Ctrl Pts',(0.124677800165771,-0.0907875342533835,
-0.0138514540629917));
#16721=CARTESIAN_POINT('Ctrl Pts',(0.172751483861701,0.00791416360185712,
-0.00855879430478784));
#16722=CARTESIAN_POINT('Ctrl Pts',(0.0868617128612901,0.149726167188418,
-0.000619804667482127));
#16723=CARTESIAN_POINT('Ctrl Pts',(-0.078614020905812,0.154028602276276,
0.00731918496982359));
#16724=CARTESIAN_POINT('Ctrl Pts',(-0.172087192378165,0.0175525219725009,
0.0152581746071293));
#16725=CARTESIAN_POINT('Ctrl Pts',(-0.108045720411827,-0.135108484733225,
0.0231971642444351));
#16726=CARTESIAN_POINT('Ctrl Pts',(0.0549144151285058,-0.164025561655164,
0.0311361538817407));
#16727=CARTESIAN_POINT('Ctrl Pts',(0.167598788591005,-0.0428207868793744,
0.0390751435190465));
#16728=CARTESIAN_POINT('Ctrl Pts',(0.126860790413016,0.117600499296196,
0.0470141331563521));
#16729=CARTESIAN_POINT('Ctrl Pts',(-0.0300110592737492,0.170357625684536,
0.054953122793658));
#16730=CARTESIAN_POINT('Ctrl Pts',(-0.159409054995301,0.0671687418111174,
0.0628921124309635));
#16731=CARTESIAN_POINT('Ctrl Pts',(-0.142879399887002,-0.0975110083167992,
0.0708311020682695));
#16732=CARTESIAN_POINT('Ctrl Pts',(0.00444677171871267,-0.172924803493063,
0.078770091705575));
#16733=CARTESIAN_POINT('Ctrl Pts',(0.147702113712341,-0.0900384822365835,
0.0867090813428809));
#16734=CARTESIAN_POINT('Ctrl Pts',(0.155746353789385,0.0752722621313087,
0.0946480709801864));
#16735=CARTESIAN_POINT('Ctrl Pts',(0.021215449100004,0.17167621786987,0.102587060617492));
#16736=CARTESIAN_POINT('Ctrl Pts',(-0.132736728465598,0.110922462699857,
0.110526050254798));
#16737=CARTESIAN_POINT('Ctrl Pts',(-0.165177537004225,-0.0513732581591355,
0.118465039892104));
#16738=CARTESIAN_POINT('Ctrl Pts',(-0.0464096261145344,-0.166640254043574,
0.126404029529409));
#16739=CARTESIAN_POINT('Ctrl Pts',(0.114843114370719,-0.129359532685675,
0.134343019166715));
#16740=CARTESIAN_POINT('Ctrl Pts',(0.170964855654229,0.0263409830179588,
0.142282008804021));
#16741=CARTESIAN_POINT('Ctrl Pts',(0.0705799878925336,0.157928129946847,
0.150220998441327));
#16742=CARTESIAN_POINT('Ctrl Pts',(-0.0944160212638482,0.144942899583874,
0.158159988078632));
#16743=CARTESIAN_POINT('Ctrl Pts',(-0.172980633894512,-0.000727622896455919,
0.166098977715938));
#16744=CARTESIAN_POINT('Ctrl Pts',(-0.0931933312323777,-0.145732055885043,
0.174037967353244));
#16745=CARTESIAN_POINT('Ctrl Pts',(0.0719060791645076,-0.157328779695546,
0.181976956990549));
#16746=CARTESIAN_POINT('Ctrl Pts',(0.171180402159323,-0.0249017879745179,
0.189915946627855));
#16747=CARTESIAN_POINT('Ctrl Pts',(0.113750798721884,0.13032108391891,0.197854936265161));
#16748=CARTESIAN_POINT('Ctrl Pts',(-0.0478098650864174,0.16624393501773,
0.205793925902467));
#16749=CARTESIAN_POINT('Ctrl Pts',(-0.16560387403618,0.0499818570245514,
0.213732915539772));
#16750=CARTESIAN_POINT('Ctrl Pts',(-0.131798885878402,-0.112035185581475,
0.221671905177078));
#16751=CARTESIAN_POINT('Ctrl Pts',(0.0226589495323734,-0.171491694067101,
0.229610894814384));
#16752=CARTESIAN_POINT('Ctrl Pts',(0.156374069566079,-0.073959309724122,
0.237549884451689));
#16753=CARTESIAN_POINT('Ctrl Pts',(0.146939445926624,0.0912777539068999,
0.245488874088995));
#16754=CARTESIAN_POINT('Ctrl Pts',(0.00299182995941577,0.172956289510158,
0.253427863726301));
#16755=CARTESIAN_POINT('Ctrl Pts',(-0.143694601292225,0.0963051955349955,
0.261366853363607));
#16756=CARTESIAN_POINT('Ctrl Pts',(-0.15883847309497,-0.0685067047260848,
0.269305843000912));
#16757=CARTESIAN_POINT('Ctrl Pts',(-0.0285766086907934,-0.170605411881679,
0.277244832638218));
#16758=CARTESIAN_POINT('Ctrl Pts',(0.12784518248692,-0.116526556812001,
0.285183822275524));
#16759=CARTESIAN_POINT('Ctrl Pts',(0.167233470900423,0.0442243749325307,
0.293122811912829));
#16760=CARTESIAN_POINT('Ctrl Pts',(0.0535309779628647,0.164490922320707,
0.301061801550136));
#16761=CARTESIAN_POINT('Ctrl Pts',(-0.109175456582181,0.134177303623408,
0.309000791187441));
#16762=CARTESIAN_POINT('Ctrl Pts',(-0.171939242908932,-0.0189664407699395,
0.316939780824747));
#16763=CARTESIAN_POINT('Ctrl Pts',(-0.0773044361184472,-0.154747708493488,
0.324878770462053));
#16764=CARTESIAN_POINT('Ctrl Pts',(0.0880972839194656,-0.148868054644337,
0.332817760099358));
#16765=CARTESIAN_POINT('Ctrl Pts',(0.172851978230285,-0.00670989936239309,
0.340756749736664));
#16766=CARTESIAN_POINT('Ctrl Pts',(0.0993725327910066,0.141590708926387,
0.34869573937397));
#16767=CARTESIAN_POINT('Ctrl Pts',(-0.0650756559739905,0.160274727038081,
0.356634729011275));
#16768=CARTESIAN_POINT('Ctrl Pts',(-0.169951541620772,0.0322382168908211,
0.364573718648582));
#16769=CARTESIAN_POINT('Ctrl Pts',(-0.119248438453561,-0.125310171390688,
0.372512708285886));
#16770=CARTESIAN_POINT('Ctrl Pts',(0.0406184374886585,-0.168145685830938,
0.380451697923193));
#16771=CARTESIAN_POINT('Ctrl Pts',(0.163301917673335,-0.0570553486694088,
0.388390687560498));
#16772=CARTESIAN_POINT('Ctrl Pts',(0.136493684039406,0.106265249940549,
0.396329677197804));
#16773=CARTESIAN_POINT('Ctrl Pts',(-0.0152651628095069,0.172307295063139,
0.404268666835109));
#16774=CARTESIAN_POINT('Ctrl Pts',(-0.153049799296248,0.0806138205455782,
0.412207656472416));
#16775=CARTESIAN_POINT('Ctrl Pts',(-0.150727833715048,-0.0848760818555219,
0.420146646109721));
#16776=CARTESIAN_POINT('Ctrl Pts',(-0.0104248664208018,-0.172667748255674,
0.428085635747027));
#16777=CARTESIAN_POINT('Ctrl Pts',(0.139421351618932,-0.10239392482138,
0.436024625384332));
#16778=CARTESIAN_POINT('Ctrl Pts',(0.16163687742079,0.0616145192729195,
0.443963615021638));
#16779=CARTESIAN_POINT('Ctrl Pts',(0.0358849196425865,0.169219093691645,
0.451902604658944));
#16780=CARTESIAN_POINT('Ctrl Pts',(-0.122717222714247,0.121915185177559,
0.45984159429625));
#16781=CARTESIAN_POINT('Ctrl Pts',(-0.168980158036723,-0.0369937199732681,
0.467780583933555));
#16782=CARTESIAN_POINT('Ctrl Pts',(-0.0605533396431397,-0.162037409833775,
0.475719573570861));
#16783=CARTESIAN_POINT('Ctrl Pts',(0.103305911202344,-0.138746956140414,
0.483658563208167));
#16784=CARTESIAN_POINT('Ctrl Pts',(0.172595680358559,0.0115568269495825,
0.491597552845473));
#16785=CARTESIAN_POINT('Ctrl Pts',(0.0838859329010004,0.151281127008313,
0.499536542482778));
#16786=CARTESIAN_POINT('Ctrl Pts',(-0.0816156370489812,0.152517923263679,
0.507475532120084));
#16787=CARTESIAN_POINT('Ctrl Pts',(-0.172403684765527,0.0141350135070757,
0.51541452175739));
#16788=CARTESIAN_POINT('Ctrl Pts',(-0.105367974675403,-0.137187532379513,
0.523353511394695));
#16789=CARTESIAN_POINT('Ctrl Pts',(0.0581248948911363,-0.162924294448283,
0.531292501032001));
#16790=CARTESIAN_POINT('Ctrl Pts',(0.168408406744046,-0.039515030880773,
0.539231490669306));
#16791=CARTESIAN_POINT('Ctrl Pts',(0.124525564004667,0.120067535316156,
0.547170480306613));
#16792=CARTESIAN_POINT('Ctrl Pts',(-0.0333518982867267,0.169736501696743,
0.555109469943918));
#16793=CARTESIAN_POINT('Ctrl Pts',(-0.160697983451488,0.0640233335761385,
0.563048459581225));
#16794=CARTESIAN_POINT('Ctrl Pts',(-0.14093607811848,-0.100298808627811,
0.570987449218529));
#16795=CARTESIAN_POINT('Ctrl Pts',(0.00784314775175556,-0.172804265459278,
0.578926438855836));
#16796=CARTESIAN_POINT('Ctrl Pts',(0.149442509381278,-0.0871192603125336,
0.586865428493141));
#16797=CARTESIAN_POINT('Ctrl Pts',(0.154237495636292,0.0783174569774929,
0.594804418130446));
#16798=CARTESIAN_POINT('Ctrl Pts',(0.0178386252221998,0.172059909850489,
0.602743407767753));
#16799=CARTESIAN_POINT('Ctrl Pts',(-0.134890284021987,0.108293307291099,
0.610682397405058));
#16800=CARTESIAN_POINT('Ctrl Pts',(-0.164136382878957,-0.0546083962682395,
0.618621387042364));
#16801=CARTESIAN_POINT('Ctrl Pts',(-0.0431268722112106,-0.167519855601819,
0.62656037667967));
#16802=CARTESIAN_POINT('Ctrl Pts',(0.117362334288317,-0.127078368017432,
0.634499366316975));
#16803=CARTESIAN_POINT('Ctrl Pts',(0.170414367112955,0.0296946562375699,
0.642438355954282));
#16804=CARTESIAN_POINT('Ctrl Pts',(0.0674637261050104,0.159284257814778,
0.650377345591586));
#16805=CARTESIAN_POINT('Ctrl Pts',(-0.0972453325609638,0.143060037825677,
0.658316335228894));
#16806=CARTESIAN_POINT('Ctrl Pts',(-0.172932953925271,-0.00412584224812367,
0.666255324866198));
#16807=CARTESIAN_POINT('Ctrl Pts',(-0.0903123078403481,-0.147534796506203,
0.674194314503505));
#16808=CARTESIAN_POINT('Ctrl Pts',(0.0749830665657334,-0.155885755782802,
0.68213330414081));
#16809=CARTESIAN_POINT('Ctrl Pts',(0.17163658245605,-0.021533989188811,
0.690072293778116));
#16810=CARTESIAN_POINT('Ctrl Pts',(0.11116857013107,0.132530668686874,0.698011283415421));
#16811=CARTESIAN_POINT('Ctrl Pts',(-0.0510666492692211,0.165272582299639,
0.705950273052727));
#16812=CARTESIAN_POINT('Ctrl Pts',(-0.166553851089581,0.0467187736868841,
0.713889262690032));
#16813=CARTESIAN_POINT('Ctrl Pts',(-0.129572416918314,-0.114602870389546,
0.721828252327339));
#16814=CARTESIAN_POINT('Ctrl Pts',(0.0260236847639906,-0.171013440871999,
0.729767241964644));
#16815=CARTESIAN_POINT('Ctrl Pts',(0.157796886564457,-0.0708729265526718,
0.73770623160195));
#16816=CARTESIAN_POINT('Ctrl Pts',(0.145117853242075,0.0941468947867542,
0.745645221239255));
#16817=CARTESIAN_POINT('Ctrl Pts',(-0.000406629147419015,0.172981686256994,
0.753584210876562));
#16818=CARTESIAN_POINT('Ctrl Pts',(-0.145558870420566,0.0934635991681543,
0.761523200513868));
#16819=CARTESIAN_POINT('Ctrl Pts',(-0.157461941624574,-0.0716140074803496,
0.769462190151172));
#16820=CARTESIAN_POINT('Ctrl Pts',(-0.0252193968429213,-0.17113389830906,
0.777401179788479));
#16821=CARTESIAN_POINT('Ctrl Pts',(0.130109777350283,-0.113992433807847,
0.785340169425784));
#16822=CARTESIAN_POINT('Ctrl Pts',(0.166332367384696,0.0475012914327479,
0.793279159063091));
#16823=CARTESIAN_POINT('Ctrl Pts',(0.0502890745800368,0.165510839842773,
0.801218148700395));
#16824=CARTESIAN_POINT('Ctrl Pts',(-0.111790419467279,0.132006557575396,
0.809157138337702));
#16825=CARTESIAN_POINT('Ctrl Pts',(-0.171533445990104,-0.0223406811520247,
0.817096127975007));
#16826=CARTESIAN_POINT('Ctrl Pts',(-0.0742493586638003,-0.156236557391639,
0.825035117612313));
#16827=CARTESIAN_POINT('Ctrl Pts',(0.0910049278783345,-0.147108572929777,
0.832974107249618));
#16828=CARTESIAN_POINT('Ctrl Pts',(0.172950439922886,-0.00331277195964383,
0.840913096886925));
#16829=CARTESIAN_POINT('Ctrl Pts',(0.0965716772857839,0.143515644700454,
0.848852086524229));
#16830=CARTESIAN_POINT('Ctrl Pts',(-0.0682118374171683,0.158965324406771,
0.856791076161536));
#16831=CARTESIAN_POINT('Ctrl Pts',(-0.170552089827228,0.0288931442238776,
0.864730065798841));
#16832=CARTESIAN_POINT('Ctrl Pts',(-0.116763592698541,-0.127628729319482,
0.872669055436147));
#16833=CARTESIAN_POINT('Ctrl Pts',(0.0439139712140358,-0.167315248138923,
0.880608045073453));
#16834=CARTESIAN_POINT('Ctrl Pts',(0.164391304101163,-0.0538361241500125,
0.888547034710759));
#16835=CARTESIAN_POINT('Ctrl Pts',(0.134379664555536,0.108926281867684,
0.896486024348063));
#16836=CARTESIAN_POINT('Ctrl Pts',(-0.018647348250808,0.17197414204115,
0.904425013985371));
#16837=CARTESIAN_POINT('Ctrl Pts',(-0.154603991719776,0.0775914613336281,
0.912364003622676));
#16838=CARTESIAN_POINT('Ctrl Pts',(-0.149031276472826,-0.0878208845346985,
0.920302993259982));
#16839=CARTESIAN_POINT('Ctrl Pts',(-0.00703064139541984,-0.172839229369798,
0.928241982897287));
#16840=CARTESIAN_POINT('Ctrl Pts',(0.141406064038169,-0.099635105162837,
0.936180972534593));
#16841=CARTESIAN_POINT('Ctrl Pts',(0.160395209035295,0.064778129380991,
0.944119962171899));
#16842=CARTESIAN_POINT('Ctrl Pts',(0.03255353276219,0.169891426011666,0.952058951809204));
#16843=CARTESIAN_POINT('Ctrl Pts',(-0.125088671715395,0.119480765548496,
0.959997941446511));
#16844=CARTESIAN_POINT('Ctrl Pts',(-0.168220770124088,-0.040306347222682,
0.967936931083815));
#16845=CARTESIAN_POINT('Ctrl Pts',(-0.0573582824064844,-0.163195761485875,
0.975875920721122));
#16846=CARTESIAN_POINT('Ctrl Pts',(0.106011781834435,-0.136690640644722,
0.983814910358427));
#16847=CARTESIAN_POINT('Ctrl Pts',(0.17233532526783,0.014945393685262,0.991753899995733));
#16848=CARTESIAN_POINT('Ctrl Pts',(0.0808976893297158,0.152899944371113,
0.999692889633039));
#16849=CARTESIAN_POINT('Ctrl Pts',(-0.0845962369090198,0.150885074902754,
1.00763187927034));
#16850=CARTESIAN_POINT('Ctrl Pts',(-0.172648106016301,0.0107452601904448,
1.01557086890765));
#16851=CARTESIAN_POINT('Ctrl Pts',(-0.102652466413112,-0.13923110380544,
1.02350985854496));
#16852=CARTESIAN_POINT('Ctrl Pts',(0.0613144709582997,-0.161750934398167,
1.03144884818226));
#16853=CARTESIAN_POINT('Ctrl Pts',(0.169152212322519,-0.0361988700648799,
1.03938783781957));
#16854=CARTESIAN_POINT('Ctrl Pts',(0.122142696063681,0.12249077894222,1.04732682745687));
#16855=CARTESIAN_POINT('Ctrl Pts',(-0.0366800874558037,0.169048514669047,
1.05526581709418));
#16856=CARTESIAN_POINT('Ctrl Pts',(-0.161924764760067,0.0608539208677085,
1.06320480673148));
#16857=CARTESIAN_POINT('Ctrl Pts',(-0.138938417355371,-0.103048266896446,
1.07114379636879));
#16858=CARTESIAN_POINT('Ctrl Pts',(0.011236529066559,-0.172616828675865,
1.0790827860061));
#16859=CARTESIAN_POINT('Ctrl Pts',(0.151125203217684,-0.0841665140064042,
1.0870217756434));
#16860=CARTESIAN_POINT('Ctrl Pts',(0.152669111109608,0.0813324759279986,
1.09496076528071));
#16861=CARTESIAN_POINT('Ctrl Pts',(0.0144549108781955,0.172377158228925,
1.10289975491801));
#16862=CARTESIAN_POINT('Ctrl Pts',(-0.136991769602464,0.10562236594946,
1.11083874455532));
#16863=CARTESIAN_POINT('Ctrl Pts',(-0.163031873671196,-0.0578224635832477,
1.11877773419263));
#16864=CARTESIAN_POINT('Ctrl Pts',(-0.0398274706979539,-0.168334790537727,
1.12671672382993));
#16865=CARTESIAN_POINT('Ctrl Pts',(0.119836252144435,-0.124748153491552,
1.13465571346724));
#16866=CARTESIAN_POINT('Ctrl Pts',(0.169798099063322,0.0330368685268242,
1.14259470310454));
#16867=CARTESIAN_POINT('Ctrl Pts',(0.0643214233134591,0.160578901573361,
1.15053369274185));
#16868=CARTESIAN_POINT('Ctrl Pts',(-0.100037107244844,0.141121955420339,
1.15847268237915));
#16869=CARTESIAN_POINT('Ctrl Pts',(-0.172818522111203,-0.00752246920075927,
1.16641167201646));
#16870=CARTESIAN_POINT('Ctrl Pts',(-0.0873964240115842,-0.149280588817046,
1.17435066165376));
#16871=CARTESIAN_POINT('Ctrl Pts',(0.0780311106025284,-0.154382560238235,
1.18228965129107));
#16872=CARTESIAN_POINT('Ctrl Pts',(0.172026511281289,-0.01815787828917,
1.19022864092837));
#16873=CARTESIAN_POINT('Ctrl Pts',(0.10854343062882,0.134689096792963,1.19816763056568));
#16874=CARTESIAN_POINT('Ctrl Pts',(-0.0543037217972188,0.164237434607784,
1.20610662020299));
#16875=CARTESIAN_POINT('Ctrl Pts',(-0.167439538594998,0.0434376569656869,
1.21404560984029));
#16876=CARTESIAN_POINT('Ctrl Pts',(-0.127295933190098,-0.117126318651471,
1.2219845994776));
#16877=CARTESIAN_POINT('Ctrl Pts',(0.0293783748903316,-0.170469176734012,
1.2299235891149));
#16878=CARTESIAN_POINT('Ctrl Pts',(0.159158794190081,-0.0677591865323411,
1.23786257875221));
#16879=CARTESIAN_POINT('Ctrl Pts',(0.143240245273553,0.0969796950995427,
1.24580156838952));
#16880=CARTESIAN_POINT('Ctrl Pts',(-0.00380493129617075,0.172940312320012,
1.25374055802682));
#16881=CARTESIAN_POINT('Ctrl Pts',(-0.147366954032488,0.0905859259858403,
1.26167954766413));
#16882=CARTESIAN_POINT('Ctrl Pts',(-0.156024630070406,-0.074693667330688,
1.26961853730143));
#16883=CARTESIAN_POINT('Ctrl Pts',(-0.0218524503424686,-0.171596327294885,
1.27755752693874));
#16884=CARTESIAN_POINT('Ctrl Pts',(0.132324150022753,-0.111414309889572,
1.28549651657604));
#16885=CARTESIAN_POINT('Ctrl Pts',(0.165367059817933,0.0507598725070622,
1.29343550621335));
#16886=CARTESIAN_POINT('Ctrl Pts',(0.0470277596764783,0.166466870408131,
1.30137449585065));
#16887=CARTESIAN_POINT('Ctrl Pts',(-0.114362231391601,0.129784857201791,
1.30931348548797));
#16888=CARTESIAN_POINT('Ctrl Pts',(-0.171061437441431,-0.0257062980954763,
1.31725247512526));
#16889=CARTESIAN_POINT('Ctrl Pts',(-0.071165620995849,-0.157665099140374,
1.32519146476257));
#16890=CARTESIAN_POINT('Ctrl Pts',(0.0938774439379855,-0.145292307632914,
1.33313045439988));
#16891=CARTESIAN_POINT('Ctrl Pts',(0.172982143233999,8.56343898915854E-5,
1.34106944403719));
#16892=CARTESIAN_POINT('Ctrl Pts',(0.0937335447930804,0.145385183220099,
1.34900843367449));
#16893=CARTESIAN_POINT('Ctrl Pts',(-0.0713216883190155,0.157594562185848,
1.3569474233118));
#16894=CARTESIAN_POINT('Ctrl Pts',(-0.171086806821499,0.0255369173285507,
1.3648864129491));
#16895=CARTESIAN_POINT('Ctrl Pts',(-0.114233673229396,-0.129898019862958,
1.37282540258641));
#16896=CARTESIAN_POINT('Ctrl Pts',(0.0471925482590101,-0.166420232464351,
1.38076439222371));
#16897=CARTESIAN_POINT('Ctrl Pts',(0.165417247017141,-0.0505961085897048,
1.38870338186102));
#16898=CARTESIAN_POINT('Ctrl Pts',(0.132213753266125,0.111545248710567,
1.39664237149832));
#16899=CARTESIAN_POINT('Ctrl Pts',(-0.0220222951247444,0.17157464463752,
1.40458136113563));
#16900=CARTESIAN_POINT('Ctrl Pts',(-0.156098584526576,0.0745390809398717,
1.41252035077293));
#16901=CARTESIAN_POINT('Ctrl Pts',(-0.147277046608992,-0.0907316537045687,
1.42045934041024));
#16902=CARTESIAN_POINT('Ctrl Pts',(-0.00363398118293899,-0.172944250658386,
1.42839833004755));
#16903=CARTESIAN_POINT('Ctrl Pts',(0.143336722904634,-0.0968373407211472,
1.43633731968485));
#16904=CARTESIAN_POINT('Ctrl Pts',(0.159090624036536,0.0679158129692223,
1.44427630932216));
#16905=CARTESIAN_POINT('Ctrl Pts',(0.0292114869387437,0.170499931406899,
1.45221529895946));
#16906=CARTESIAN_POINT('Ctrl Pts',(-0.127415456569397,0.116996902323752,
1.46015428859677));
#16907=CARTESIAN_POINT('Ctrl Pts',(-0.167389576437263,-0.0435971050111283,
1.46809327823408));
#16908=CARTESIAN_POINT('Ctrl Pts',(-0.0541541359620402,-0.164303103757731,
1.47603226787138));
#16909=CARTESIAN_POINT('Ctrl Pts',(0.108701533888403,-0.13455879509903,
1.48397125750869));
#16910=CARTESIAN_POINT('Ctrl Pts',(0.171961157005542,0.0182848320604298,
1.49191024714599));
#16911=CARTESIAN_POINT('Ctrl Pts',(0.0779697431325927,0.154543202561513,
1.4998492367833));
#16912=CARTESIAN_POINT('Ctrl Pts',(-0.0877325682749983,0.149025855561406,
1.5077882264206));
#16913=CARTESIAN_POINT('Ctrl Pts',(-0.144149484752264,0.0548439265155397,
1.51308088617881));
#16914=CARTESIAN_POINT('Ctrl Pts',(-0.146217781693078,0.00621955116994065,
1.51572721605791));
#16915=CARTESIAN_POINT('Ctrl Pts',(0.0795408277542855,-0.111329858282327,
-0.0109985226280624));
#16916=CARTESIAN_POINT('Ctrl Pts',(0.116563307192903,-0.0848787452970238,
-0.00835219274896048));
#16917=CARTESIAN_POINT('Ctrl Pts',(0.16150817751539,0.00739908052493189,
-0.00305953299075667));
#16918=CARTESIAN_POINT('Ctrl Pts',(0.0812084309002137,0.139981433724326,
0.00487945664654907));
#16919=CARTESIAN_POINT('Ctrl Pts',(-0.0734975292821143,0.144003850402812,
0.0128184462838548));
#16920=CARTESIAN_POINT('Ctrl Pts',(-0.160887120581772,0.0164101388376342,
0.0207574359211605));
#16921=CARTESIAN_POINT('Ctrl Pts',(-0.101013704785435,-0.126315124179183,
0.0286964255584662));
#16922=CARTESIAN_POINT('Ctrl Pts',(0.0513403816191153,-0.153350170642076,
0.0366354151957719));
#16923=CARTESIAN_POINT('Ctrl Pts',(0.156690838735662,-0.0400338514845966,
0.0445744048330777));
#16924=CARTESIAN_POINT('Ctrl Pts',(0.118604220350264,0.109946623274354,
0.0525133944703833));
#16925=CARTESIAN_POINT('Ctrl Pts',(-0.0280578283917351,0.15927012049393,
0.0604523841076892));
#16926=CARTESIAN_POINT('Ctrl Pts',(-0.14903412333264,0.0627971513379326,
0.0683913737449947));
#16927=CARTESIAN_POINT('Ctrl Pts',(-0.133580279395553,-0.0911646307683348,
0.0763303633823007));
#16928=CARTESIAN_POINT('Ctrl Pts',(0.0041573593468571,-0.161670216863261,
0.0842693530196062));
#16929=CARTESIAN_POINT('Ctrl Pts',(0.138089113144455,-0.0841784443595545,
0.0922083426569122));
#16930=CARTESIAN_POINT('Ctrl Pts',(0.14560980428584,0.0703732645446943,
0.100147332294218));
#16931=CARTESIAN_POINT('Ctrl Pts',(0.0198346691022095,0.160502893816501,
0.108086321931524));
#16932=CARTESIAN_POINT('Ctrl Pts',(-0.124097730593135,0.103703218031488,
0.116025311568829));
#16933=CARTESIAN_POINT('Ctrl Pts',(-0.154427171169137,-0.0480296962598115,
0.123964301206135));
#16934=CARTESIAN_POINT('Ctrl Pts',(-0.0433891157712434,-0.155794689166463,
0.13190329084344));
#16935=CARTESIAN_POINT('Ctrl Pts',(0.107368699171666,-0.12094033522185,
0.139842280480747));
#16936=CARTESIAN_POINT('Ctrl Pts',(0.15983782968835,0.0246266142906177,
0.147781270118052));
#16937=CARTESIAN_POINT('Ctrl Pts',(0.0659863808909888,0.147649582370873,
0.155720259755358));
#16938=CARTESIAN_POINT('Ctrl Pts',(-0.0882710769349216,0.135509478890084,
0.163659249392663));
#16939=CARTESIAN_POINT('Ctrl Pts',(-0.161722413615419,-0.00068026650363694,
0.171598239029969));
#16940=CARTESIAN_POINT('Ctrl Pts',(-0.0871279640988751,-0.136247273976568,
0.179537228667275));
#16941=CARTESIAN_POINT('Ctrl Pts',(0.0672261652318651,-0.147089240053593,
0.187476218304581));
#16942=CARTESIAN_POINT('Ctrl Pts',(0.160039347628626,-0.023281087390596,
0.195415207941886));
#16943=CARTESIAN_POINT('Ctrl Pts',(0.106347475470598,0.121839305139765,
0.203354197579192));
#16944=CARTESIAN_POINT('Ctrl Pts',(-0.0446982220051161,0.15542416405057,
0.211293187216498));
#16945=CARTESIAN_POINT('Ctrl Pts',(-0.154825760608133,0.0467288526640558,
0.219232176853804));
#16946=CARTESIAN_POINT('Ctrl Pts',(-0.12322092627477,-0.104743520787053,
0.227171166491109));
#16947=CARTESIAN_POINT('Ctrl Pts',(0.0211842211805034,-0.160330379506191,
0.235110156128415));
#16948=CARTESIAN_POINT('Ctrl Pts',(0.146196665995071,-0.0691457639426259,
0.24304914576572));
#16949=CARTESIAN_POINT('Ctrl Pts',(0.137376082602736,0.0853370596399817,
0.250988135403027));
#16950=CARTESIAN_POINT('Ctrl Pts',(0.00279711058556459,0.161699653653757,
0.258927125040332));
#16951=CARTESIAN_POINT('Ctrl Pts',(-0.134342424474264,0.0900372967480426,
0.266866114677638));
#16952=CARTESIAN_POINT('Ctrl Pts',(-0.148500677015507,-0.0640480346713102,
0.274805104314944));
#16953=CARTESIAN_POINT('Ctrl Pts',(-0.0267167371651392,-0.159501779847699,
0.282744093952249));
#16954=CARTESIAN_POINT('Ctrl Pts',(0.119524544542348,-0.108942576944327,
0.290683083589556));
#16955=CARTESIAN_POINT('Ctrl Pts',(0.156349297273321,0.0413460888291301,
0.29862207322686));
#16956=CARTESIAN_POINT('Ctrl Pts',(0.0500469836677093,0.153785243912065,
0.306561062864167));
#16957=CARTESIAN_POINT('Ctrl Pts',(-0.102069913541897,0.125444547784578,
0.314500052501472));
#16958=CARTESIAN_POINT('Ctrl Pts',(-0.160748800211922,-0.0177320345633525,
0.322439042138778));
#16959=CARTESIAN_POINT('Ctrl Pts',(-0.0722731771226978,-0.144676154524232,
0.330378031776084));
#16960=CARTESIAN_POINT('Ctrl Pts',(0.082363586418043,-0.139179170322594,
0.338317021413389));
#16961=CARTESIAN_POINT('Ctrl Pts',(0.16160213133829,-0.00627319426210969,
0.346256011050695));
#16962=CARTESIAN_POINT('Ctrl Pts',(0.0929050003357002,0.132375461215256,
0.354195000688001));
#16963=CARTESIAN_POINT('Ctrl Pts',(-0.0608402912787218,0.149843454232904,
0.362133990325306));
#16964=CARTESIAN_POINT('Ctrl Pts',(-0.158890465884947,0.0301400343429239,
0.370072979962613));
#16965=CARTESIAN_POINT('Ctrl Pts',(-0.1114873084483,-0.117154521356547,
0.378011969599918));
#16966=CARTESIAN_POINT('Ctrl Pts',(0.0379748391485164,-0.157202141877815,
0.385950959237223));
#16967=CARTESIAN_POINT('Ctrl Pts',(0.152673624090564,-0.0533419752763387,
0.39388994887453));
#16968=CARTESIAN_POINT('Ctrl Pts',(0.127610169584502,0.0993491139263089,
0.401828938511835));
#16969=CARTESIAN_POINT('Ctrl Pts',(-0.014271649480085,0.16109289816887,
0.409767928149142));
#16970=CARTESIAN_POINT('Ctrl Pts',(-0.143088751545671,0.0753671745551693,
0.417706917786446));
#16971=CARTESIAN_POINT('Ctrl Pts',(-0.140917908083783,-0.0793520321139836,
0.425645907423752));
#16972=CARTESIAN_POINT('Ctrl Pts',(-0.00974637750615997,-0.161429891732714,
0.433584897061058));
#16973=CARTESIAN_POINT('Ctrl Pts',(0.130347293715478,-0.0957297489831606,
0.441523886698364));
#16974=CARTESIAN_POINT('Ctrl Pts',(0.15111695082405,0.0576044181723055,
0.449462876335669));
#16975=CARTESIAN_POINT('Ctrl Pts',(0.0335493961742207,0.158205688379633,
0.457401865972975));
#16976=CARTESIAN_POINT('Ctrl Pts',(-0.114730331382826,0.113980493419335,
0.465340855610281));
#16977=CARTESIAN_POINT('Ctrl Pts',(-0.157982303542021,-0.03458603167299,
0.473279845247587));
#16978=CARTESIAN_POINT('Ctrl Pts',(-0.0566123040428622,-0.151491415104245,
0.481218834884892));
#16979=CARTESIAN_POINT('Ctrl Pts',(0.0965823799129518,-0.129716790392294,
0.489157824522198));
#16980=CARTESIAN_POINT('Ctrl Pts',(0.161362514281243,0.0108046658515635,
0.497096814159504));
#16981=CARTESIAN_POINT('Ctrl Pts',(0.0784263257203939,0.141435191000425,
0.50503580379681));
#16982=CARTESIAN_POINT('Ctrl Pts',(-0.076303789130349,0.14259149197508,
0.512974793434115));
#16983=CARTESIAN_POINT('Ctrl Pts',(-0.161183014472451,0.0132150544797126,
0.520913783071421));
#16984=CARTESIAN_POINT('Ctrl Pts',(-0.0985102366584373,-0.128258859705,
0.528852772708727));
#16985=CARTESIAN_POINT('Ctrl Pts',(0.0543419114689404,-0.152320577983508,
0.536791762346032));
#16986=CARTESIAN_POINT('Ctrl Pts',(0.157447763940923,-0.0369432463290883,
0.544730751983338));
#16987=CARTESIAN_POINT('Ctrl Pts',(0.116420979124965,0.112253095453589,
0.552669741620643));
#16988=CARTESIAN_POINT('Ctrl Pts',(-0.0311812332291155,0.158689421555565,
0.56060873125795));
#16989=CARTESIAN_POINT('Ctrl Pts',(-0.150239163551416,0.0598564579197502,
0.568547720895255));
#16990=CARTESIAN_POINT('Ctrl Pts',(-0.131763436204723,-0.0937709907106254,
0.576486710532561));
#16991=CARTESIAN_POINT('Ctrl Pts',(0.00733268664935855,-0.161557523891122,
0.584425700169866));
#16992=CARTESIAN_POINT('Ctrl Pts',(0.139716237417787,-0.0814492162095161,
0.592364689807173));
#16993=CARTESIAN_POINT('Ctrl Pts',(0.144199148209332,0.0732202668325601,
0.600303679444478));
#16994=CARTESIAN_POINT('Ctrl Pts',(0.0166776214282734,0.160861613702037,
0.608242669081784));
#16995=CARTESIAN_POINT('Ctrl Pts',(-0.126111124778327,0.101245177793678,
0.616181658719089));
#16996=CARTESIAN_POINT('Ctrl Pts',(-0.153453779210204,-0.0510542795996006,
0.624120648356396));
#16997=CARTESIAN_POINT('Ctrl Pts',(-0.0403200156494649,-0.156617042997737,
0.6320596379937));
#16998=CARTESIAN_POINT('Ctrl Pts',(0.10972395892722,-0.118807637198397,
0.639998627631007));
#16999=CARTESIAN_POINT('Ctrl Pts',(0.159323168980049,0.0277620180369333,
0.647937617268312));
#17000=CARTESIAN_POINT('Ctrl Pts',(0.0630729369615192,0.148917448414806,
0.655876606905618));
#17001=CARTESIAN_POINT('Ctrl Pts',(-0.0909162461746061,0.133749160748195,
0.663815596542924));
#17002=CARTESIAN_POINT('Ctrl Pts',(-0.161677836835157,-0.00385731715476066,
0.671754586180229));
#17003=CARTESIAN_POINT('Ctrl Pts',(-0.0844344483789265,-0.137932685561743,
0.679693575817536));
#17004=CARTESIAN_POINT('Ctrl Pts',(0.0701028908975481,-0.145740133481257,
0.687632565454841));
#17005=CARTESIAN_POINT('Ctrl Pts',(0.1604658380222,-0.0201324774223393,
0.695571555092147));
#17006=CARTESIAN_POINT('Ctrl Pts',(0.10393330787963,0.123905081947942,0.703510544729453));
#17007=CARTESIAN_POINT('Ctrl Pts',(-0.0477430426119635,0.15451603056473,
0.711449534366758));
#17008=CARTESIAN_POINT('Ctrl Pts',(-0.155713909636705,0.0436781428746717,
0.719388524004064));
#17009=CARTESIAN_POINT('Ctrl Pts',(-0.121139364160222,-0.10714409115852,
0.72732751364137));
#17010=CARTESIAN_POINT('Ctrl Pts',(0.0243299669821161,-0.159883252800214,
0.735266503278675));
#17011=CARTESIAN_POINT('Ctrl Pts',(0.147526880793862,-0.0662602540182413,
0.743205492915981));
#17012=CARTESIAN_POINT('Ctrl Pts',(0.135673045916277,0.0880194662056535,
0.751144482553287));
#17013=CARTESIAN_POINT('Ctrl Pts',(-0.000380164216571841,0.161723397486253,
0.759083472190592));
#17014=CARTESIAN_POINT('Ctrl Pts',(-0.136085360063504,0.0873806419964673,
0.767022461827899));
#17015=CARTESIAN_POINT('Ctrl Pts',(-0.147213735311121,-0.0669531026545853,
0.774961451465203));
#17016=CARTESIAN_POINT('Ctrl Pts',(-0.023578025097595,-0.159995870421162,
0.78290044110251));
#17017=CARTESIAN_POINT('Ctrl Pts',(0.121641751185188,-0.106573384050283,
0.790839430739816));
#17018=CARTESIAN_POINT('Ctrl Pts',(0.155506840911589,0.0444097314676148,
0.798778420377121));
#17019=CARTESIAN_POINT('Ctrl Pts',(0.047016075363265,0.15473878142458,0.806717410014428));
#17020=CARTESIAN_POINT('Ctrl Pts',(-0.104514684958047,0.123415081928621,
0.814656399651731));
#17021=CARTESIAN_POINT('Ctrl Pts',(-0.16036941405942,-0.020886666885039,
0.82259538928904));
#17022=CARTESIAN_POINT('Ctrl Pts',(-0.0694169354231278,-0.146068103622213,
0.830534378926343));
#17023=CARTESIAN_POINT('Ctrl Pts',(0.085081990139753,-0.137534202194171,
0.838473368563651));
#17024=CARTESIAN_POINT('Ctrl Pts',(0.161694184779289,-0.00309716449182502,
0.846412358200955));
#17025=CARTESIAN_POINT('Ctrl Pts',(0.0902864348795877,0.134175115040242,
0.854351347838261));
#17026=CARTESIAN_POINT('Ctrl Pts',(-0.0637723584188847,0.148619272374149,
0.862290337475567));
#17027=CARTESIAN_POINT('Ctrl Pts',(-0.159451928190027,0.0270126713934565,
0.870229327112872));
#17028=CARTESIAN_POINT('Ctrl Pts',(-0.109164185657521,-0.119322178948671,
0.878168316750179));
#17029=CARTESIAN_POINT('Ctrl Pts',(0.0410558873341998,-0.156425752146281,
0.886107306387484));
#17030=CARTESIAN_POINT('Ctrl Pts',(0.153692109215179,-0.0503322698109037,
0.894046296024789));
#17031=CARTESIAN_POINT('Ctrl Pts',(0.125633738317809,0.101836956040625,
0.901985285662096));
#17032=CARTESIAN_POINT('Ctrl Pts',(-0.0174337097671096,0.160781427979367,
0.909924275299401));
#17033=CARTESIAN_POINT('Ctrl Pts',(-0.144541791370401,0.072541521673891,
0.917863264936708));
#17034=CARTESIAN_POINT('Ctrl Pts',(-0.13933176907,-0.082105176128868,0.925802254574012));
#17035=CARTESIAN_POINT('Ctrl Pts',(-0.00657306121577474,-0.161590212220858,
0.933741244211319));
#17036=CARTESIAN_POINT('Ctrl Pts',(0.132202833700187,-0.0931504835251481,
0.941680233848624));
#17037=CARTESIAN_POINT('Ctrl Pts',(0.149956094815541,0.0605621288182698,
0.949619223485929));
#17038=CARTESIAN_POINT('Ctrl Pts',(0.0304348282896272,0.158834262822317,
0.957558213123236));
#17039=CARTESIAN_POINT('Ctrl Pts',(-0.116947437700435,0.111704514835484,
0.965497202760542));
#17040=CARTESIAN_POINT('Ctrl Pts',(-0.157272339407096,-0.0376830608728604,
0.973436192397847));
#17041=CARTESIAN_POINT('Ctrl Pts',(-0.0536251929639052,-0.152574376940928,
0.981375182035153));
#17042=CARTESIAN_POINT('Ctrl Pts',(0.0991121424632477,-0.127794307524525,
0.989314171672459));
#17043=CARTESIAN_POINT('Ctrl Pts',(0.161119104064031,0.0139726921146952,
0.997253161309763));
#17044=CARTESIAN_POINT('Ctrl Pts',(0.0756325681075411,0.142948649734045,
1.00519215094707));
#17045=CARTESIAN_POINT('Ctrl Pts',(-0.0790904005129918,0.141064915432658,
1.01313114058437));
#17046=CARTESIAN_POINT('Ctrl Pts',(-0.161411527883023,0.0100459188627121,
1.02107013022168));
#17047=CARTESIAN_POINT('Ctrl Pts',(-0.095971463730607,-0.130169427934261,
1.02900911985899));
#17048=CARTESIAN_POINT('Ctrl Pts',(0.0573238981132153,-0.151223584550935,
1.03694810949629));
#17049=CARTESIAN_POINT('Ctrl Pts',(0.158143159897702,-0.0338429135403315,
1.0448870991336));
#17050=CARTESIAN_POINT('Ctrl Pts',(0.114193197054413,0.114518625410106,
1.0528260887709));
#17051=CARTESIAN_POINT('Ctrl Pts',(-0.0342928115212847,0.158046211271557,
1.06076507840821));
#17052=CARTESIAN_POINT('Ctrl Pts',(-0.151386101389109,0.0568933223281485,
1.06870406804552));
#17053=CARTESIAN_POINT('Ctrl Pts',(-0.129895790602315,-0.0963415040526547,
1.07664305768282));
#17054=CARTESIAN_POINT('Ctrl Pts',(0.0105052141409744,-0.161382286187737,
1.08458204732013));
#17055=CARTESIAN_POINT('Ctrl Pts',(0.141289415307547,-0.0786886455683398,
1.09252103695743));
#17056=CARTESIAN_POINT('Ctrl Pts',(0.14273283995608,0.076039057183793,1.10046002659474));
#17057=CARTESIAN_POINT('Ctrl Pts',(0.013514131745196,0.161158214381091,
1.10839901623204));
#17058=CARTESIAN_POINT('Ctrl Pts',(-0.128075837894479,0.0987480712062529,
1.11633800586935));
#17059=CARTESIAN_POINT('Ctrl Pts',(-0.152421155552179,-0.0540591635106084,
1.12427699550666));
#17060=CARTESIAN_POINT('Ctrl Pts',(-0.0372353514058616,-0.157378938949945,
1.13221598514396));
#17061=CARTESIAN_POINT('Ctrl Pts',(0.11203686504723,-0.116629081663695,
1.14015497478127));
#17062=CARTESIAN_POINT('Ctrl Pts',(0.158747009937404,0.0308867067726846,
1.14809396441857));
#17063=CARTESIAN_POINT('Ctrl Pts',(0.0601351468730053,0.150127831962932,
1.15603295405588));
#17064=CARTESIAN_POINT('Ctrl Pts',(-0.0935263218228598,0.13193721592339,
1.16397194369318));
#17065=CARTESIAN_POINT('Ctrl Pts',(-0.161570852667341,-0.00703287904607843,
1.17191093333049));
#17066=CARTESIAN_POINT('Ctrl Pts',(-0.0817083410685703,-0.13956485524354,
1.17984992296779));
#17067=CARTESIAN_POINT('Ctrl Pts',(0.0729525569401478,-0.144334771469742,
1.1877889126051));
#17068=CARTESIAN_POINT('Ctrl Pts',(0.160830388835411,-0.016976096323307,
1.19572790224241));
#17069=CARTESIAN_POINT('Ctrl Pts',(0.101479022178261,0.125923031559255,
1.20366689187971));
#17070=CARTESIAN_POINT('Ctrl Pts',(-0.0507694344715009,0.153548254118279,
1.21160588151702));
#17071=CARTESIAN_POINT('Ctrl Pts',(-0.15654195331917,0.0406105733811438,
1.21954487115432));
#17072=CARTESIAN_POINT('Ctrl Pts',(-0.119011042423884,-0.109503304062093,
1.22748386079163));
#17073=CARTESIAN_POINT('Ctrl Pts',(0.0274663214511058,-0.159374411387982,
1.23542285042894));
#17074=CARTESIAN_POINT('Ctrl Pts',(0.148800150427453,-0.0633491677300162,
1.24336184006624));
#17075=CARTESIAN_POINT('Ctrl Pts',(0.133917639627974,0.0906678973829495,
1.25130082970354));
#17076=CARTESIAN_POINT('Ctrl Pts',(-0.00355729227603857,0.161684716318317,
1.25923981934086));
#17077=CARTESIAN_POINT('Ctrl Pts',(-0.137775766897813,0.0846902584421788,
1.26717880897816));
#17078=CARTESIAN_POINT('Ctrl Pts',(-0.14586996931591,-0.0698323268364953,
1.27511779861547));
#17079=CARTESIAN_POINT('Ctrl Pts',(-0.0204302119447119,-0.160428202816007,
1.28305678825277));
#17080=CARTESIAN_POINT('Ctrl Pts',(0.123712004283314,-0.104163053984564,
1.29099577789008));
#17081=CARTESIAN_POINT('Ctrl Pts',(0.15460435913624,0.0474562320176185,
1.29893476752738));
#17082=CARTESIAN_POINT('Ctrl Pts',(0.043967018911749,0.155632589980133,
1.30687375716469));
#17083=CARTESIAN_POINT('Ctrl Pts',(-0.106919113837756,0.121337978043289,
1.31481274680199));
#17084=CARTESIAN_POINT('Ctrl Pts',(-0.159928125575155,-0.0240332370134145,
1.3227517364393));
#17085=CARTESIAN_POINT('Ctrl Pts',(-0.0665338988230771,-0.147403670583407,
1.33069072607661));
#17086=CARTESIAN_POINT('Ctrl Pts',(0.0877675522160205,-0.135836146169277,
1.33862971571391));
#17087=CARTESIAN_POINT('Ctrl Pts',(0.161723824721502,8.00609866524728E-5,
1.34656870535122));
#17088=CARTESIAN_POINT('Ctrl Pts',(0.0876330185603928,0.135922977069285,
1.35450769498852));
#17089=CARTESIAN_POINT('Ctrl Pts',(-0.0666798087068602,0.147337724435113,
1.36244668462583));
#17090=CARTESIAN_POINT('Ctrl Pts',(-0.159951843822013,0.0238748801740983,
1.37038567426313));
#17091=CARTESIAN_POINT('Ctrl Pts',(-0.106798922716859,-0.121443775659372,
1.37832466390044));
#17092=CARTESIAN_POINT('Ctrl Pts',(0.0441210824430389,-0.155588987406456,
1.38626365353774));
#17093=CARTESIAN_POINT('Ctrl Pts',(0.154651279966657,-0.0473031264624986,
1.39420264317505));
#17094=CARTESIAN_POINT('Ctrl Pts',(0.123608792556459,0.10428547082216,1.40214163281236));
#17095=CARTESIAN_POINT('Ctrl Pts',(-0.020589002599541,0.160407931346284,
1.41008062244966));
#17096=CARTESIAN_POINT('Ctrl Pts',(-0.145939110542184,0.0696878015005003,
1.41801961208697));
#17097=CARTESIAN_POINT('Ctrl Pts',(-0.137691710982408,-0.0848265016612731,
1.42595860172427));
#17098=CARTESIAN_POINT('Ctrl Pts',(-0.00339746822928561,-0.161688398335044,
1.43389759136158));
#17099=CARTESIAN_POINT('Ctrl Pts',(0.134007838137522,-0.0905348079547059,
1.44183658099889));
#17100=CARTESIAN_POINT('Ctrl Pts',(0.148736417039967,0.0634956003383226,
1.44977557063619));
#17101=CARTESIAN_POINT('Ctrl Pts',(0.0273102951854726,0.159403164432859,
1.4577145602735));
#17102=CARTESIAN_POINT('Ctrl Pts',(-0.119122786779006,0.109382310628272,
1.4656535499108));
#17103=CARTESIAN_POINT('Ctrl Pts',(-0.156495242883694,-0.0407596439572756,
1.47359253954811));
#17104=CARTESIAN_POINT('Ctrl Pts',(-0.0506295842364637,-0.153609649276743,
1.48153152918541));
#17105=CARTESIAN_POINT('Ctrl Pts',(0.10162683549218,-0.125801210382132,
1.48947051882272));
#17106=CARTESIAN_POINT('Ctrl Pts',(0.160769288057966,0.017094787472962,
1.49740950846002));
#17107=CARTESIAN_POINT('Ctrl Pts',(0.0728951834924312,0.144484958595688,
1.50534849809733));
#17108=CARTESIAN_POINT('Ctrl Pts',(-0.0820226078184241,0.139326700971572,
1.51328748773464));
#17109=CARTESIAN_POINT('Ctrl Pts',(-0.134767702434085,0.0512744806661359,
1.51858014749284));
#17110=CARTESIAN_POINT('Ctrl Pts',(-0.136701386950156,0.00581475974600206,
1.52122647737194));
#17111=CARTESIAN_POINT('Ctrl Pts',(0.0740036351041134,-0.103579689087085,
-0.0054992613140312));
#17112=CARTESIAN_POINT('Ctrl Pts',(0.108448814220036,-0.0789699563406641,
-0.00285293143492929));
#17113=CARTESIAN_POINT('Ctrl Pts',(0.150264871169078,0.00688399744800666,
0.00243972832327453));
#17114=CARTESIAN_POINT('Ctrl Pts',(0.0755551489391376,0.130236700260234,
0.0103787179605803));
#17115=CARTESIAN_POINT('Ctrl Pts',(-0.0683810376584167,0.133979098529349,
0.0183177075978859));
#17116=CARTESIAN_POINT('Ctrl Pts',(-0.14968704878538,0.0152677557027674,
0.0262566972351917));
#17117=CARTESIAN_POINT('Ctrl Pts',(-0.0939816891590436,-0.11752176362514,
0.0341956868724974));
#17118=CARTESIAN_POINT('Ctrl Pts',(0.0477663481097245,-0.142674779628989,
0.0421346765098031));
#17119=CARTESIAN_POINT('Ctrl Pts',(0.14578288888032,-0.0372469160898187,
0.0500736661471088));
#17120=CARTESIAN_POINT('Ctrl Pts',(0.110347650287512,0.102292747252513,
0.0580126557844146));
#17121=CARTESIAN_POINT('Ctrl Pts',(-0.0261045975097209,0.148182615303324,
0.0659516454217203));
#17122=CARTESIAN_POINT('Ctrl Pts',(-0.13865919166998,0.0584255608647477,
0.073890635059026));
#17123=CARTESIAN_POINT('Ctrl Pts',(-0.124281158904105,-0.0848182532198701,
0.0818296246963318));
#17124=CARTESIAN_POINT('Ctrl Pts',(0.00386794697500161,-0.15041563023346,
0.0897686143336374));
#17125=CARTESIAN_POINT('Ctrl Pts',(0.128476112576568,-0.0783184064825255,
0.0977076039709433));
#17126=CARTESIAN_POINT('Ctrl Pts',(0.135473254782295,0.0654742669580799,
0.105646593608249));
#17127=CARTESIAN_POINT('Ctrl Pts',(0.0184538891044151,0.149329569763132,
0.113585583245555));
#17128=CARTESIAN_POINT('Ctrl Pts',(-0.115458732720671,0.096483973363118,
0.12152457288286));
#17129=CARTESIAN_POINT('Ctrl Pts',(-0.143676805334049,-0.0446861343604874,
0.129463562520166));
#17130=CARTESIAN_POINT('Ctrl Pts',(-0.0403686054279526,-0.144949124289353,
0.137402552157472));
#17131=CARTESIAN_POINT('Ctrl Pts',(0.0998942839726139,-0.112521137758025,
0.145341541794778));
#17132=CARTESIAN_POINT('Ctrl Pts',(0.14871080372247,0.0229122455632766,
0.153280531432083));
#17133=CARTESIAN_POINT('Ctrl Pts',(0.0613927738894439,0.137371034794898,
0.161219521069389));
#17134=CARTESIAN_POINT('Ctrl Pts',(-0.0821261326059948,0.126076058196294,
0.169158510706695));
#17135=CARTESIAN_POINT('Ctrl Pts',(-0.150464193336327,-0.000632910110818063,
0.177097500344));
#17136=CARTESIAN_POINT('Ctrl Pts',(-0.0810625969653723,-0.126762492068094,
0.185036489981306));
#17137=CARTESIAN_POINT('Ctrl Pts',(0.0625462512992226,-0.136849700411639,
0.192975479618612));
#17138=CARTESIAN_POINT('Ctrl Pts',(0.148898293097928,-0.0216603868066741,
0.200914469255917));
#17139=CARTESIAN_POINT('Ctrl Pts',(0.0989441522193119,0.113357526360621,
0.208853458893223));
#17140=CARTESIAN_POINT('Ctrl Pts',(-0.0415865789238149,0.144604393083411,
0.216792448530529));
#17141=CARTESIAN_POINT('Ctrl Pts',(-0.144047647180085,0.0434758483035601,
0.224731438167835));
#17142=CARTESIAN_POINT('Ctrl Pts',(-0.114642966671137,-0.0974518559926297,
0.232670427805141));
#17143=CARTESIAN_POINT('Ctrl Pts',(0.0197094928286333,-0.149169064945282,
0.240609417442446));
#17144=CARTESIAN_POINT('Ctrl Pts',(0.136019262424063,-0.0643322181611298,
0.248548407079752));
#17145=CARTESIAN_POINT('Ctrl Pts',(0.127812719278849,0.0793963653730636,
0.256487396717058));
#17146=CARTESIAN_POINT('Ctrl Pts',(0.00260239121171357,0.150443017797356,
0.264426386354363));
#17147=CARTESIAN_POINT('Ctrl Pts',(-0.124990247656303,0.0837693979610897,
0.272365375991669));
#17148=CARTESIAN_POINT('Ctrl Pts',(-0.138162880936044,-0.0595893646165358,
0.280304365628975));
#17149=CARTESIAN_POINT('Ctrl Pts',(-0.0248568656394851,-0.148398147813718,
0.288243355266281));
#17150=CARTESIAN_POINT('Ctrl Pts',(0.111203906597776,-0.101358597076653,
0.296182344903586));
#17151=CARTESIAN_POINT('Ctrl Pts',(0.145465123646218,0.0384678027257296,
0.304121334540892));
#17152=CARTESIAN_POINT('Ctrl Pts',(0.0465629893725541,0.143079565503422,
0.312060324178198));
#17153=CARTESIAN_POINT('Ctrl Pts',(-0.0949643705016135,0.116711791945748,
0.319999313815503));
#17154=CARTESIAN_POINT('Ctrl Pts',(-0.149558357514911,-0.0164976283567656,
0.327938303452809));
#17155=CARTESIAN_POINT('Ctrl Pts',(-0.0672419181269484,-0.134604600554976,
0.335877293090115));
#17156=CARTESIAN_POINT('Ctrl Pts',(0.0766298889166206,-0.12949028600085,
0.343816282727421));
#17157=CARTESIAN_POINT('Ctrl Pts',(0.150352284446295,-0.00583648916182633,
0.351755272364726));
#17158=CARTESIAN_POINT('Ctrl Pts',(0.0864374678803939,0.123160213504125,
0.359694262002032));
#17159=CARTESIAN_POINT('Ctrl Pts',(-0.0566049265834532,0.139412181427728,
0.367633251639338));
#17160=CARTESIAN_POINT('Ctrl Pts',(-0.147829390149123,0.0280418517950267,
0.375572241276644));
#17161=CARTESIAN_POINT('Ctrl Pts',(-0.103726178443039,-0.108998871322406,
0.383511230913949));
#17162=CARTESIAN_POINT('Ctrl Pts',(0.0353312408083745,-0.146258597924691,
0.391450220551255));
#17163=CARTESIAN_POINT('Ctrl Pts',(0.142045330507792,-0.0496286018832686,
0.399389210188561));
#17164=CARTESIAN_POINT('Ctrl Pts',(0.118726655129599,0.0924329779120693,
0.407328199825866));
#17165=CARTESIAN_POINT('Ctrl Pts',(-0.0132781361506635,0.1498785012746,
0.415267189463172));
#17166=CARTESIAN_POINT('Ctrl Pts',(-0.133127703795094,0.0701205285647604,
0.423206179100478));
#17167=CARTESIAN_POINT('Ctrl Pts',(-0.131107982452518,-0.0738279823724454,
0.431145168737783));
#17168=CARTESIAN_POINT('Ctrl Pts',(-0.00906788859151817,-0.150192035209753,
0.439084158375089));
#17169=CARTESIAN_POINT('Ctrl Pts',(0.121273235812024,-0.0890655731449414,
0.447023148012395));
#17170=CARTESIAN_POINT('Ctrl Pts',(0.14059702422731,0.0535943170716914,
0.4549621376497));
#17171=CARTESIAN_POINT('Ctrl Pts',(0.031213872705855,0.14719228306762,0.462901127287006));
#17172=CARTESIAN_POINT('Ctrl Pts',(-0.106743440051405,0.106045801661112,
0.470840116924312));
#17173=CARTESIAN_POINT('Ctrl Pts',(-0.146984449047318,-0.0321783433727119,
0.478779106561618));
#17174=CARTESIAN_POINT('Ctrl Pts',(-0.0526712684425847,-0.140945420374714,
0.486718096198923));
#17175=CARTESIAN_POINT('Ctrl Pts',(0.0898588486235595,-0.120686624644175,
0.49465708583623));
#17176=CARTESIAN_POINT('Ctrl Pts',(0.150129348203927,0.0100525047535443,
0.502596075473534));
#17177=CARTESIAN_POINT('Ctrl Pts',(0.0729667185397875,0.131589254992538,
0.510535065110842));
#17178=CARTESIAN_POINT('Ctrl Pts',(-0.0709919412117167,0.132665060686482,
0.518474054748145));
#17179=CARTESIAN_POINT('Ctrl Pts',(-0.149962344179375,0.0122950954523496,
0.526413044385453));
#17180=CARTESIAN_POINT('Ctrl Pts',(-0.0916524986414713,-0.119330187030486,
0.534352034022757));
#17181=CARTESIAN_POINT('Ctrl Pts',(0.0505589280467443,-0.141716861518734,
0.542291023660064));
#17182=CARTESIAN_POINT('Ctrl Pts',(0.146487121137799,-0.0343714617774037,
0.550230013297369));
#17183=CARTESIAN_POINT('Ctrl Pts',(0.108316394245265,0.104438655591022,
0.558169002934674));
#17184=CARTESIAN_POINT('Ctrl Pts',(-0.0290105681715044,0.147642341414387,
0.566107992571982));
#17185=CARTESIAN_POINT('Ctrl Pts',(-0.139780343651344,0.0556895822633619,
0.574046982209285));
#17186=CARTESIAN_POINT('Ctrl Pts',(-0.122590794290966,-0.0872431727934394,
0.581985971846593));
#17187=CARTESIAN_POINT('Ctrl Pts',(0.00682222554696161,-0.150310782322966,
0.589924961483898));
#17188=CARTESIAN_POINT('Ctrl Pts',(0.129989965454297,-0.0757791721064987,
0.597863951121203));
#17189=CARTESIAN_POINT('Ctrl Pts',(0.134160800782372,0.0681230766876274,
0.60580294075851));
#17190=CARTESIAN_POINT('Ctrl Pts',(0.015516617634347,0.149663317553585,
0.613741930395814));
#17191=CARTESIAN_POINT('Ctrl Pts',(-0.117331965534667,0.0941970482962578,
0.621680920033121));
#17192=CARTESIAN_POINT('Ctrl Pts',(-0.142771175541451,-0.0475001629309618,
0.629619909670426));
#17193=CARTESIAN_POINT('Ctrl Pts',(-0.0375131590877193,-0.145714230393655,
0.637558899307733));
#17194=CARTESIAN_POINT('Ctrl Pts',(0.102085583566124,-0.110536906379362,
0.645497888945037));
#17195=CARTESIAN_POINT('Ctrl Pts',(0.148231970847143,0.0258293798362968,
0.653436878582344));
#17196=CARTESIAN_POINT('Ctrl Pts',(0.0586821478180281,0.138550639014834,
0.661375868219649));
#17197=CARTESIAN_POINT('Ctrl Pts',(-0.0845871597882484,0.124438283670714,
0.669314857856955));
#17198=CARTESIAN_POINT('Ctrl Pts',(-0.150422719745043,-0.00358879206139753,
0.67725384749426));
#17199=CARTESIAN_POINT('Ctrl Pts',(-0.078556588917505,-0.128330574617282,
0.685192837131567));
#17200=CARTESIAN_POINT('Ctrl Pts',(0.065222715229363,-0.135594511179713,
0.693131826768872));
#17201=CARTESIAN_POINT('Ctrl Pts',(0.149295093588351,-0.0187309656558678,
0.701070816406178));
#17202=CARTESIAN_POINT('Ctrl Pts',(0.0966980456281902,0.11527949520901,
0.709009806043483));
#17203=CARTESIAN_POINT('Ctrl Pts',(-0.044419435954706,0.14375947882982,
0.716948795680789));
#17204=CARTESIAN_POINT('Ctrl Pts',(-0.144873968183829,0.0406375120624596,
0.724887785318095));
#17205=CARTESIAN_POINT('Ctrl Pts',(-0.112706311402131,-0.099685311927494,
0.732826774955401));
#17206=CARTESIAN_POINT('Ctrl Pts',(0.0226362492002416,-0.148753064728429,
0.740765764592706));
#17207=CARTESIAN_POINT('Ctrl Pts',(0.137256875023267,-0.0616475814838108,
0.748704754230013));
#17208=CARTESIAN_POINT('Ctrl Pts',(0.126228238590478,0.0818920376245527,
0.756643743867318));
#17209=CARTESIAN_POINT('Ctrl Pts',(-0.000353699285724532,0.150465108715513,
0.764582733504624));
#17210=CARTESIAN_POINT('Ctrl Pts',(-0.126611849706441,0.0812976848247803,
0.772521723141928));
#17211=CARTESIAN_POINT('Ctrl Pts',(-0.136965528997667,-0.0622921978288208,
0.780460712779236));
#17212=CARTESIAN_POINT('Ctrl Pts',(-0.0219366533522686,-0.148857842533265,
0.788399702416541));
#17213=CARTESIAN_POINT('Ctrl Pts',(0.113173725020093,-0.0991543342927188,
0.796338692053846));
#17214=CARTESIAN_POINT('Ctrl Pts',(0.144681314438483,0.0413181715024817,
0.804277681691154));
#17215=CARTESIAN_POINT('Ctrl Pts',(0.0437430761464933,0.143966723006387,
0.812216671328456));
#17216=CARTESIAN_POINT('Ctrl Pts',(-0.0972389504488157,0.114823606281847,
0.820155660965765));
#17217=CARTESIAN_POINT('Ctrl Pts',(-0.149205382128735,-0.0194326526180533,
0.828094650603069));
#17218=CARTESIAN_POINT('Ctrl Pts',(-0.0645845121824554,-0.135899649852787,
0.836033640240376));
#17219=CARTESIAN_POINT('Ctrl Pts',(0.0791590524011713,-0.127959831458565,
0.843972629877681));
#17220=CARTESIAN_POINT('Ctrl Pts',(0.150437929635691,-0.00288155702400619,
0.851911619514986));
#17221=CARTESIAN_POINT('Ctrl Pts',(0.0840011924733913,0.12483458538003,
0.859850609152293));
#17222=CARTESIAN_POINT('Ctrl Pts',(-0.0593328794206009,0.138273220341526,
0.867789598789597));
#17223=CARTESIAN_POINT('Ctrl Pts',(-0.148351766552825,0.0251321985630355,
0.875728588426904));
#17224=CARTESIAN_POINT('Ctrl Pts',(-0.1015647786165,-0.111015628577859,
0.883667578064211));
#17225=CARTESIAN_POINT('Ctrl Pts',(0.0381978034543637,-0.145536256153639,
0.891606567701514));
#17226=CARTESIAN_POINT('Ctrl Pts',(0.142992914329196,-0.046828415471795,
0.899545557338823));
#17227=CARTESIAN_POINT('Ctrl Pts',(0.116887812080083,0.0947476302135675,
0.907484546976125));
#17228=CARTESIAN_POINT('Ctrl Pts',(-0.0162200712834111,0.149588713917584,
0.915423536613434));
#17229=CARTESIAN_POINT('Ctrl Pts',(-0.134479591021026,0.067491582014154,
0.923362526250738));
#17230=CARTESIAN_POINT('Ctrl Pts',(-0.129632261667175,-0.0763894677230377,
0.931301515888044));
#17231=CARTESIAN_POINT('Ctrl Pts',(-0.00611548103612966,-0.150341195071919,
0.93924050552535));
#17232=CARTESIAN_POINT('Ctrl Pts',(0.122999603362204,-0.0866658618874593,
0.947179495162656));
#17233=CARTESIAN_POINT('Ctrl Pts',(0.139516980595786,0.0563461282555487,
0.95511848479996));
#17234=CARTESIAN_POINT('Ctrl Pts',(0.0283161238170646,0.147777099632969,
0.963057474437267));
#17235=CARTESIAN_POINT('Ctrl Pts',(-0.108806203685475,0.103928264122473,
0.970996464074573));
#17236=CARTESIAN_POINT('Ctrl Pts',(-0.146323908690103,-0.0350597745230392,
0.978935453711877));
#17237=CARTESIAN_POINT('Ctrl Pts',(-0.049892103521326,-0.14195299239598,
0.986874443349185));
#17238=CARTESIAN_POINT('Ctrl Pts',(0.0922125030920605,-0.118897974404329,
0.994813432986488));
#17239=CARTESIAN_POINT('Ctrl Pts',(0.149902882860231,0.0129999905441286,
1.0027524226238));
#17240=CARTESIAN_POINT('Ctrl Pts',(0.0703674468853664,0.132997355096976,
1.0106914122611));
#17241=CARTESIAN_POINT('Ctrl Pts',(-0.0735845641169637,0.131244755962562,
1.01863040189841));
#17242=CARTESIAN_POINT('Ctrl Pts',(-0.150174949749745,0.00934657753497952,
1.02656939153571));
#17243=CARTESIAN_POINT('Ctrl Pts',(-0.0892904610481016,-0.121107752063083,
1.03450838117302));
#17244=CARTESIAN_POINT('Ctrl Pts',(0.0533333252681307,-0.140696234703703,
1.04244737081032));
#17245=CARTESIAN_POINT('Ctrl Pts',(0.147134107472884,-0.031486957015783,
1.05038636044763));
#17246=CARTESIAN_POINT('Ctrl Pts',(0.106243698045146,0.106546471877992,
1.05832535008494));
#17247=CARTESIAN_POINT('Ctrl Pts',(-0.0319055355867657,0.147043907874068,
1.06626433972224));
#17248=CARTESIAN_POINT('Ctrl Pts',(-0.14084743801815,0.0529327237885883,
1.07420332935955));
#17249=CARTESIAN_POINT('Ctrl Pts',(-0.120853163849259,-0.0896347412088629,
1.08214231899685));
#17250=CARTESIAN_POINT('Ctrl Pts',(0.00977389921538986,-0.150147743699608,
1.09008130863416));
#17251=CARTESIAN_POINT('Ctrl Pts',(0.13145362739741,-0.0732107771302755,
1.09802029827146));
#17252=CARTESIAN_POINT('Ctrl Pts',(0.132796568802552,0.0707456384395876,
1.10595928790877));
#17253=CARTESIAN_POINT('Ctrl Pts',(0.0125733526121963,0.149939270533256,
1.11389827754607));
#17254=CARTESIAN_POINT('Ctrl Pts',(-0.119159906186493,0.0918737764630459,
1.12183726718338));
#17255=CARTESIAN_POINT('Ctrl Pts',(-0.141810437433163,-0.0502958634379693,
1.12977625682069));
#17256=CARTESIAN_POINT('Ctrl Pts',(-0.0346432321137694,-0.146423087362162,
1.13771524645799));
#17257=CARTESIAN_POINT('Ctrl Pts',(0.104237477950025,-0.108510009835838,
1.1456542360953));
#17258=CARTESIAN_POINT('Ctrl Pts',(0.147695920811486,0.0287365450185451,
1.1535932257326));
#17259=CARTESIAN_POINT('Ctrl Pts',(0.0559488704325515,0.139676762352502,
1.16153221536991));
#17260=CARTESIAN_POINT('Ctrl Pts',(-0.0870155364008756,0.12275247642644,
1.16947120500722));
#17261=CARTESIAN_POINT('Ctrl Pts',(-0.150323183223479,-0.00654328889139735,
1.17741019464452));
#17262=CARTESIAN_POINT('Ctrl Pts',(-0.0760202581255566,-0.129849121670035,
1.18534918428183));
#17263=CARTESIAN_POINT('Ctrl Pts',(0.0678740032777675,-0.134286982701248,
1.19328817391913));
#17264=CARTESIAN_POINT('Ctrl Pts',(0.149634266389533,-0.0157943143574443,
1.20122716355644));
#17265=CARTESIAN_POINT('Ctrl Pts',(0.0944146137277022,0.117156966325547,
1.20916615319374));
#17266=CARTESIAN_POINT('Ctrl Pts',(-0.047235147145783,0.142859073628774,
1.21710514283105));
#17267=CARTESIAN_POINT('Ctrl Pts',(-0.145644368043342,0.037783489796601,
1.22504413246835));
#17268=CARTESIAN_POINT('Ctrl Pts',(-0.11072615165767,-0.101880289472715,
1.23298312210566));
#17269=CARTESIAN_POINT('Ctrl Pts',(0.0255542680118797,-0.148279646041953,
1.24092211174296));
#17270=CARTESIAN_POINT('Ctrl Pts',(0.138441506664824,-0.0589391489276913,
1.24886110138027));
#17271=CARTESIAN_POINT('Ctrl Pts',(0.124595033982396,0.0843560996663564,
1.25680009101758));
#17272=CARTESIAN_POINT('Ctrl Pts',(-0.00330965325590636,0.150429120316621,
1.26473908065488));
#17273=CARTESIAN_POINT('Ctrl Pts',(-0.128184579763139,0.0787945908985174,
1.27267807029219));
#17274=CARTESIAN_POINT('Ctrl Pts',(-0.135715308561414,-0.0649709863423027,
1.2806170599295));
#17275=CARTESIAN_POINT('Ctrl Pts',(-0.0190079735469551,-0.149260078337129,
1.2885560495668));
#17276=CARTESIAN_POINT('Ctrl Pts',(0.115099858543875,-0.0969117980795561,
1.29649503920411));
#17277=CARTESIAN_POINT('Ctrl Pts',(0.143841658454547,0.0441525915281748,
1.30443402884141));
#17278=CARTESIAN_POINT('Ctrl Pts',(0.0409062781470196,0.144798309552134,
1.31237301847872));
#17279=CARTESIAN_POINT('Ctrl Pts',(-0.0994759962839106,0.112891098884786,
1.32031200811602));
#17280=CARTESIAN_POINT('Ctrl Pts',(-0.148794813708878,-0.0223601759313527,
1.32825099775333));
#17281=CARTESIAN_POINT('Ctrl Pts',(-0.0619021766503053,-0.13714224202644,
1.33618998739064));
#17282=CARTESIAN_POINT('Ctrl Pts',(0.0816576604940555,-0.126379984705639,
1.34412897702794));
#17283=CARTESIAN_POINT('Ctrl Pts',(0.150465506209006,7.4487583413377E-5,
1.35206796666525));
#17284=CARTESIAN_POINT('Ctrl Pts',(0.0815324923277053,0.126460770918471,
1.36000695630255));
#17285=CARTESIAN_POINT('Ctrl Pts',(-0.062037929094705,0.137080886684378,
1.36794594593986));
#17286=CARTESIAN_POINT('Ctrl Pts',(-0.148816880822527,0.0222128430196456,
1.37588493557716));
#17287=CARTESIAN_POINT('Ctrl Pts',(-0.0993641722043223,-0.112989531455785,
1.38382392521447));
#17288=CARTESIAN_POINT('Ctrl Pts',(0.0410496166270677,-0.144757742348562,
1.39176291485178));
#17289=CARTESIAN_POINT('Ctrl Pts',(0.143885312916173,-0.0440101443352923,
1.39970190448908));
#17290=CARTESIAN_POINT('Ctrl Pts',(0.115003831846793,0.0970256929337524,
1.40764089412639));
#17291=CARTESIAN_POINT('Ctrl Pts',(-0.0191557100743377,0.149241218055048,
1.41557988376369));
#17292=CARTESIAN_POINT('Ctrl Pts',(-0.135779636557791,0.0648365220611291,
1.423518873401));
#17293=CARTESIAN_POINT('Ctrl Pts',(-0.128106375355825,-0.0789213496179777,
1.4314578630383));
#17294=CARTESIAN_POINT('Ctrl Pts',(-0.00316095527563228,-0.150432546011701,
1.43939685267561));
#17295=CARTESIAN_POINT('Ctrl Pts',(0.12467895337041,-0.0842322751882648,
1.44733584231291));
#17296=CARTESIAN_POINT('Ctrl Pts',(0.138382210043398,0.0590753877074232,
1.45527483195022));
#17297=CARTESIAN_POINT('Ctrl Pts',(0.0254091034322018,0.148306397458819,
1.46321382158753));
#17298=CARTESIAN_POINT('Ctrl Pts',(-0.110830116988615,0.101767718932792,
1.47115281122483));
#17299=CARTESIAN_POINT('Ctrl Pts',(-0.145600909330124,-0.0379221829034233,
1.47909180086214));
#17300=CARTESIAN_POINT('Ctrl Pts',(-0.0471050325108872,-0.142916194795756,
1.48703079049945));
#17301=CARTESIAN_POINT('Ctrl Pts',(0.0945521370959566,-0.117043625665234,
1.49496978013675));
#17302=CARTESIAN_POINT('Ctrl Pts',(0.14957741911039,0.0159047428854941,
1.50290876977406));
#17303=CARTESIAN_POINT('Ctrl Pts',(0.0678206238522695,0.134426714629862,
1.51084775941136));
#17304=CARTESIAN_POINT('Ctrl Pts',(-0.0763126473618499,0.129627546381738,
1.51878674904867));
#17305=CARTESIAN_POINT('Ctrl Pts',(-0.125385920115907,0.0477050348167321,
1.52407940880687));
#17306=CARTESIAN_POINT('Ctrl Pts',(-0.127184992207234,0.00540996832206346,
1.52672573868597));
#17307=CARTESIAN_POINT('Ctrl Pts',(0.0684664424539414,-0.095829519891843,
-1.38777878078145E-17));
#17308=CARTESIAN_POINT('Ctrl Pts',(0.100334321247169,-0.0730611673843044,
0.00264632987910189));
#17309=CARTESIAN_POINT('Ctrl Pts',(0.139021564822767,0.00636891437108143,
0.00793898963730573));
#17310=CARTESIAN_POINT('Ctrl Pts',(0.0699018669780613,0.120491966796142,
0.0158779792746114));
#17311=CARTESIAN_POINT('Ctrl Pts',(-0.0632645460347191,0.123954346655885,
0.0238169689119172));
#17312=CARTESIAN_POINT('Ctrl Pts',(-0.138486976988987,0.0141253725679007,
0.0317559585492228));
#17313=CARTESIAN_POINT('Ctrl Pts',(-0.0869496735326521,-0.108728403071097,
0.0396949481865287));
#17314=CARTESIAN_POINT('Ctrl Pts',(0.0441923146003338,-0.131999388615902,
0.0476339378238343));
#17315=CARTESIAN_POINT('Ctrl Pts',(0.134874939024977,-0.034459980695041,
0.0555729274611401));
#17316=CARTESIAN_POINT('Ctrl Pts',(0.102091080224759,0.094638871230671,
0.0635119170984456));
#17317=CARTESIAN_POINT('Ctrl Pts',(-0.0241513666277066,0.137095110112719,
0.0714509067357516));
#17318=CARTESIAN_POINT('Ctrl Pts',(-0.128284260007319,0.0540539703915629,
0.0793898963730571));
#17319=CARTESIAN_POINT('Ctrl Pts',(-0.114982038412656,-0.0784718756714057,
0.0873288860103631));
#17320=CARTESIAN_POINT('Ctrl Pts',(0.00357853460314598,-0.139161043603659,
0.0952678756476685));
#17321=CARTESIAN_POINT('Ctrl Pts',(0.118863112008681,-0.0724583686054966,
0.103206865284975));
#17322=CARTESIAN_POINT('Ctrl Pts',(0.125336705278751,0.0605752693714656,
0.11114585492228));
#17323=CARTESIAN_POINT('Ctrl Pts',(0.0170731091066207,0.138156245709763,
0.119084844559586));
#17324=CARTESIAN_POINT('Ctrl Pts',(-0.106819734848208,0.0892647286947484,
0.127023834196891));
#17325=CARTESIAN_POINT('Ctrl Pts',(-0.132926439498961,-0.0413425724611633,
0.134962823834197));
#17326=CARTESIAN_POINT('Ctrl Pts',(-0.0373480950846616,-0.134103559412242,
0.142901813471503));
#17327=CARTESIAN_POINT('Ctrl Pts',(0.0924198687735613,-0.104101940294199,
0.150840803108809));
#17328=CARTESIAN_POINT('Ctrl Pts',(0.137583777756591,0.0211978768359354,
0.158779792746114));
#17329=CARTESIAN_POINT('Ctrl Pts',(0.0567991668878991,0.127092487218924,
0.16671878238342));
#17330=CARTESIAN_POINT('Ctrl Pts',(-0.075981188277068,0.116642637502503,
0.174657772020726));
#17331=CARTESIAN_POINT('Ctrl Pts',(-0.139205973057234,-0.000585553717998882,
0.182596761658032));
#17332=CARTESIAN_POINT('Ctrl Pts',(-0.0749972298318695,-0.11727771015962,
0.190535751295337));
#17333=CARTESIAN_POINT('Ctrl Pts',(0.0578663373665801,-0.126610160769685,
0.198474740932643));
#17334=CARTESIAN_POINT('Ctrl Pts',(0.13775723856723,-0.0200396862227523,
0.206413730569949));
#17335=CARTESIAN_POINT('Ctrl Pts',(0.091540828968026,0.104875747581476,
0.214352720207254));
#17336=CARTESIAN_POINT('Ctrl Pts',(-0.0384749358425138,0.133784622116252,
0.22229170984456));
#17337=CARTESIAN_POINT('Ctrl Pts',(-0.133269533752038,0.0402228439430644,
0.230230699481866));
#17338=CARTESIAN_POINT('Ctrl Pts',(-0.106065007067505,-0.0901601911982067,
0.238169689119172));
#17339=CARTESIAN_POINT('Ctrl Pts',(0.0182347644767634,-0.138007750384372,
0.246108678756477));
#17340=CARTESIAN_POINT('Ctrl Pts',(0.125841858853055,-0.0595186723796334,
0.254047668393783));
#17341=CARTESIAN_POINT('Ctrl Pts',(0.118249355954961,0.073455671106145,
0.261986658031089));
#17342=CARTESIAN_POINT('Ctrl Pts',(0.00240767183786234,0.139186381940956,
0.269925647668394));
#17343=CARTESIAN_POINT('Ctrl Pts',(-0.115638070838342,0.0775014991741366,
0.277864637305701));
#17344=CARTESIAN_POINT('Ctrl Pts',(-0.12782508485658,-0.0551306945617612,
0.285803626943006));
#17345=CARTESIAN_POINT('Ctrl Pts',(-0.0229969941138309,-0.137294515779738,
0.293742616580312));
#17346=CARTESIAN_POINT('Ctrl Pts',(0.102883268653204,-0.0937746172089793,
0.301681606217617));
#17347=CARTESIAN_POINT('Ctrl Pts',(0.134580950019115,0.0355895166223291,
0.309620595854923));
#17348=CARTESIAN_POINT('Ctrl Pts',(0.0430789950773988,0.13237388709478,
0.317559585492229));
#17349=CARTESIAN_POINT('Ctrl Pts',(-0.0878588274613298,0.107979036106918,
0.325498575129534));
#17350=CARTESIAN_POINT('Ctrl Pts',(-0.1383679148179,-0.0152632221501787,
0.33343756476684));
#17351=CARTESIAN_POINT('Ctrl Pts',(-0.0622106591311991,-0.12453304658572,
0.341376554404146));
#17352=CARTESIAN_POINT('Ctrl Pts',(0.0708961914151981,-0.119801401679107,
0.349315544041452));
#17353=CARTESIAN_POINT('Ctrl Pts',(0.1391024375543,-0.00539978406154301,
0.357254533678757));
#17354=CARTESIAN_POINT('Ctrl Pts',(0.0799699354250877,0.113944965792994,
0.365193523316063));
#17355=CARTESIAN_POINT('Ctrl Pts',(-0.0523695618881846,0.128980908622551,
0.373132512953369));
#17356=CARTESIAN_POINT('Ctrl Pts',(-0.136768314413298,0.0259436692471295,
0.381071502590675));
#17357=CARTESIAN_POINT('Ctrl Pts',(-0.0959650484377783,-0.100843221288265,
0.38901049222798));
#17358=CARTESIAN_POINT('Ctrl Pts',(0.0326876424682324,-0.135315053971568,
0.396949481865287));
#17359=CARTESIAN_POINT('Ctrl Pts',(0.13141703692502,-0.0459152284901983,
0.404888471502591));
#17360=CARTESIAN_POINT('Ctrl Pts',(0.109843140674695,0.0855168418978295,
0.412827461139898));
#17361=CARTESIAN_POINT('Ctrl Pts',(-0.0122846228212416,0.13866410438033,
0.420766450777203));
#17362=CARTESIAN_POINT('Ctrl Pts',(-0.123166656044517,0.0648738825743514,
0.428705440414509));
#17363=CARTESIAN_POINT('Ctrl Pts',(-0.121298056821252,-0.0683039326309071,
0.436644430051815));
#17364=CARTESIAN_POINT('Ctrl Pts',(-0.00838939967687663,-0.138954178686792,
0.44458341968912));
#17365=CARTESIAN_POINT('Ctrl Pts',(0.11219917790857,-0.0824013973067221,
0.452522409326426));
#17366=CARTESIAN_POINT('Ctrl Pts',(0.13007709763057,0.0495842159710775,
0.460461398963732));
#17367=CARTESIAN_POINT('Ctrl Pts',(0.0288783492374893,0.136178877755608,
0.468400388601037));
#17368=CARTESIAN_POINT('Ctrl Pts',(-0.0987565487199846,0.0981111099028881,
0.476339378238344));
#17369=CARTESIAN_POINT('Ctrl Pts',(-0.135986594552616,-0.0297706550724338,
0.484278367875649));
#17370=CARTESIAN_POINT('Ctrl Pts',(-0.0487302328423073,-0.130399425645183,
0.492217357512954));
#17371=CARTESIAN_POINT('Ctrl Pts',(0.0831353173341669,-0.111656458896056,
0.50015634715026));
#17372=CARTESIAN_POINT('Ctrl Pts',(0.13889618212661,0.00930034365552528,
0.508095336787567));
#17373=CARTESIAN_POINT('Ctrl Pts',(0.0675071113591811,0.12174331898465,
0.516034326424871));
#17374=CARTESIAN_POINT('Ctrl Pts',(-0.0656800932930844,0.122738629397884,
0.523973316062178));
#17375=CARTESIAN_POINT('Ctrl Pts',(-0.138741673886299,0.0113751364249866,
0.531912305699483));
#17376=CARTESIAN_POINT('Ctrl Pts',(-0.0847947606245053,-0.110401514355972,
0.539851295336789));
#17377=CARTESIAN_POINT('Ctrl Pts',(0.0467759446245483,-0.131113145053959,
0.547790284974095));
#17378=CARTESIAN_POINT('Ctrl Pts',(0.135526478334676,-0.031799677225719,
0.555729274611401));
#17379=CARTESIAN_POINT('Ctrl Pts',(0.100211809365564,0.0966242157284558,
0.563668264248707));
#17380=CARTESIAN_POINT('Ctrl Pts',(-0.0268399031138932,0.136595261273209,
0.571607253886012));
#17381=CARTESIAN_POINT('Ctrl Pts',(-0.129321523751272,0.0515227066069736,
0.579546243523318));
#17382=CARTESIAN_POINT('Ctrl Pts',(-0.113418152377209,-0.0807153548762533,
0.587485233160623));
#17383=CARTESIAN_POINT('Ctrl Pts',(0.00631176444456456,-0.139064040754811,
0.595424222797929));
#17384=CARTESIAN_POINT('Ctrl Pts',(0.120263693490807,-0.0701091280034811,
0.603363212435234));
#17385=CARTESIAN_POINT('Ctrl Pts',(0.124122453355413,0.0630258865426945,
0.611302202072541));
#17386=CARTESIAN_POINT('Ctrl Pts',(0.0143556138404206,0.138465021405133,
0.619241191709845));
#17387=CARTESIAN_POINT('Ctrl Pts',(-0.108552806291007,0.0871489187988374,
0.627180181347153));
#17388=CARTESIAN_POINT('Ctrl Pts',(-0.132088571872698,-0.043946046262323,
0.635119170984457));
#17389=CARTESIAN_POINT('Ctrl Pts',(-0.0347063025259737,-0.134811417789573,
0.643058160621763));
#17390=CARTESIAN_POINT('Ctrl Pts',(0.0944472082050275,-0.102266175560326,
0.65099715025907));
#17391=CARTESIAN_POINT('Ctrl Pts',(0.137140772714236,0.0238967416356601,
0.658936139896373));
#17392=CARTESIAN_POINT('Ctrl Pts',(0.054291358674537,0.128183829614862,
0.666875129533682));
#17393=CARTESIAN_POINT('Ctrl Pts',(-0.0782580734018908,0.115127406593233,
0.674814119170985));
#17394=CARTESIAN_POINT('Ctrl Pts',(-0.139167602654929,-0.00332026696803425,
0.682753108808293));
#17395=CARTESIAN_POINT('Ctrl Pts',(-0.0726787294560835,-0.118728463672822,
0.690692098445597));
#17396=CARTESIAN_POINT('Ctrl Pts',(0.0603425395611779,-0.125448888878168,
0.698631088082904));
#17397=CARTESIAN_POINT('Ctrl Pts',(0.138124349154501,-0.0173294538893964,
0.706570077720209));
#17398=CARTESIAN_POINT('Ctrl Pts',(0.0894627833767505,0.106653908470079,
0.714509067357515));
#17399=CARTESIAN_POINT('Ctrl Pts',(-0.0410958292974484,0.133002927094911,
0.72244805699482));
#17400=CARTESIAN_POINT('Ctrl Pts',(-0.134034026730954,0.0375968812502473,
0.730387046632127));
#17401=CARTESIAN_POINT('Ctrl Pts',(-0.104273258644039,-0.0922265326964679,
0.738326036269432));
#17402=CARTESIAN_POINT('Ctrl Pts',(0.0209425314183671,-0.137622876656644,
0.746265025906738));
#17403=CARTESIAN_POINT('Ctrl Pts',(0.126986869252672,-0.0570349089493802,
0.754204015544043));
#17404=CARTESIAN_POINT('Ctrl Pts',(0.11678343126468,0.0757646090434518,
0.762143005181349));
#17405=CARTESIAN_POINT('Ctrl Pts',(-0.000327234354877375,0.139206819944772,
0.770081994818654));
#17406=CARTESIAN_POINT('Ctrl Pts',(-0.117138339349379,0.0752147276530931,
0.778020984455961));
#17407=CARTESIAN_POINT('Ctrl Pts',(-0.126717322684213,-0.0576312930030564,
0.785959974093266));
#17408=CARTESIAN_POINT('Ctrl Pts',(-0.0202952816069424,-0.137719814645367,
0.793898963730571));
#17409=CARTESIAN_POINT('Ctrl Pts',(0.104705698854998,-0.0917352845351548,
0.801837953367879));
#17410=CARTESIAN_POINT('Ctrl Pts',(0.133855787965376,0.0382266115373486,
0.809776943005182));
#17411=CARTESIAN_POINT('Ctrl Pts',(0.0404700769297216,0.133194664588195,
0.81771593264249));
#17412=CARTESIAN_POINT('Ctrl Pts',(-0.0899632159395838,0.106232130635072,
0.825654922279794));
#17413=CARTESIAN_POINT('Ctrl Pts',(-0.13804135019805,-0.0179786383510676,
0.833593911917101));
#17414=CARTESIAN_POINT('Ctrl Pts',(-0.059752088941783,-0.125731196083361,
0.841532901554406));
#17415=CARTESIAN_POINT('Ctrl Pts',(0.0732361146625898,-0.118385460722959,
0.849471891191712));
#17416=CARTESIAN_POINT('Ctrl Pts',(0.139181674492094,-0.00266594955618734,
0.857410880829018));
#17417=CARTESIAN_POINT('Ctrl Pts',(0.077715950067195,0.115494055719818,
0.865349870466323));
#17418=CARTESIAN_POINT('Ctrl Pts',(-0.0548934004223171,0.127927168308903,
0.87328886010363));
#17419=CARTESIAN_POINT('Ctrl Pts',(-0.137251604915624,0.0232517257326144,
0.881227849740934));
#17420=CARTESIAN_POINT('Ctrl Pts',(-0.0939653715754795,-0.102709078207047,
0.889166839378241));
#17421=CARTESIAN_POINT('Ctrl Pts',(0.0353397195745277,-0.134646760160997,
0.897105829015547));
#17422=CARTESIAN_POINT('Ctrl Pts',(0.132293719443212,-0.0433245611326863,
0.905044818652852));
#17423=CARTESIAN_POINT('Ctrl Pts',(0.108141885842356,0.0876583043865096,
0.912983808290157));
#17424=CARTESIAN_POINT('Ctrl Pts',(-0.0150064327997127,0.138395999855801,
0.920922797927463));
#17425=CARTESIAN_POINT('Ctrl Pts',(-0.124417390671652,0.0624416423544169,
0.928861787564769));
#17426=CARTESIAN_POINT('Ctrl Pts',(-0.119932754264349,-0.0706737593172073,
0.936800777202075));
#17427=CARTESIAN_POINT('Ctrl Pts',(-0.00565790085648466,-0.139092177922979,
0.944739766839381));
#17428=CARTESIAN_POINT('Ctrl Pts',(0.113796373024222,-0.0801812402497705,
0.952678756476687));
#17429=CARTESIAN_POINT('Ctrl Pts',(0.129077866376032,0.0521301276928276,
0.960617746113992));
#17430=CARTESIAN_POINT('Ctrl Pts',(0.026197419344502,0.13671993644362,0.968556735751298));
#17431=CARTESIAN_POINT('Ctrl Pts',(-0.100664969670515,0.0961520134094621,
0.976495725388603));
#17432=CARTESIAN_POINT('Ctrl Pts',(-0.13537547797311,-0.0324364881732178,
0.98443471502591));
#17433=CARTESIAN_POINT('Ctrl Pts',(-0.0461590140787468,-0.131331607851033,
0.992373704663214));
#17434=CARTESIAN_POINT('Ctrl Pts',(0.0853128637208732,-0.110001641284132,
1.00031269430052));
#17435=CARTESIAN_POINT('Ctrl Pts',(0.138686661656432,0.0120272889735618,
1.00825168393783));
#17436=CARTESIAN_POINT('Ctrl Pts',(0.0651023256631918,0.123046060459907,
1.01619067357513));
#17437=CARTESIAN_POINT('Ctrl Pts',(-0.0680787277209358,0.121424596492465,
1.02412966321244));
#17438=CARTESIAN_POINT('Ctrl Pts',(-0.138938371616466,0.00864723620724691,
1.03206865284975));
#17439=CARTESIAN_POINT('Ctrl Pts',(-0.0826094583655966,-0.112046076191904,
1.04000764248705));
#17440=CARTESIAN_POINT('Ctrl Pts',(0.0493427524230464,-0.130168884856471,
1.04794663212436));
#17441=CARTESIAN_POINT('Ctrl Pts',(0.136125055048066,-0.0291310004912345,
1.05588562176166));
#17442=CARTESIAN_POINT('Ctrl Pts',(0.0982941990358779,0.0985743183458784,
1.06382461139897));
#17443=CARTESIAN_POINT('Ctrl Pts',(-0.0295182596522469,0.136041604476578,
1.07176360103627));
#17444=CARTESIAN_POINT('Ctrl Pts',(-0.130308774647192,0.0489721252490281,
1.07970259067358));
#17445=CARTESIAN_POINT('Ctrl Pts',(-0.111810537096203,-0.0829279783650712,
1.08764158031088));
#17446=CARTESIAN_POINT('Ctrl Pts',(0.00904258428980543,-0.13891320121148,
1.09558056994819));
#17447=CARTESIAN_POINT('Ctrl Pts',(0.121617839487272,-0.067732908692211,
1.1035195595855));
#17448=CARTESIAN_POINT('Ctrl Pts',(0.122860297649024,0.0654522196953821,
1.1114585492228));
#17449=CARTESIAN_POINT('Ctrl Pts',(0.0116325734791967,0.138720326685422,
1.11939753886011));
#17450=CARTESIAN_POINT('Ctrl Pts',(-0.110243974478508,0.0849994817198388,
1.12733652849741));
#17451=CARTESIAN_POINT('Ctrl Pts',(-0.131199719314147,-0.0465325633653302,
1.13527551813472));
#17452=CARTESIAN_POINT('Ctrl Pts',(-0.0320511128216771,-0.13546723577438,
1.14321450777202));
#17453=CARTESIAN_POINT('Ctrl Pts',(0.0964380908528195,-0.100390938007982,
1.15115349740933));
#17454=CARTESIAN_POINT('Ctrl Pts',(0.136644831685568,0.0265863832644056,
1.15909248704664));
#17455=CARTESIAN_POINT('Ctrl Pts',(0.0517625939920979,0.129225692742072,
1.16703147668394));
#17456=CARTESIAN_POINT('Ctrl Pts',(-0.0805047509788913,0.113567736929491,
1.17497046632125));
#17457=CARTESIAN_POINT('Ctrl Pts',(-0.139075513779617,-0.00605369873671642,
1.18290945595855));
#17458=CARTESIAN_POINT('Ctrl Pts',(-0.0703321751825429,-0.12013338809653,
1.19084844559586));
#17459=CARTESIAN_POINT('Ctrl Pts',(0.0627954496153871,-0.124239193932754,
1.19878743523316));
#17460=CARTESIAN_POINT('Ctrl Pts',(0.138438143943654,-0.0146125323915816,
1.20672642487047));
#17461=CARTESIAN_POINT('Ctrl Pts',(0.0873502052771435,0.108390901091839,
1.21466541450777));
#17462=CARTESIAN_POINT('Ctrl Pts',(-0.043700859820065,0.132169893139269,
1.22260440414508));
#17463=CARTESIAN_POINT('Ctrl Pts',(-0.134746782767514,0.0349564062120582,
1.23054339378239));
#17464=CARTESIAN_POINT('Ctrl Pts',(-0.102441260891455,-0.0942572748833364,
1.23848238341969));
#17465=CARTESIAN_POINT('Ctrl Pts',(0.0236422145726536,-0.137184880695923,
1.246421373057));
#17466=CARTESIAN_POINT('Ctrl Pts',(0.128082862902196,-0.0545291301253663,
1.2543603626943));
#17467=CARTESIAN_POINT('Ctrl Pts',(0.115272428336817,0.0780443019497631,
1.26229935233161));
#17468=CARTESIAN_POINT('Ctrl Pts',(-0.00306201423577413,0.139173524314926,
1.27023834196891));
#17469=CARTESIAN_POINT('Ctrl Pts',(-0.118593392628464,0.0728989233548558,
1.27817733160622));
#17470=CARTESIAN_POINT('Ctrl Pts',(-0.125560647806918,-0.06010964584811,
1.28611632124353));
#17471=CARTESIAN_POINT('Ctrl Pts',(-0.0175857351491984,-0.138091953858251,
1.29405531088083));
#17472=CARTESIAN_POINT('Ctrl Pts',(0.106487712804436,-0.089660542174548,
1.30199430051814));
#17473=CARTESIAN_POINT('Ctrl Pts',(0.133078957772855,0.0408489510387311,
1.30993329015544));
#17474=CARTESIAN_POINT('Ctrl Pts',(0.0378455373822902,0.133964029124136,
1.31787227979275));
#17475=CARTESIAN_POINT('Ctrl Pts',(-0.0920328787300654,0.104444219726284,
1.32581126943006));
#17476=CARTESIAN_POINT('Ctrl Pts',(-0.137661501842601,-0.0206871148492911,
1.33375025906736));
#17477=CARTESIAN_POINT('Ctrl Pts',(-0.0572704544775333,-0.126880813469472,
1.34168924870467));
#17478=CARTESIAN_POINT('Ctrl Pts',(0.0755477687720905,-0.116923823242002,
1.34962823834197));
#17479=CARTESIAN_POINT('Ctrl Pts',(0.13920718769651,6.89141801743488E-5,
1.35756722797928));
#17480=CARTESIAN_POINT('Ctrl Pts',(0.0754319660950179,0.116998564767658,
1.36550621761658));
#17481=CARTESIAN_POINT('Ctrl Pts',(-0.0573960494825499,0.126824048933643,
1.37344520725389));
#17482=CARTESIAN_POINT('Ctrl Pts',(-0.13768191782304,0.0205508058651932,
1.38138419689119));
#17483=CARTESIAN_POINT('Ctrl Pts',(-0.0919294216917856,-0.104535287252199,
1.3893231865285));
#17484=CARTESIAN_POINT('Ctrl Pts',(0.0379781508110965,-0.133926497290667,
1.39726217616581));
#17485=CARTESIAN_POINT('Ctrl Pts',(0.133119345865688,-0.0407171622080862,
1.40520116580311));
#17486=CARTESIAN_POINT('Ctrl Pts',(0.106398871137127,0.0897659150453452,
1.41314015544042));
#17487=CARTESIAN_POINT('Ctrl Pts',(-0.0177224175491345,0.138074504763813,
1.42107914507772));
#17488=CARTESIAN_POINT('Ctrl Pts',(-0.125620162573399,0.0599852426217579,
1.42901813471503));
#17489=CARTESIAN_POINT('Ctrl Pts',(-0.118521039729242,-0.0730161975746823,
1.43695712435233));
#17490=CARTESIAN_POINT('Ctrl Pts',(-0.00292444232197888,-0.139176693688359,
1.44489611398964));
#17491=CARTESIAN_POINT('Ctrl Pts',(0.115350068603298,-0.0779297424218237,
1.45283510362695));
#17492=CARTESIAN_POINT('Ctrl Pts',(0.128028003046829,0.0546551750765237,
1.46077409326425));
#17493=CARTESIAN_POINT('Ctrl Pts',(0.0235079116789307,0.137209630484779,
1.46871308290156));
#17494=CARTESIAN_POINT('Ctrl Pts',(-0.102537447198224,0.0941531272373115,
1.47665207253886));
#17495=CARTESIAN_POINT('Ctrl Pts',(-0.134706575776555,-0.0350847218495708,
1.48459106217617));
#17496=CARTESIAN_POINT('Ctrl Pts',(-0.0435804807853106,-0.132222740314769,
1.49253005181348));
#17497=CARTESIAN_POINT('Ctrl Pts',(0.0874774386997331,-0.108286040948335,
1.50046904145078));
#17498=CARTESIAN_POINT('Ctrl Pts',(0.138385550162814,0.0147146982980264,
1.50840803108809));
#17499=CARTESIAN_POINT('Ctrl Pts',(0.0627460642121078,0.124368470664037,
1.51634702072539));
#17500=CARTESIAN_POINT('Ctrl Pts',(-0.0706026869052757,0.119928391791904,
1.5242860103627));
#17501=CARTESIAN_POINT('Ctrl Pts',(-0.116004137797729,0.0441355889673283,
1.5295786701209));
#17502=CARTESIAN_POINT('Ctrl Pts',(-0.117668597464313,0.00500517689812487,
1.532225));
#17503=CARTESIAN_POINT('',(0.0684664424539461,-0.0958295198918396,0.));
#17504=CARTESIAN_POINT('Ctrl Pts',(0.0684664424539414,-0.095829519891843,
-1.38777878078145E-17));
#17505=CARTESIAN_POINT('Ctrl Pts',(0.100334321247169,-0.0730611673843044,
0.00264632987910189));
#17506=CARTESIAN_POINT('Ctrl Pts',(0.139021564822767,0.00636891437108143,
0.00793898963730573));
#17507=CARTESIAN_POINT('Ctrl Pts',(0.0699018669780613,0.120491966796142,
0.0158779792746114));
#17508=CARTESIAN_POINT('Ctrl Pts',(-0.0632645460347191,0.123954346655885,
0.0238169689119172));
#17509=CARTESIAN_POINT('Ctrl Pts',(-0.11596266760442,0.0470121293552651,
0.0293787386625077));
#17510=CARTESIAN_POINT('Ctrl Pts',(-0.117944740497024,0.00404481602818191,
0.0322941785339964));
#17511=CARTESIAN_POINT('Ctrl Pts',(-0.117917485785546,7.60014832213644E-5,
0.0325632885263832));
#17512=CARTESIAN_POINT('Ctrl Pts',(0.0635546915223951,0.132092229195826,
-2.16840434497101E-19));
#17513=CARTESIAN_POINT('Ctrl Pts',(0.0668114782730532,0.13015255741457,
-1.00603861447787E-18));
#17514=CARTESIAN_POINT('Ctrl Pts',(0.0699821360194518,0.12808121947321,
-2.9262196004085E-17));
#17515=CARTESIAN_POINT('Ctrl Pts',(0.0730575207853233,0.125877721325919,
-2.71050543121376E-17));
#17516=CARTESIAN_POINT('Ctrl Pts',(0.0789281193465506,0.121671466161783,
-2.36378102375718E-17));
#17517=CARTESIAN_POINT('Ctrl Pts',(0.0844522091809674,0.11698398814956,
1.43782932504085E-18));
#17518=CARTESIAN_POINT('Ctrl Pts',(0.0895990070394484,0.111875963994554,
9.97465998686664E-18));
#17519=CARTESIAN_POINT('Ctrl Pts',(0.0928865546640729,0.108613183302742,
1.54276111490851E-17));
#17520=CARTESIAN_POINT('Ctrl Pts',(0.0960206821069302,0.105176950779614,
-2.53636710091701E-17));
#17521=CARTESIAN_POINT('Ctrl Pts',(0.098978417360439,0.101599719103904,
-1.56125112837913E-17));
#17522=CARTESIAN_POINT('Ctrl Pts',(0.103148772110026,0.0965558852815647,
-1.86354736740503E-18));
#17523=CARTESIAN_POINT('Ctrl Pts',(0.106976174326278,0.0912251680483688,
1.1337629845105E-17));
#17524=CARTESIAN_POINT('Ctrl Pts',(0.110435561611279,0.0856523061447448,
2.03830008427275E-17));
#17525=CARTESIAN_POINT('Ctrl Pts',(0.112407683932559,0.0824753373788608,
2.55395723911076E-17));
#17526=CARTESIAN_POINT('Ctrl Pts',(0.114261188142284,0.0792174064057451,
2.29308760465575E-17));
#17527=CARTESIAN_POINT('Ctrl Pts',(0.115986535786665,0.0758936579718971,
2.08166817117217E-17));
#17528=CARTESIAN_POINT('Ctrl Pts',(0.120573220307724,0.0670577659456877,
1.51962825639422E-17));
#17529=CARTESIAN_POINT('Ctrl Pts',(0.124235263225439,0.0578042025119142,
2.52358375750583E-18));
#17530=CARTESIAN_POINT('Ctrl Pts',(0.126883306113679,0.0482911783993335,
1.30104260698261E-17));
#17531=CARTESIAN_POINT('Ctrl Pts',(0.128478610866444,0.0425600882242624,
1.93281898253259E-17));
#17532=CARTESIAN_POINT('Ctrl Pts',(0.129704960854084,0.0367345196138549,
-5.78096029915021E-19));
#17533=CARTESIAN_POINT('Ctrl Pts',(0.130533291754837,0.0308494671050701,
0.));
#17534=CARTESIAN_POINT('Ctrl Pts',(0.131003715791213,0.0275072397983871,
3.2831114661813E-19));
#17535=CARTESIAN_POINT('Ctrl Pts',(0.131345346899704,0.0241444941465381,
-1.7128612844445E-18));
#17536=CARTESIAN_POINT('Ctrl Pts',(0.131551728167405,0.0207857616715298,
2.60208521396521E-18));
#17537=CARTESIAN_POINT('Ctrl Pts',(0.131851321606701,0.0159100565018035,
8.86587880453295E-18));
#17538=CARTESIAN_POINT('Ctrl Pts',(0.131867617692795,0.0110341713389591,
-1.68111772803455E-17));
#17539=CARTESIAN_POINT('Ctrl Pts',(0.131586936334964,0.0061777758930637,
-6.93889390390723E-18));
#17540=CARTESIAN_POINT('Ctrl Pts',(0.131099036368572,-0.00226395031615145,
9.98510028643051E-18));
#17541=CARTESIAN_POINT('Ctrl Pts',(0.129715139118287,-0.0106479390144509,
1.03491660509995E-17));
#17542=CARTESIAN_POINT('Ctrl Pts',(0.127493709984164,-0.018859987399606,
1.04083408558608E-17));
#17543=CARTESIAN_POINT('Ctrl Pts',(0.126553994220251,-0.0223338732882013,
1.04333731632617E-17));
#17544=CARTESIAN_POINT('Ctrl Pts',(0.125463061762623,-0.0257782540966497,
1.75224609115742E-17));
#17545=CARTESIAN_POINT('Ctrl Pts',(0.124232565886791,-0.0291638780753137,
1.73472347597681E-17));
#17546=CARTESIAN_POINT('Ctrl Pts',(0.12170396813588,-0.0361211392462112,
1.69871551674183E-17));
#17547=CARTESIAN_POINT('Ctrl Pts',(0.118582485980247,-0.0428512226170345,
-6.45748389186585E-19));
#17548=CARTESIAN_POINT('Ctrl Pts',(0.114911168983798,-0.0492778939609075,
3.46944695195361E-18));
#17549=CARTESIAN_POINT('Ctrl Pts',(0.112347970921096,-0.0537647937721124,
6.34254691478841E-18));
#17550=CARTESIAN_POINT('Ctrl Pts',(0.109516356061708,-0.0581036184196785,
-1.05628593522785E-17));
#17551=CARTESIAN_POINT('Ctrl Pts',(0.106427098863261,-0.0622637901458048,
-1.21430643318376E-17));
#17552=CARTESIAN_POINT('Ctrl Pts',(0.104287070791936,-0.0651456752410043,
-1.32377232732828E-17));
#17553=CARTESIAN_POINT('Ctrl Pts',(0.102021590876101,-0.067943056099314,
-1.03088264066386E-17));
#17554=CARTESIAN_POINT('Ctrl Pts',(0.0996491962474235,-0.0706287444932102,
-1.04083408558608E-17));
#17555=CARTESIAN_POINT('Ctrl Pts',(0.0938611946766418,-0.0771810981592459,
-1.06511292104842E-17));
#17556=CARTESIAN_POINT('Ctrl Pts',(0.0874218747326319,-0.0830961188460978,
9.460259835177E-18));
#17557=CARTESIAN_POINT('Ctrl Pts',(0.0803902102994179,-0.0882260767030795,
2.94902990916057E-17));
#17558=CARTESIAN_POINT('Ctrl Pts',(0.0765868618375105,-0.091000813397402,
4.03243227742548E-17));
#17559=CARTESIAN_POINT('Ctrl Pts',(0.0726097989303321,-0.0935451549285004,
-2.49510848448888E-18));
#17560=CARTESIAN_POINT('Ctrl Pts',(0.0684664424539416,-0.0958295198918429,
0.));
#17561=CARTESIAN_POINT('Ctrl Pts',(-0.00156962371674571,0.146072546381438,
1.50365));
#17562=CARTESIAN_POINT('Ctrl Pts',(0.0218361081466035,0.146362061217761,
1.50238307892777));
#17563=CARTESIAN_POINT('Ctrl Pts',(0.0452966847593804,0.141345883428421,
1.50111615785553));
#17564=CARTESIAN_POINT('Ctrl Pts',(0.0660179268768178,0.130913916311315,
1.4998492367833));
#17565=CARTESIAN_POINT('Ctrl Pts',(0.109300214423576,0.109123745727819,
1.4972029069042));
#17566=CARTESIAN_POINT('Ctrl Pts',(0.140630685714559,0.0637042888941242,
1.49455657702509));
#17567=CARTESIAN_POINT('Ctrl Pts',(0.145752650840527,0.0155206226173656,
1.49191024714599));
#17568=CARTESIAN_POINT('Ctrl Pts',(0.150874615966495,-0.0326630436593903,
1.48926391726689));
#17569=CARTESIAN_POINT('Ctrl Pts',(0.129788074927449,-0.0836109193792113,
1.48661758738779));
#17570=CARTESIAN_POINT('Ctrl Pts',(0.0921021927661857,-0.114042242015571,
1.48397125750869));
#17571=CARTESIAN_POINT('Ctrl Pts',(0.0544163106049216,-0.144473564651931,
1.48132492762959));
#17572=CARTESIAN_POINT('Ctrl Pts',(0.000131087321441313,-0.154388334204831,
1.47867859775048));
#17573=CARTESIAN_POINT('Ctrl Pts',(-0.0458840977328367,-0.139228052523514,
1.47603226787138));
#17574=CARTESIAN_POINT('Ctrl Pts',(-0.0918992827871148,-0.124067770842196,
1.47338593799228));
#17575=CARTESIAN_POINT('Ctrl Pts',(-0.129644429612189,-0.0838324379266627,
1.47073960811318));
#17576=CARTESIAN_POINT('Ctrl Pts',(-0.141854649713415,-0.0369491035797489,
1.46809327823408));
#17577=CARTESIAN_POINT('Ctrl Pts',(-0.14497337938942,-0.0249741805295802,
1.46741735368415));
#17578=CARTESIAN_POINT('Ctrl Pts',(-0.146426231435716,-0.0125655473306973,
1.46674142913422));
#17579=CARTESIAN_POINT('Ctrl Pts',(-0.14631473222987,-0.000131398079681141,
1.46606550458429));
#17580=CARTESIAN_POINT('Origin',(0.,0.,-0.0924367114736175));
#17581=CARTESIAN_POINT('',(-0.0684664424539507,-0.0958295198918364,0.));
#17582=CARTESIAN_POINT('Ctrl Pts',(-0.0686146973663072,-0.0959584553529141,
8.16675286424706E-17));
#17583=CARTESIAN_POINT('Ctrl Pts',(-0.0391968190522335,-0.116741470120209,
0.00244290680874874));
#17584=CARTESIAN_POINT('Ctrl Pts',(0.0436301113039178,-0.130476273073809,
0.0075332029917574));
#17585=CARTESIAN_POINT('Ctrl Pts',(0.134092250525203,-0.0374520209666004,
0.0152708885490261));
#17586=CARTESIAN_POINT('Ctrl Pts',(0.104134301645602,0.0924305194826295,
0.023213056671806));
#17587=CARTESIAN_POINT('Ctrl Pts',(-0.0212379681243542,0.137589894578696,
0.0311552247945861));
#17588=CARTESIAN_POINT('Ctrl Pts',(-0.106685947947232,0.0723488109778776,
0.0375631097285225));
#17589=CARTESIAN_POINT('Ctrl Pts',(-0.117663533972591,0.0165813593984342,
0.041323605288199));
#17590=CARTESIAN_POINT('Ctrl Pts',(-0.117600989619072,5.04992496179954E-5,
0.0424367114736154));
#17591=CARTESIAN_POINT('Origin',(0.,0.,0.));
#17592=CARTESIAN_POINT('Ctrl Pts',(-0.0510216505388318,0.106149619882943,
-0.0164977839420939));
#17593=CARTESIAN_POINT('Ctrl Pts',(-0.0863355867949722,0.0891756983861136,
-0.0138503945678339));
#17594=CARTESIAN_POINT('Ctrl Pts',(-0.13808023131828,0.0175094743621551,
-0.00855561581931395));
#17595=CARTESIAN_POINT('Ctrl Pts',(-0.0894531427980795,-0.106808298616542,
-0.000613447696533924));
#17596=CARTESIAN_POINT('Ctrl Pts',(0.0412394829729132,-0.132934609947913,
0.00732872042624606));
#17597=CARTESIAN_POINT('Ctrl Pts',(0.134092250525203,-0.0374520209666004,
0.0152708885490261));
#17598=CARTESIAN_POINT('Ctrl Pts',(0.104134301645602,0.0924305194826295,
0.023213056671806));
#17599=CARTESIAN_POINT('Ctrl Pts',(-0.0212379681243542,0.137589894578696,
0.0311552247945861));
#17600=CARTESIAN_POINT('Ctrl Pts',(-0.127145335141994,0.0567276974868182,
0.039097392917366));
#17601=CARTESIAN_POINT('Ctrl Pts',(-0.116579117211717,-0.0761160149501382,
0.0470395610401461));
#17602=CARTESIAN_POINT('Ctrl Pts',(0.000787973702835166,-0.139222729671589,
0.054981729162926));
#17603=CARTESIAN_POINT('Ctrl Pts',(0.117431922513572,-0.0747907597173192,
0.0629238972857061));
#17604=CARTESIAN_POINT('Ctrl Pts',(0.126496838785129,0.0581591461343325,
0.070866065408486));
#17605=CARTESIAN_POINT('Ctrl Pts',(0.0196773008918215,0.137828289815661,
0.0788082335312661));
#17606=CARTESIAN_POINT('Ctrl Pts',(-0.105168479521776,0.0912330920368172,
0.0867504016540459));
#17607=CARTESIAN_POINT('Ctrl Pts',(-0.133669226619255,-0.0389412707994331,
0.0946925697768262));
#17608=CARTESIAN_POINT('Ctrl Pts',(-0.0397151780004399,-0.133441281507892,
0.102634737899606));
#17609=CARTESIAN_POINT('Ctrl Pts',(0.0906220264938673,-0.105695447092796,
0.110576906022386));
#17610=CARTESIAN_POINT('Ctrl Pts',(0.137940159127448,0.0188783162799928,
0.118519074145166));
#17611=CARTESIAN_POINT('Ctrl Pts',(0.0588909273047484,0.126157580947307,
0.126461242267946));
#17612=CARTESIAN_POINT('Ctrl Pts',(-0.074108440039672,0.117863552156501,
0.134403410390726));
#17613=CARTESIAN_POINT('Ctrl Pts',(-0.139216864956951,0.00159439502933392,
0.142345578513506));
#17614=CARTESIAN_POINT('Ctrl Pts',(-0.0767883381764272,-0.116135388594389,
0.150287746636286));
#17615=CARTESIAN_POINT('Ctrl Pts',(0.0559861945572589,-0.127473226882309,
0.158229914759066));
#17616=CARTESIAN_POINT('Ctrl Pts',(0.137471621702818,-0.0220324926503626,
0.166172082881846));
#17617=CARTESIAN_POINT('Ctrl Pts',(0.0930189202108026,0.103592267873211,
0.174114251004626));
#17618=CARTESIAN_POINT('Ctrl Pts',(-0.0366486683060043,0.134315868829211,
0.182056419127406));
#17619=CARTESIAN_POINT('Ctrl Pts',(-0.132742311638566,0.0419923350165386,
0.189998587250186));
#17620=CARTESIAN_POINT('Ctrl Pts',(-0.107230360350792,-0.0888004916405464,
0.197940755372966));
#17621=CARTESIAN_POINT('Ctrl Pts',(0.0165156171993534,-0.138242945169174,
0.205882923495746));
#17622=CARTESIAN_POINT('Ctrl Pts',(0.125131592687617,-0.061040658666823,
0.213825091618526));
#17623=CARTESIAN_POINT('Ctrl Pts',(0.119114174013628,0.0720811421096423,
0.221767259741306));
#17624=CARTESIAN_POINT('Ctrl Pts',(0.0039759348809324,0.139169211541763,
0.229709427864086));
#17625=CARTESIAN_POINT('Ctrl Pts',(-0.114804669066963,0.0787639858025777,
0.237651595986866));
#17626=CARTESIAN_POINT('Ctrl Pts',(-0.128412401817242,-0.0537971426620367,
0.245593764109646));
#17627=CARTESIAN_POINT('Ctrl Pts',(-0.024381182195918,-0.137074561658528,
0.253535932232426));
#17628=CARTESIAN_POINT('Ctrl Pts',(0.101985705091022,-0.094777599970642,
0.261478100355206));
#17629=CARTESIAN_POINT('Ctrl Pts',(0.134923209124943,0.0343453801629359,
0.269420268477986));
#17630=CARTESIAN_POINT('Ctrl Pts',(0.0442571924125319,0.132004463632409,
0.277362436600766));
#17631=CARTESIAN_POINT('Ctrl Pts',(-0.0869529592639067,0.108733897080731,
0.285304604723546));
#17632=CARTESIAN_POINT('Ctrl Pts',(-0.138505267237684,-0.0141480898545381,
0.293246772846326));
#17633=CARTESIAN_POINT('Ctrl Pts',(-0.0631725212350128,-0.124068972994571,
0.301188940969106));
#17634=CARTESIAN_POINT('Ctrl Pts',(0.0700327441786229,-0.12032993078169,
0.309131109091886));
#17635=CARTESIAN_POINT('Ctrl Pts',(0.139080821187468,-0.00635631000930847,
0.317073277214666));
#17636=CARTESIAN_POINT('Ctrl Pts',(0.0807165776729536,0.11344034374014,
0.325015445337446));
#17637=CARTESIAN_POINT('Ctrl Pts',(-0.0515923433190751,0.129313988454311,
0.332957613460226));
#17638=CARTESIAN_POINT('Ctrl Pts',(-0.136637377548019,0.026722734813544,
0.340899781583006));
#17639=CARTESIAN_POINT('Ctrl Pts',(-0.0965085366518414,-0.100349289247285,
0.348841949705786));
#17640=CARTESIAN_POINT('Ctrl Pts',(0.0320320385160992,-0.135491055083419,
0.356784117828566));
#17641=CARTESIAN_POINT('Ctrl Pts',(0.131227975626944,-0.0465090949381858,
0.364726285951346));
#17642=CARTESIAN_POINT('Ctrl Pts',(0.110205605501345,0.0850799742312894,
0.372668454074126));
#17643=CARTESIAN_POINT('Ctrl Pts',(-0.0117764211155082,0.138727046407055,
0.380610622196906));
#17644=CARTESIAN_POINT('Ctrl Pts',(-0.122970036152848,0.065285892102983,
0.388552790319686));
#17645=CARTESIAN_POINT('Ctrl Pts',(-0.121510464882371,-0.0679638464419502,
0.396494958442466));
#17646=CARTESIAN_POINT('Ctrl Pts',(-0.00873482453528946,-0.138951719454826,
0.404437126565246));
#17647=CARTESIAN_POINT('Ctrl Pts',(0.112042812448737,-0.0826455423945668,
0.412379294688026));
#17648=CARTESIAN_POINT('Ctrl Pts',(0.130177722634257,0.049372441998279,
0.420321462810806));
#17649=CARTESIAN_POINT('Ctrl Pts',(0.0290564652212241,0.136160197297018,
0.428263630933586));
#17650=CARTESIAN_POINT('Ctrl Pts',(-0.098683499418539,0.098211223603141,
0.436205799056366));
#17651=CARTESIAN_POINT('Ctrl Pts',(-0.136019240449831,-0.0297093205335648,
0.444147967179146));
#17652=CARTESIAN_POINT('Ctrl Pts',(-0.0487473834415776,-0.130413074907061,
0.452090135301926));
#17653=CARTESIAN_POINT('Ctrl Pts',(0.0831820848081396,-0.111645054821459,
0.460032303424706));
#17654=CARTESIAN_POINT('Ctrl Pts',(0.138908217753341,0.00940130521287039,
0.467974471547486));
#17655=CARTESIAN_POINT('Ctrl Pts',(0.0673801526530663,0.121835103839429,
0.475916639670265));
#17656=CARTESIAN_POINT('Ctrl Pts',(-0.0658750545035054,0.12265543075329,
0.483858807793047));
#17657=CARTESIAN_POINT('Ctrl Pts',(-0.138781944133385,0.0111107822259715,
0.491800975915825));
#17658=CARTESIAN_POINT('Ctrl Pts',(-0.084550315326251,-0.110612484274364,
0.499743144038607));
#17659=CARTESIAN_POINT('Ctrl Pts',(0.0471380885036503,-0.131003351527116,
0.507685312161385));
#17660=CARTESIAN_POINT('Ctrl Pts',(0.135643160584381,-0.031381690295376,
0.515627480284167));
#17661=CARTESIAN_POINT('Ctrl Pts',(0.0998851624184703,0.0969888232104648,
0.523569648406945));
#17662=CARTESIAN_POINT('Ctrl Pts',(-0.0273779061153799,0.136507610615132,
0.531511816529727));
#17663=CARTESIAN_POINT('Ctrl Pts',(-0.129560000008381,0.0509714027366644,
0.539453984652505));
#17664=CARTESIAN_POINT('Ctrl Pts',(-0.113051823689188,-0.0812598465397498,
0.547396152775286));
#17665=CARTESIAN_POINT('Ctrl Pts',(0.00702343738442799,-0.139048728244533,
0.555338320898066));
#17666=CARTESIAN_POINT('Ctrl Pts',(0.12066450826877,-0.0694546898587181,
0.563280489020846));
#17667=CARTESIAN_POINT('Ctrl Pts',(0.123764493242992,0.063766979789076,
0.571222657143626));
#17668=CARTESIAN_POINT('Ctrl Pts',(0.0134834875971477,0.13857154491934,
0.579164825266405));
#17669=CARTESIAN_POINT('Ctrl Pts',(-0.109149777898995,0.0864303389077871,
0.587106993389186));
#17670=CARTESIAN_POINT('Ctrl Pts',(-0.131790633456927,-0.0448899368693808,
0.595049161511966));
#17671=CARTESIAN_POINT('Ctrl Pts',(-0.0336977294021144,-0.135086418755761,
0.602991329634746));
#17672=CARTESIAN_POINT('Ctrl Pts',(0.0952657566843092,-0.101529863106778,
0.610933497757526));
#17673=CARTESIAN_POINT('Ctrl Pts',(0.136956022624868,0.025038477707157,
0.618875665880307));
#17674=CARTESIAN_POINT('Ctrl Pts',(0.0531805018142573,0.128669000640787,
0.626817834003085));
#17675=CARTESIAN_POINT('Ctrl Pts',(-0.0793138220987445,0.114425500318782,
0.634760002125867));
#17676=CARTESIAN_POINT('Ctrl Pts',(-0.139148536750765,-0.00464351367351466,
0.642702170248646));
#17677=CARTESIAN_POINT('Ctrl Pts',(-0.0715088964667609,-0.119458592094588,
0.650644338371427));
#17678=CARTESIAN_POINT('Ctrl Pts',(0.0616402393688536,-0.124837327709565,
0.658586506494205));
#17679=CARTESIAN_POINT('Ctrl Pts',(0.138320583400205,-0.0158522461166236,
0.666528674616987));
#17680=CARTESIAN_POINT('Ctrl Pts',(0.0882850628235238,0.107655121482266,
0.674470842739765));
#17681=CARTESIAN_POINT('Ctrl Pts',(-0.0426286451686149,0.132539337972556,
0.682413010862546));
#17682=CARTESIAN_POINT('Ctrl Pts',(-0.13449013477919,0.0360039045964495,
0.690355178985326));
#17683=CARTESIAN_POINT('Ctrl Pts',(-0.103144844235522,-0.0935148042116587,
0.698297347108106));
#17684=CARTESIAN_POINT('Ctrl Pts',(0.022691720100341,-0.137364345221032,
0.706239515230886));
#17685=CARTESIAN_POINT('Ctrl Pts',(0.127740337615313,-0.0553740340325759,
0.714181683353665));
#17686=CARTESIAN_POINT('Ctrl Pts',(0.115765682611161,0.077344581120379,
0.722123851476446));
#17687=CARTESIAN_POINT('Ctrl Pts',(-0.00226223072526165,0.139207614056346,
0.730066019599226));
#17688=CARTESIAN_POINT('Ctrl Pts',(-0.118217708309552,0.0735421711751344,
0.738008187722006));
#17689=CARTESIAN_POINT('Ctrl Pts',(-0.125873620115675,-0.059495455776806,
0.745950355844786));
#17690=CARTESIAN_POINT('Ctrl Pts',(-0.0182163644075178,-0.138029133036789,
0.753892523967566));
#17691=CARTESIAN_POINT('Ctrl Pts',(0.106128952536144,-0.0901139441634624,
0.761834692090347));
#17692=CARTESIAN_POINT('Ctrl Pts',(0.133249245915149,0.0403548753208232,
0.769776860213125));
#17693=CARTESIAN_POINT('Ctrl Pts',(0.0382995408207276,0.133854483197375,
0.777719028335907));
#17694=CARTESIAN_POINT('Ctrl Pts',(-0.0917364783268051,0.104729633071593,
0.785661196458685));
#17695=CARTESIAN_POINT('Ctrl Pts',(-0.137732458880487,-0.0203383202317681,
0.793603364581467));
#17696=CARTESIAN_POINT('Ctrl Pts',(-0.0575513573065257,-0.126774282767806,
0.801545532704245));
#17697=CARTESIAN_POINT('Ctrl Pts',(0.0753527000357912,-0.117071978271622,
0.809487700827026));
#17698=CARTESIAN_POINT('Ctrl Pts',(0.139225942868322,-0.000119714417332432,
0.817429868949805));
#17699=CARTESIAN_POINT('Ctrl Pts',(0.0755539188089132,0.116942220141962,
0.825372037072586));
#17700=CARTESIAN_POINT('Ctrl Pts',(-0.0573332568284509,0.12687306712048,
0.833314205195366));
#17701=CARTESIAN_POINT('Ctrl Pts',(-0.13769727914169,0.0205751504512258,
0.841256373318145));
#17702=CARTESIAN_POINT('Ctrl Pts',(-0.0919164475821765,-0.104571717796869,
0.849198541440926));
#17703=CARTESIAN_POINT('Ctrl Pts',(0.0380692928980519,-0.133920149482284,
0.857140709563706));
#17704=CARTESIAN_POINT('Ctrl Pts',(0.133179650076608,-0.0405839661022353,
0.865082877686486));
#17705=CARTESIAN_POINT('Ctrl Pts',(0.106283765719693,0.0899312995767124,
0.873025045809266));
#17706=CARTESIAN_POINT('Ctrl Pts',(-0.0179789669825735,0.138060255849953,
0.880967213932046));
#17707=CARTESIAN_POINT('Ctrl Pts',(-0.125771118879347,0.0597118342956578,
0.888909382054826));
#17708=CARTESIAN_POINT('Ctrl Pts',(-0.118344004924669,-0.0733387619032726,
0.896851550177606));
#17709=CARTESIAN_POINT('Ctrl Pts',(-0.00250162451743248,-0.139203517821528,
0.904793718300386));
#17710=CARTESIAN_POINT('Ctrl Pts',(0.115632500949424,-0.0775435504945224,
0.912735886423165));
#17711=CARTESIAN_POINT('Ctrl Pts',(0.127835376168433,0.0551542754370876,
0.920678054545947));
#17712=CARTESIAN_POINT('Ctrl Pts',(0.0229279137899797,0.137325118854324,
0.928620222668725));
#17713=CARTESIAN_POINT('Ctrl Pts',(-0.102983873094174,0.0936920454555137,
0.936562390791507));
#17714=CARTESIAN_POINT('Ctrl Pts',(-0.134551852288801,-0.0357725669300891,
0.944504558914285));
#17715=CARTESIAN_POINT('Ctrl Pts',(-0.0428565117498991,-0.132465832952297,
0.952446727037066));
#17716=CARTESIAN_POINT('Ctrl Pts',(0.0880997963686447,-0.107806787258123,
0.960388895159846));
#17717=CARTESIAN_POINT('Ctrl Pts',(0.138347640177547,0.0156143509765511,
0.968331063282625));
#17718=CARTESIAN_POINT('Ctrl Pts',(0.061854832590724,0.124731139593481,
0.976273231405407));
#17719=CARTESIAN_POINT('Ctrl Pts',(-0.0713033562375951,0.119581390225944,
0.984215399528185));
#17720=CARTESIAN_POINT('Ctrl Pts',(-0.139140345480169,0.00488280234845834,
0.992157567650966));
#17721=CARTESIAN_POINT('Ctrl Pts',(-0.0795104838321055,-0.114288934109561,
1.00009973577375));
#17722=CARTESIAN_POINT('Ctrl Pts',(0.0529591494285269,-0.128760265574912,
1.00804190389653));
#17723=CARTESIAN_POINT('Ctrl Pts',(0.136912761112491,-0.0252739657289669,
1.0159840720193));
#17724=CARTESIAN_POINT('Ctrl Pts',(0.0954402180350474,0.101365883217864,
1.02392624014209));
#17725=CARTESIAN_POINT('Ctrl Pts',(-0.0334653697086341,0.135144169424284,
1.03186840826486));
#17726=CARTESIAN_POINT('Ctrl Pts',(-0.131713240771149,0.0451165125500212,
1.03981057638765));
#17727=CARTESIAN_POINT('Ctrl Pts',(-0.109298251871946,-0.0862425048155002,
1.04775274451043));
#17728=CARTESIAN_POINT('Ctrl Pts',(0.0132451643780021,-0.13859452774087,
1.05569491263321));
#17729=CARTESIAN_POINT('Ctrl Pts',(0.123654649330263,-0.0639797248987874,
1.06363708075599));
#17730=CARTESIAN_POINT('Ctrl Pts',(0.120783771971213,0.0692470788374567,
1.07157924887876));
#17731=CARTESIAN_POINT('Ctrl Pts',(0.00726255089817806,0.139036444335888,
1.07952141700155));
#17732=CARTESIAN_POINT('Ctrl Pts',(-0.112911912907791,0.0814541430660127,
1.08746358512433));
#17733=CARTESIAN_POINT('Ctrl Pts',(-0.129647464608677,-0.0507485213543897,
1.09540575324711));
#17734=CARTESIAN_POINT('Ctrl Pts',(-0.0276126195379174,-0.136460326620484,
1.10334792136989));
#17735=CARTESIAN_POINT('Ctrl Pts',(0.0997182217817603,-0.0971604536002107,
1.11129008949267));
#17736=CARTESIAN_POINT('Ctrl Pts',(0.135696927507188,0.0311483765905046,
1.11923225761545));
#17737=CARTESIAN_POINT('Ctrl Pts',(0.0473633069609982,0.130922093830007,
1.12717442573822));
#17738=CARTESIAN_POINT('Ctrl Pts',(-0.0843599685788644,0.110757722983492,
1.13511659386101));
#17739=CARTESIAN_POINT('Ctrl Pts',(-0.138800846271631,-0.0108721006891078,
1.14305876198379));
#17740=CARTESIAN_POINT('Ctrl Pts',(-0.0660858892268601,-0.122541963197144,
1.15100093010657));
#17741=CARTESIAN_POINT('Ctrl Pts',(0.0671705316110708,-0.121950798202395,
1.15894309822935));
#17742=CARTESIAN_POINT('Ctrl Pts',(0.138891844802359,-0.00964017357273747,
1.16688526635212));
#17743=CARTESIAN_POINT('Ctrl Pts',(0.0833739592533277,0.111501840422208,
1.17482743447491));
#17744=CARTESIAN_POINT('Ctrl Pts',(-0.0485230383040216,0.130496713571114,
1.18276960259768));
#17745=CARTESIAN_POINT('Ctrl Pts',(-0.135967947813762,0.0299431906521225,
1.19071177072047));
#17746=CARTESIAN_POINT('Ctrl Pts',(-0.0988522486080867,-0.0980413710850678,
1.19865393884324));
#17747=CARTESIAN_POINT('Ctrl Pts',(0.0288222657999454,-0.136209964735594,
1.20659610696603));
#17748=CARTESIAN_POINT('Ctrl Pts',(0.130092623711363,-0.0495962373069701,
1.21453827508881));
#17749=CARTESIAN_POINT('Ctrl Pts',(0.112184773380136,0.082452738709893,
1.22248044321158));
#17750=CARTESIAN_POINT('Ctrl Pts',(-0.00849585454694533,0.138966535376798,
1.23042261133437));
#17751=CARTESIAN_POINT('Ctrl Pts',(-0.121393406896754,0.0681727090639588,
1.23836477945715));
#17752=CARTESIAN_POINT('Ctrl Pts',(-0.123082127310551,-0.0650743223999996,
1.24630694757992));
#17753=CARTESIAN_POINT('Ctrl Pts',(-0.0120149744006178,-0.138706589206355,
1.25424911570271));
#17754=CARTESIAN_POINT('Ctrl Pts',(0.110059129405696,-0.0852693704304675,
1.26219128382548));
#17755=CARTESIAN_POINT('Ctrl Pts',(0.13130776387206,0.0462833517151888,
1.27013345194827));
#17756=CARTESIAN_POINT('Ctrl Pts',(0.0322649968732001,0.135435768819968,
1.27807562007105));
#17757=CARTESIAN_POINT('Ctrl Pts',(-0.0963358219719167,0.100515107841202,
1.28601778819382));
#17758=CARTESIAN_POINT('Ctrl Pts',(-0.136683130933199,-0.0264877182308561,
1.29395995631661));
#17759=CARTESIAN_POINT('Ctrl Pts',(-0.0518146499729274,-0.129225073214149,
1.30190212443939));
#17760=CARTESIAN_POINT('Ctrl Pts',(0.0805213734929343,-0.11357898534207,
1.30984429256217));
#17761=CARTESIAN_POINT('Ctrl Pts',(0.1390915465469,0.0061171215252809,1.31778646068495));
#17762=CARTESIAN_POINT('Ctrl Pts',(0.0702395735793815,0.120209316621791,
1.32572862880773));
#17763=CARTESIAN_POINT('Ctrl Pts',(-0.0629590648350173,0.124177428154433,
1.33367079693051));
#17764=CARTESIAN_POINT('Ctrl Pts',(-0.138480731711197,0.0143862582011507,
1.34161296505328));
#17765=CARTESIAN_POINT('Ctrl Pts',(-0.0871398218994898,-0.108584202098263,
1.34955513317607));
#17766=CARTESIAN_POINT('Ctrl Pts',(0.0440301174146577,-0.132080378229483,
1.35749730129884));
#17767=CARTESIAN_POINT('Ctrl Pts',(0.13486394497766,-0.0345773583278084,
1.36543946942163));
#17768=CARTESIAN_POINT('Ctrl Pts',(0.102148545386143,0.0946020732301706,
1.3733816375444));
#17769=CARTESIAN_POINT('Ctrl Pts',(-0.0241454188302812,0.137116288461919,
1.38132380566719));
#17770=CARTESIAN_POINT('Ctrl Pts',(-0.128319693277533,0.0540178939468163,
1.38926597378996));
#17771=CARTESIAN_POINT('Ctrl Pts',(-0.114939956470138,-0.0785664351508689,
1.39720814191275));
#17772=CARTESIAN_POINT('Ctrl Pts',(0.00373660876362508,-0.139175849115243,
1.40515031003553));
#17773=CARTESIAN_POINT('Ctrl Pts',(0.118990018389619,-0.0722858665142316,
1.41309247815831));
#17774=CARTESIAN_POINT('Ctrl Pts',(0.125236419206141,0.0608253567263532,
1.42103464628109));
#17775=CARTESIAN_POINT('Ctrl Pts',(0.0167532566496359,0.13821437898841,
1.42897681440387));
#17776=CARTESIAN_POINT('Ctrl Pts',(-0.107077349343502,0.0889846891406984,
1.43691898252665));
#17777=CARTESIAN_POINT('Ctrl Pts',(-0.132814597987359,-0.0417638487589672,
1.44486115064943));
#17778=CARTESIAN_POINT('Ctrl Pts',(-0.0368790902657646,-0.134252921254984,
1.45280331877221));
#17779=CARTESIAN_POINT('Ctrl Pts',(0.0928396680879532,-0.103751556080299,
1.46074548689499));
#17780=CARTESIAN_POINT('Ctrl Pts',(0.137511141307062,0.0217950526079239,
1.46868765501776));
#17781=CARTESIAN_POINT('Ctrl Pts',(0.0562018483347667,0.127378648737854,
1.47662982314055));
#17782=CARTESIAN_POINT('Ctrl Pts',(-0.0765818961642769,0.116263681173923,
1.48457199126332));
#17783=CARTESIAN_POINT('Ctrl Pts',(-0.13923195096087,-0.00134816270381636,
1.49251415938611));
#17784=CARTESIAN_POINT('Ctrl Pts',(-0.0742871760264013,-0.117748889605885,
1.50045632750888));
#17785=CARTESIAN_POINT('Ctrl Pts',(0.0586284551779338,-0.126233948370975,
1.50839849563167));
#17786=CARTESIAN_POINT('Ctrl Pts',(0.137995068118234,-0.019163470063063,
1.51634066375444));
#17787=CARTESIAN_POINT('Ctrl Pts',(0.0906261803825392,0.105639137646141,
1.52428283187723));
#17788=CARTESIAN_POINT('Ctrl Pts',(0.00417072711528833,0.124051375507138,
1.52957761062575));
#17789=CARTESIAN_POINT('Ctrl Pts',(-0.0334019664627544,0.1129391839063,
1.53222500000001));
#17790=CARTESIAN_POINT('Ctrl Pts',(-0.0551480035117261,0.114734422509858,
-0.0109985226280628));
#17791=CARTESIAN_POINT('Ctrl Pts',(-0.093317938433455,0.0963877427684319,
-0.00835113325380276));
#17792=CARTESIAN_POINT('Ctrl Pts',(-0.149247407742026,0.0189255452031589,
-0.00305635450528277));
#17793=CARTESIAN_POINT('Ctrl Pts',(-0.0966876253720675,-0.115446371588928,
0.00488581361749726));
#17794=CARTESIAN_POINT('Ctrl Pts',(0.0445747075563756,-0.143685636564375,
0.0128279817402772));
#17795=CARTESIAN_POINT('Ctrl Pts',(0.144936900801175,-0.0404809362687151,
0.0207701498630572));
#17796=CARTESIAN_POINT('Ctrl Pts',(0.112556116319125,0.0999057960529736,
0.0287123179858373));
#17797=CARTESIAN_POINT('Ctrl Pts',(-0.0229555792165621,0.148717415239805,
0.0366544861086172));
#17798=CARTESIAN_POINT('Ctrl Pts',(-0.137428156769908,0.0613155244327884,
0.0445966542313972));
#17799=CARTESIAN_POINT('Ctrl Pts',(-0.126007400730642,-0.0822718633254329,
0.0525388223541772));
#17800=CARTESIAN_POINT('Ctrl Pts',(0.000851700720621877,-0.150482305134309,
0.0604809904769572));
#17801=CARTESIAN_POINT('Ctrl Pts',(0.126929176276611,-0.0808394286734405,
0.0684231585997372));
#17802=CARTESIAN_POINT('Ctrl Pts',(0.136727213562698,0.0628627408439891,
0.0763653267225173));
#17803=CARTESIAN_POINT('Ctrl Pts',(0.0212686937255662,0.148975090584026,
0.0843074948452972));
#17804=CARTESIAN_POINT('Ctrl Pts',(-0.113673932864549,0.0986115272026031,
0.0922496629680772));
#17805=CARTESIAN_POINT('Ctrl Pts',(-0.144479665027646,-0.0420906285100245,
0.100191831090857));
#17806=CARTESIAN_POINT('Ctrl Pts',(-0.0429271251068198,-0.144233284958223,
0.108133999213637));
#17807=CARTESIAN_POINT('Ctrl Pts',(0.0979510420095061,-0.114243518700172,
0.116076167336417));
#17808=CARTESIAN_POINT('Ctrl Pts',(0.149096007275942,0.0204050915936607,
0.124018335459197));
#17809=CARTESIAN_POINT('Ctrl Pts',(0.0636537044864716,0.136360518400275,
0.131960503581977));
#17810=CARTESIAN_POINT('Ctrl Pts',(-0.0801019266996435,0.127395713772213,
0.139902671704757));
#17811=CARTESIAN_POINT('Ctrl Pts',(-0.15047596611352,0.00172334100814176,
0.147844839827537));
#17812=CARTESIAN_POINT('Ctrl Pts',(-0.0829985603893774,-0.125527785761544,
0.155787007950317));
#17813=CARTESIAN_POINT('Ctrl Pts',(0.0605140527882773,-0.137782566606816,
0.163729176073097));
#17814=CARTESIAN_POINT('Ctrl Pts',(0.148589577098441,-0.0238143605552183,
0.171671344195877));
#17815=CARTESIAN_POINT('Ctrl Pts',(0.100541783424623,0.111970245809892,
0.179613512318657));
#17816=CARTESIAN_POINT('Ctrl Pts',(-0.0396126128240685,0.145178604134651,
0.187555680441437));
#17817=CARTESIAN_POINT('Ctrl Pts',(-0.143477786216001,0.0453884461694337,
0.195497848564217));
#17818=CARTESIAN_POINT('Ctrl Pts',(-0.115902567375552,-0.095982191346566,
0.203440016686997));
#17819=CARTESIAN_POINT('Ctrl Pts',(0.0178513102906219,-0.149423281002214,
0.211382184809777));
#17820=CARTESIAN_POINT('Ctrl Pts',(0.135251553802876,-0.0659772944027704,
0.219324352932557));
#17821=CARTESIAN_POINT('Ctrl Pts',(0.128747479107914,0.07791067196398,0.227266521055337));
#17822=CARTESIAN_POINT('Ctrl Pts',(0.00429748682099232,0.150424458749874,
0.235208689178117));
#17823=CARTESIAN_POINT('Ctrl Pts',(-0.124089444892588,0.0851339876261335,
0.243150857300897));
#17824=CARTESIAN_POINT('Ctrl Pts',(-0.138797696890977,-0.0581479623084488,
0.251093025423677));
#17825=CARTESIAN_POINT('Ctrl Pts',(-0.0263529993083425,-0.148160405002171,
0.259035193546457));
#17826=CARTESIAN_POINT('Ctrl Pts',(0.110233752987369,-0.102442695616748,
0.266977361669237));
#17827=CARTESIAN_POINT('Ctrl Pts',(0.145835062802846,0.0371230472913779,
0.274919529792017));
#17828=CARTESIAN_POINT('Ctrl Pts',(0.0478364728857143,0.142680265085169,
0.282861697914797));
#17829=CARTESIAN_POINT('Ctrl Pts',(-0.0939852406223356,0.117527701960322,
0.290803866037577));
#17830=CARTESIAN_POINT('Ctrl Pts',(-0.14970681824969,-0.01529231023972,
0.298746034160357));
#17831=CARTESIAN_POINT('Ctrl Pts',(-0.0682815703945392,-0.134102995221473,
0.306688202283137));
#17832=CARTESIAN_POINT('Ctrl Pts',(0.0756966107742644,-0.1300615596562,
0.314630370405917));
#17833=CARTESIAN_POINT('Ctrl Pts',(0.150328919865546,-0.00687037371415525,
0.322572538528697));
#17834=CARTESIAN_POINT('Ctrl Pts',(0.0872444944832666,0.122614780370367,
0.330514706651477));
#17835=CARTESIAN_POINT('Ctrl Pts',(-0.0557648508131485,0.139772198940638,
0.338456874774257));
#17836=CARTESIAN_POINT('Ctrl Pts',(-0.147687863823926,0.0288839239377102,
0.346399042897038));
#17837=CARTESIAN_POINT('Ctrl Pts',(-0.104313621021262,-0.10846499275041,
0.354341211019817));
#17838=CARTESIAN_POINT('Ctrl Pts',(0.0346226151823369,-0.146448833047075,
0.362283379142597));
#17839=CARTESIAN_POINT('Ctrl Pts',(0.141840978962514,-0.0502704970123603,
0.370225547265377));
#17840=CARTESIAN_POINT('Ctrl Pts',(0.119118434135606,0.0919607787700563,
0.378167715388157));
#17841=CARTESIAN_POINT('Ctrl Pts',(-0.0127288338612142,0.149946533709345,
0.386109883510937));
#17842=CARTESIAN_POINT('Ctrl Pts',(-0.132915182358376,0.070565859178174,
0.394052051633717));
#17843=CARTESIAN_POINT('Ctrl Pts',(-0.131337568919768,-0.0734603918663599,
0.401994219756497));
#17844=CARTESIAN_POINT('Ctrl Pts',(-0.00944124952954395,-0.150189377088511,
0.409936387879277));
#17845=CARTESIAN_POINT('Ctrl Pts',(0.121104224366159,-0.0893294633566384,
0.417878556002057));
#17846=CARTESIAN_POINT('Ctrl Pts',(0.140705787232781,0.0533654159743681,
0.425820724124838));
#17847=CARTESIAN_POINT('Ctrl Pts',(0.0314063937394313,0.147172091835368,
0.433762892247617));
#17848=CARTESIAN_POINT('Ctrl Pts',(-0.106664482920656,0.106154012011714,
0.441705060370398));
#17849=CARTESIAN_POINT('Ctrl Pts',(-0.147019735166745,-0.032112048430678,
0.449647228493177));
#17850=CARTESIAN_POINT('Ctrl Pts',(-0.052689806088835,-0.14096017351449,
0.457589396615958));
#17851=CARTESIAN_POINT('Ctrl Pts',(0.0899093983958942,-0.120674298270189,
0.465531564738737));
#17852=CARTESIAN_POINT('Ctrl Pts',(0.15014235720654,0.0101616315312987,
0.473473732861518));
#17853=CARTESIAN_POINT('Ctrl Pts',(0.0728294921055832,0.131688462906045,
0.481415900984297));
#17854=CARTESIAN_POINT('Ctrl Pts',(-0.071202669822089,0.132575133389036,
0.489358069107078));
#17855=CARTESIAN_POINT('Ctrl Pts',(-0.150005871264529,0.012009361726732,
0.497300237229857));
#17856=CARTESIAN_POINT('Ctrl Pts',(-0.0913882839399832,-0.119558219045865,
0.505242405352637));
#17857=CARTESIAN_POINT('Ctrl Pts',(0.0509503601487159,-0.141598188489932,
0.513184573475417));
#17858=CARTESIAN_POINT('Ctrl Pts',(0.146613240011817,-0.0339196703426114,
0.521126741598197));
#17859=CARTESIAN_POINT('Ctrl Pts',(0.107963329873666,0.104832750538675,
0.529068909720978));
#17860=CARTESIAN_POINT('Ctrl Pts',(-0.0295920819230583,0.147547602048875,
0.537011077843756));
#17861=CARTESIAN_POINT('Ctrl Pts',(-0.140038106568177,0.055093691941219,
0.544953245966537));
#17862=CARTESIAN_POINT('Ctrl Pts',(-0.122194838935542,-0.0878316999746162,
0.552895414089317));
#17863=CARTESIAN_POINT('Ctrl Pts',(0.00759145471482065,-0.150294231420327,
0.560837582212097));
#17864=CARTESIAN_POINT('Ctrl Pts',(0.130423195946632,-0.0750718065719766,
0.568779750334878));
#17865=CARTESIAN_POINT('Ctrl Pts',(0.133773890807325,0.0689241055160235,
0.576721918457657));
#17866=CARTESIAN_POINT('Ctrl Pts',(0.0145739585745413,0.149778456108953,
0.584664086580438));
#17867=CARTESIAN_POINT('Ctrl Pts',(-0.117977216952174,0.0934203535806499,
0.592606254703216));
#17868=CARTESIAN_POINT('Ctrl Pts',(-0.142449141490696,-0.0485203902651028,
0.600548422825998));
#17869=CARTESIAN_POINT('Ctrl Pts',(-0.036423018067407,-0.146011471938939,
0.608490590948776));
#17870=CARTESIAN_POINT('Ctrl Pts',(0.102970331784443,-0.109741044988262,
0.616432759071558));
#17871=CARTESIAN_POINT('Ctrl Pts',(0.148032279177632,0.0270634532975707,
0.624374927194337));
#17872=CARTESIAN_POINT('Ctrl Pts',(0.0574814509102497,0.139075048028633,
0.632317095317117));
#17873=CARTESIAN_POINT('Ctrl Pts',(-0.0857282916847416,0.123679611042927,
0.640259263439898));
#17874=CARTESIAN_POINT('Ctrl Pts',(-0.150402111894479,-0.00501905574730406,
0.648201431562677));
#17875=CARTESIAN_POINT('Ctrl Pts',(-0.0772921462128499,-0.129119751845818,
0.656143599685457));
#17876=CARTESIAN_POINT('Ctrl Pts',(0.0666253659236285,-0.134933490277457,
0.664085767808237));
#17877=CARTESIAN_POINT('Ctrl Pts',(0.14950719819016,-0.0171342893707992,
0.672027935931017));
#17878=CARTESIAN_POINT('Ctrl Pts',(0.0954250774564579,0.11636168087194,
0.679970104053797));
#17879=CARTESIAN_POINT('Ctrl Pts',(-0.0460762176180427,0.143258397146306,
0.687912272176577));
#17880=CARTESIAN_POINT('Ctrl Pts',(-0.145366963764729,0.0389157041403328,
0.695854440299358));
#17881=CARTESIAN_POINT('Ctrl Pts',(-0.111486636987321,-0.101077771820372,
0.703796608422136));
#17882=CARTESIAN_POINT('Ctrl Pts',(0.02452690272786,-0.148473624679578,
0.711738776544918));
#17883=CARTESIAN_POINT('Ctrl Pts',(0.138071279799868,-0.0598523840572839,
0.719680944667696));
#17884=CARTESIAN_POINT('Ctrl Pts',(0.125128179973684,0.0835997892305201,
0.727623112790477));
#17885=CARTESIAN_POINT('Ctrl Pts',(-0.00244518761474098,0.150465967050502,
0.735565280913257));
#17886=CARTESIAN_POINT('Ctrl Pts',(-0.127778512144395,0.0794898610961098,
0.743507449036036));
#17887=CARTESIAN_POINT('Ctrl Pts',(-0.136053592364468,-0.0643071239260258,
0.751449617158818));
#17888=CARTESIAN_POINT('Ctrl Pts',(-0.019689604662082,-0.149192176910068,
0.759391785281597));
#17889=CARTESIAN_POINT('Ctrl Pts',(0.114712083700712,-0.0974018687498071,
0.767333953404378));
#17890=CARTESIAN_POINT('Ctrl Pts',(0.144025718573537,0.0436185576594447,
0.775276121527157));
#17891=CARTESIAN_POINT('Ctrl Pts',(0.0413969989087525,0.14467990414796,
0.783218289649938));
#17892=CARTESIAN_POINT('Ctrl Pts',(-0.0991556246317344,0.113199594905656,
0.791160457772717));
#17893=CARTESIAN_POINT('Ctrl Pts',(-0.148871509365196,-0.021983172706469,
0.799102625895497));
#17894=CARTESIAN_POINT('Ctrl Pts',(-0.062205797368885,-0.137027095702329,
0.807044794018277));
#17895=CARTESIAN_POINT('Ctrl Pts',(0.081446815661698,-0.126540121706451,
0.814986962141057));
#17896=CARTESIAN_POINT('Ctrl Pts',(0.150485778196879,-0.000129396266831759,
0.822929130263837));
#17897=CARTESIAN_POINT('Ctrl Pts',(0.0816643079123276,0.126399869446589,
0.830871298386618));
#17898=CARTESIAN_POINT('Ctrl Pts',(-0.0619700581130299,0.137133869194964,
0.838813466509397));
#17899=CARTESIAN_POINT('Ctrl Pts',(-0.148833484480893,0.0222391564630926,
0.846755634632177));
#17900=CARTESIAN_POINT('Ctrl Pts',(-0.0993501488194509,-0.113028908304323,
0.854697802754957));
#17901=CARTESIAN_POINT('Ctrl Pts',(0.041148129789194,-0.144750881164039,
0.862639970877736));
#17902=CARTESIAN_POINT('Ctrl Pts',(0.143950494202948,-0.0438661760544617,
0.870582139000517));
#17903=CARTESIAN_POINT('Ctrl Pts',(0.114879417330645,0.0972044528644933,
0.878524307123298));
#17904=CARTESIAN_POINT('Ctrl Pts',(-0.0194330078274841,0.149225816766708,
0.886466475246077));
#17905=CARTESIAN_POINT('Ctrl Pts',(-0.135942801386891,0.0645410019599824,
0.894408643368857));
#17906=CARTESIAN_POINT('Ctrl Pts',(-0.127915022941288,-0.0792700011911429,
0.902350811491637));
#17907=CARTESIAN_POINT('Ctrl Pts',(-0.00270394227186439,-0.150461539534541,
0.910292979614417));
#17908=CARTESIAN_POINT('Ctrl Pts',(0.124984227305131,-0.0838148501630433,
0.918235147737197));
#17909=CARTESIAN_POINT('Ctrl Pts',(0.138174004553101,0.0596148525845174,
0.926177315859977));
#17910=CARTESIAN_POINT('Ctrl Pts',(0.0247821984756025,0.148431225898158,
0.934119483982757));
#17911=CARTESIAN_POINT('Ctrl Pts',(-0.11131264737753,0.101269347369872,
0.942061652105537));
#17912=CARTESIAN_POINT('Ctrl Pts',(-0.145433672650089,-0.0386656571445607,
0.950003820228317));
#17913=CARTESIAN_POINT('Ctrl Pts',(-0.0463225128062989,-0.143178947440692,
0.957945988351097));
#17914=CARTESIAN_POINT('Ctrl Pts',(0.0952248276606132,-0.116525612549003,
0.965888156473877));
#17915=CARTESIAN_POINT('Ctrl Pts',(0.149536443172165,0.0168771545685866,
0.973830324596656));
#17916=CARTESIAN_POINT('Ctrl Pts',(0.0668573142755158,0.134818714245386,
0.981772492719438));
#17917=CARTESIAN_POINT('Ctrl Pts',(-0.0770699830103684,0.129252481220654,
0.989714660842216));
#17918=CARTESIAN_POINT('Ctrl Pts',(-0.15039325815857,0.00527769678589187,
0.997656828964997));
#17919=CARTESIAN_POINT('Ctrl Pts',(-0.0859408583470751,-0.123532000103139,
1.00559899708778));
#17920=CARTESIAN_POINT('Ctrl Pts',(0.0572421967501742,-0.139173693973137,
1.01354116521056));
#17921=CARTESIAN_POINT('Ctrl Pts',(0.147985518909957,-0.0273179863069172,
1.02148333333334));
#17922=CARTESIAN_POINT('Ctrl Pts',(0.103158902618224,0.109563803299803,
1.02942550145612));
#17923=CARTESIAN_POINT('Ctrl Pts',(-0.0361718663885326,0.146073893166727,
1.0373676695789));
#17924=CARTESIAN_POINT('Ctrl Pts',(-0.142365489706367,0.0487652901517079,
1.04530983770168));
#17925=CARTESIAN_POINT('Ctrl Pts',(-0.118137698690712,-0.0932173284908804,
1.05325200582446));
#17926=CARTESIAN_POINT('Ctrl Pts',(0.0143163610725534,-0.149803297655807,
1.06119417394724));
#17927=CARTESIAN_POINT('Ctrl Pts',(0.133655163317704,-0.0691540562905145,
1.06913634207002));
#17928=CARTESIAN_POINT('Ctrl Pts',(0.130552105047211,0.0748474051030229,
1.0770785101928));
#17929=CARTESIAN_POINT('Ctrl Pts',(0.0078499064261323,0.150280954056111,
1.08502067831558));
#17930=CARTESIAN_POINT('Ctrl Pts',(-0.122043612932812,0.0880417101447944,
1.09296284643836));
#17931=CARTESIAN_POINT('Ctrl Pts',(-0.140132644828567,-0.0548527851276936,
1.10090501456114));
#17932=CARTESIAN_POINT('Ctrl Pts',(-0.0298457776877653,-0.147496493982489,
1.10884718268392));
#17933=CARTESIAN_POINT('Ctrl Pts',(0.107782887988268,-0.10501826145877,
1.1167893508067));
#17934=CARTESIAN_POINT('Ctrl Pts',(0.146671355310253,0.033667487497105,
1.12473151892948));
#17935=CARTESIAN_POINT('Ctrl Pts',(0.0511937930472066,0.141510359113225,
1.13267368705226));
#17936=CARTESIAN_POINT('Ctrl Pts',(-0.0911825429852659,0.119715203870077,
1.14061585517504));
#17937=CARTESIAN_POINT('Ctrl Pts',(-0.150026302104679,-0.0117513769282424,
1.14855802329782));
#17938=CARTESIAN_POINT('Ctrl Pts',(-0.0714305557085884,-0.132452489195471,
1.1565001914206));
#17939=CARTESIAN_POINT('Ctrl Pts',(0.0726029180563751,-0.131813513998426,
1.16444235954338));
#17940=CARTESIAN_POINT('Ctrl Pts',(0.150124660100533,-0.010419818262018,
1.17238452766616));
#17941=CARTESIAN_POINT('Ctrl Pts',(0.0901167906002831,0.120519501471002,
1.18032669578894));
#17942=CARTESIAN_POINT('Ctrl Pts',(-0.0524473171394798,0.141050576417769,
1.18826886391172));
#17943=CARTESIAN_POINT('Ctrl Pts',(-0.146964294261872,0.0323648326895764,
1.1962110320345));
#17944=CARTESIAN_POINT('Ctrl Pts',(-0.106846879624786,-0.105970422747861,
1.20415320015727));
#17945=CARTESIAN_POINT('Ctrl Pts',(0.0311532535456026,-0.14722588419309,
1.21209536828006));
#17946=CARTESIAN_POINT('Ctrl Pts',(0.140613805972886,-0.0536073106276968,
1.22003753640283));
#17947=CARTESIAN_POINT('Ctrl Pts',(0.121257666323848,0.0891210667609394,
1.22797970452562));
#17948=CARTESIAN_POINT('Ctrl Pts',(-0.00918295295119051,0.150205391241489,
1.2359218726484));
#17949=CARTESIAN_POINT('Ctrl Pts',(-0.131211043922368,0.0736861461587066,
1.24386404077118));
#17950=CARTESIAN_POINT('Ctrl Pts',(-0.133036338837895,-0.0703371788708997,
1.25180620889396));
#17951=CARTESIAN_POINT('Ctrl Pts',(-0.0129866800356469,-0.149924422041766,
1.25974837701674));
#17952=CARTESIAN_POINT('Ctrl Pts',(0.118960111851797,-0.0921654923014072,
1.26769054513952));
#17953=CARTESIAN_POINT('Ctrl Pts',(0.141927220045961,0.050026496908035,
1.2756327132623));
#17954=CARTESIAN_POINT('Ctrl Pts',(0.0348744139414821,0.146389075532006,
1.28357488138508));
#17955=CARTESIAN_POINT('Ctrl Pts',(-0.104126938119509,0.108644221848311,
1.29151704950786));
#17956=CARTESIAN_POINT('Ctrl Pts',(-0.147737317493493,-0.0286299004949125,
1.29945921763064));
#17957=CARTESIAN_POINT('Ctrl Pts',(-0.0560051364173496,-0.139676092720537,
1.30740138575342));
#17958=CARTESIAN_POINT('Ctrl Pts',(0.0870335032532438,-0.122764634549313,
1.3153435538762));
#17959=CARTESIAN_POINT('Ctrl Pts',(0.150340512633584,0.00661184096937889,
1.32328572199898));
#17960=CARTESIAN_POINT('Ctrl Pts',(0.0759201674095095,0.129931190880528,
1.33122789012176));
#17961=CARTESIAN_POINT('Ctrl Pts',(-0.0680508508044829,0.134220221643466,
1.33917005824454));
#17962=CARTESIAN_POINT('Ctrl Pts',(-0.149680298423566,0.0155497403439283,
1.34711222636732));
#17963=CARTESIAN_POINT('Ctrl Pts',(-0.0941872156892785,-0.117365900463673,
1.3550543944901));
#17964=CARTESIAN_POINT('Ctrl Pts',(0.0475910332998192,-0.142762319241037,
1.36299656261288));
#17965=CARTESIAN_POINT('Ctrl Pts',(0.145771005694385,-0.0373737865856905,
1.37093873073566));
#17966=CARTESIAN_POINT('Ctrl Pts',(0.110409762917901,0.10225297323032,1.37888089885844));
#17967=CARTESIAN_POINT('Ctrl Pts',(-0.0260981686868614,0.148205506441964,
1.38682306698121));
#17968=CARTESIAN_POINT('Ctrl Pts',(-0.138697490589939,0.0583865667538053,
1.394765235104));
#17969=CARTESIAN_POINT('Ctrl Pts',(-0.124235673603468,-0.0849204601545819,
1.40270740322677));
#17970=CARTESIAN_POINT('Ctrl Pts',(0.0040388053119065,-0.150431633134115,
1.41064957134956));
#17971=CARTESIAN_POINT('Ctrl Pts',(0.12861328245382,-0.0781319533624403,
1.41859173947234));
#17972=CARTESIAN_POINT('Ctrl Pts',(0.1353648581188,0.0657445800149866,1.42653390759512));
#17973=CARTESIAN_POINT('Ctrl Pts',(0.0181081687242482,0.149392404544468,
1.43447607571789));
#17974=CARTESIAN_POINT('Ctrl Pts',(-0.115737181672069,0.0961812857364522,
1.44241824384068));
#17975=CARTESIAN_POINT('Ctrl Pts',(-0.143555918690644,-0.0451414811888502,
1.45036041196346));
#17976=CARTESIAN_POINT('Ctrl Pts',(-0.0398616700558823,-0.145110565703753,
1.45830258008624));
#17977=CARTESIAN_POINT('Ctrl Pts',(0.100348034367198,-0.112142416378873,
1.46624474820902));
#17978=CARTESIAN_POINT('Ctrl Pts',(0.14863229283285,0.0235577176564554,
1.4741869163318));
#17979=CARTESIAN_POINT('Ctrl Pts',(0.0607471474677608,0.137680339497592,
1.48212908445458));
#17980=CARTESIAN_POINT('Ctrl Pts',(-0.0827754224726193,0.125666453945577,
1.49007125257736));
#17981=CARTESIAN_POINT('Ctrl Pts',(-0.150492272191201,-0.00145719475437189,
1.49801342070014));
#17982=CARTESIAN_POINT('Ctrl Pts',(-0.0802951178786721,-0.12727177793954,
1.50595558882292));
#17983=CARTESIAN_POINT('Ctrl Pts',(0.0633700050447994,-0.136443062004882,
1.5138977569457));
#17984=CARTESIAN_POINT('Ctrl Pts',(0.149155357006591,-0.0207133070603065,
1.52183992506848));
#17985=CARTESIAN_POINT('Ctrl Pts',(0.0979555318420461,0.114182655252422,
1.52978209319126));
#17986=CARTESIAN_POINT('Ctrl Pts',(0.00450803278943675,0.134083974545181,
1.53507687193978));
#17987=CARTESIAN_POINT('Ctrl Pts',(-0.0361033354337414,0.122073089461022,
1.53772426131404));
#17988=CARTESIAN_POINT('Ctrl Pts',(-0.0592743564846203,0.123319225136773,
-0.00549926131403157));
#17989=CARTESIAN_POINT('Ctrl Pts',(-0.100300290071938,0.10359978715075,
-0.00285187193977157));
#17990=CARTESIAN_POINT('Ctrl Pts',(-0.160414584165772,0.0203416160441626,
0.00244290680874841));
#17991=CARTESIAN_POINT('Ctrl Pts',(-0.103922107946056,-0.124084444561314,
0.0103850749315284));
#17992=CARTESIAN_POINT('Ctrl Pts',(0.0479099321398382,-0.154436663180837,
0.0183272430543084));
#17993=CARTESIAN_POINT('Ctrl Pts',(0.155781551077148,-0.0435098515708298,
0.0262694111770884));
#17994=CARTESIAN_POINT('Ctrl Pts',(0.120977930992648,0.107381072623318,
0.0342115792998684));
#17995=CARTESIAN_POINT('Ctrl Pts',(-0.0246731903087699,0.159844935900913,
0.0421537474226484));
#17996=CARTESIAN_POINT('Ctrl Pts',(-0.147710978397823,0.0659033513787588,
0.0500959155454284));
#17997=CARTESIAN_POINT('Ctrl Pts',(-0.135435684249567,-0.0884277117007276,
0.0580380836682085));
#17998=CARTESIAN_POINT('Ctrl Pts',(0.000915427738408385,-0.16174188059703,
0.0659802517909884));
#17999=CARTESIAN_POINT('Ctrl Pts',(0.13642643003965,-0.0868880976295618,
0.0739224199137684));
#18000=CARTESIAN_POINT('Ctrl Pts',(0.146957588340267,0.0675663355536457,
0.0818645880365484));
#18001=CARTESIAN_POINT('Ctrl Pts',(0.0228600865593111,0.160121891352391,
0.0898067561593285));
#18002=CARTESIAN_POINT('Ctrl Pts',(-0.122179386207322,0.105989962368389,
0.0977489242821083));
#18003=CARTESIAN_POINT('Ctrl Pts',(-0.155290103436038,-0.0452399862206161,
0.105691092404888));
#18004=CARTESIAN_POINT('Ctrl Pts',(-0.0461390722131997,-0.155025288408554,
0.113633260527668));
#18005=CARTESIAN_POINT('Ctrl Pts',(0.105280057525145,-0.122791590307548,
0.121575428650448));
#18006=CARTESIAN_POINT('Ctrl Pts',(0.160251855424436,0.0219318669073289,
0.129517596773229));
#18007=CARTESIAN_POINT('Ctrl Pts',(0.0684164816681947,0.146563455853242,
0.137459764896008));
#18008=CARTESIAN_POINT('Ctrl Pts',(-0.086095413359615,0.136927875387926,
0.145401933018789));
#18009=CARTESIAN_POINT('Ctrl Pts',(-0.16173506727009,0.00185228698694943,
0.153344101141568));
#18010=CARTESIAN_POINT('Ctrl Pts',(-0.0892087826023274,-0.134920182928699,
0.161286269264348));
#18011=CARTESIAN_POINT('Ctrl Pts',(0.0650419110192955,-0.148091906331324,
0.169228437387128));
#18012=CARTESIAN_POINT('Ctrl Pts',(0.159707532494063,-0.025596228460074,
0.177170605509908));
#18013=CARTESIAN_POINT('Ctrl Pts',(0.108064646638443,0.120348223746572,
0.185112773632688));
#18014=CARTESIAN_POINT('Ctrl Pts',(-0.0425765573421325,0.156041339440091,
0.193054941755468));
#18015=CARTESIAN_POINT('Ctrl Pts',(-0.154213260793436,0.0487845573223287,
0.200997109878248));
#18016=CARTESIAN_POINT('Ctrl Pts',(-0.124574774400312,-0.103163891052585,
0.208939278001028));
#18017=CARTESIAN_POINT('Ctrl Pts',(0.0191870033818907,-0.160603616835255,
0.216881446123808));
#18018=CARTESIAN_POINT('Ctrl Pts',(0.145371514918136,-0.0709139301387177,
0.224823614246588));
#18019=CARTESIAN_POINT('Ctrl Pts',(0.138380784202201,0.0837402018183176,
0.232765782369368));
#18020=CARTESIAN_POINT('Ctrl Pts',(0.00461903876105218,0.161679705957985,
0.240707950492149));
#18021=CARTESIAN_POINT('Ctrl Pts',(-0.133374220718213,0.0915039894496894,
0.248650118614928));
#18022=CARTESIAN_POINT('Ctrl Pts',(-0.149182991964712,-0.0624987819548612,
0.256592286737709));
#18023=CARTESIAN_POINT('Ctrl Pts',(-0.0283248164207669,-0.159246248345813,
0.264534454860488));
#18024=CARTESIAN_POINT('Ctrl Pts',(0.118481800883715,-0.110107791262854,
0.272476622983269));
#18025=CARTESIAN_POINT('Ctrl Pts',(0.156746916480749,0.0399007144198201,
0.280418791106048));
#18026=CARTESIAN_POINT('Ctrl Pts',(0.0514157533588968,0.153356066537929,
0.288360959228829));
#18027=CARTESIAN_POINT('Ctrl Pts',(-0.101017521980764,0.126321506839912,
0.296303127351608));
#18028=CARTESIAN_POINT('Ctrl Pts',(-0.160908369261695,-0.0164365306249019,
0.304245295474388));
#18029=CARTESIAN_POINT('Ctrl Pts',(-0.0733906195540655,-0.144137017448375,
0.312187463597168));
#18030=CARTESIAN_POINT('Ctrl Pts',(0.0813604773699057,-0.13979318853071,
0.320129631719948));
#18031=CARTESIAN_POINT('Ctrl Pts',(0.161577018543625,-0.00738443741900211,
0.328071799842729));
#18032=CARTESIAN_POINT('Ctrl Pts',(0.0937724112935796,0.131789217000595,
0.336013967965508));
#18033=CARTESIAN_POINT('Ctrl Pts',(-0.0599373583072218,0.150230409426965,
0.343956136088289));
#18034=CARTESIAN_POINT('Ctrl Pts',(-0.158738350099833,0.0310451130618767,
0.351898304211068));
#18035=CARTESIAN_POINT('Ctrl Pts',(-0.112118705390683,-0.116580696253536,
0.359840472333849));
#18036=CARTESIAN_POINT('Ctrl Pts',(0.0372131918485748,-0.15740661101073,
0.367782640456628));
#18037=CARTESIAN_POINT('Ctrl Pts',(0.152453982298084,-0.0540318990865351,
0.375724808579408));
#18038=CARTESIAN_POINT('Ctrl Pts',(0.128031262769868,0.0988415833088236,
0.383666976702188));
#18039=CARTESIAN_POINT('Ctrl Pts',(-0.0136812466069205,0.161166021011634,
0.391609144824968));
#18040=CARTESIAN_POINT('Ctrl Pts',(-0.142860328563903,0.0758458262533652,
0.399551312947749));
#18041=CARTESIAN_POINT('Ctrl Pts',(-0.141164672957165,-0.0789569372907697,
0.407493481070528));
#18042=CARTESIAN_POINT('Ctrl Pts',(-0.0101476745237983,-0.161427034722196,
0.415435649193308));
#18043=CARTESIAN_POINT('Ctrl Pts',(0.130165636283581,-0.0960133843187101,
0.423377817316089));
#18044=CARTESIAN_POINT('Ctrl Pts',(0.151233851831306,0.0573583899504574,
0.431319985438868));
#18045=CARTESIAN_POINT('Ctrl Pts',(0.0337563222576384,0.158183986373718,
0.439262153561649));
#18046=CARTESIAN_POINT('Ctrl Pts',(-0.114645466422773,0.114096800420287,
0.447204321684428));
#18047=CARTESIAN_POINT('Ctrl Pts',(-0.158020229883659,-0.0345147763277912,
0.455146489807208));
#18048=CARTESIAN_POINT('Ctrl Pts',(-0.0566322287360923,-0.151507272121918,
0.463088657929988));
#18049=CARTESIAN_POINT('Ctrl Pts',(0.0966367119836487,-0.129703541718919,
0.471030826052768));
#18050=CARTESIAN_POINT('Ctrl Pts',(0.161376496659739,0.0109219578497271,
0.478972994175549));
#18051=CARTESIAN_POINT('Ctrl Pts',(0.0782788315581001,0.141541821972661,
0.486915162298328));
#18052=CARTESIAN_POINT('Ctrl Pts',(-0.0765302851406724,0.142494836024782,
0.494857330421108));
#18053=CARTESIAN_POINT('Ctrl Pts',(-0.161229798395673,0.0129079412274925,
0.502799498543889));
#18054=CARTESIAN_POINT('Ctrl Pts',(-0.0982262525537151,-0.128503953817366,
0.510741666666668));
#18055=CARTESIAN_POINT('Ctrl Pts',(0.0547626317937811,-0.152193025452748,
0.518683834789449));
#18056=CARTESIAN_POINT('Ctrl Pts',(0.157583319439253,-0.0364576503898468,
0.526626002912228));
#18057=CARTESIAN_POINT('Ctrl Pts',(0.116041497328862,0.112676677866884,
0.534568171035008));
#18058=CARTESIAN_POINT('Ctrl Pts',(-0.0318062577307366,0.158587593482618,
0.542510339157789));
#18059=CARTESIAN_POINT('Ctrl Pts',(-0.150516213127973,0.0592159811457737,
0.550452507280567));
#18060=CARTESIAN_POINT('Ctrl Pts',(-0.131337854181896,-0.0944035534094825,
0.558394675403349));
#18061=CARTESIAN_POINT('Ctrl Pts',(0.00815947204521347,-0.161539734596121,
0.566336843526128));
#18062=CARTESIAN_POINT('Ctrl Pts',(0.140181883624494,-0.080688923285235,
0.574279011648909));
#18063=CARTESIAN_POINT('Ctrl Pts',(0.143783288371658,0.0740812312429708,
0.582221179771688));
#18064=CARTESIAN_POINT('Ctrl Pts',(0.0156644295519346,0.160985367298567,
0.590163347894469));
#18065=CARTESIAN_POINT('Ctrl Pts',(-0.126804656005353,0.100410368253513,
0.598105516017247));
#18066=CARTESIAN_POINT('Ctrl Pts',(-0.153107649524464,-0.0521508436608248,
0.606047684140029));
#18067=CARTESIAN_POINT('Ctrl Pts',(-0.0391483067326994,-0.156936525122116,
0.613989852262808));
#18068=CARTESIAN_POINT('Ctrl Pts',(0.110674906884577,-0.117952226869747,
0.621932020385589));
#18069=CARTESIAN_POINT('Ctrl Pts',(0.159108535730396,0.0290884288879846,
0.629874188508368));
#18070=CARTESIAN_POINT('Ctrl Pts',(0.061782400006242,0.14948109541648,0.637816356631148));
#18071=CARTESIAN_POINT('Ctrl Pts',(-0.0921427612707386,0.132933721767072,
0.645758524753929));
#18072=CARTESIAN_POINT('Ctrl Pts',(-0.161655687038194,-0.0053945978210935,
0.653700692876707));
#18073=CARTESIAN_POINT('Ctrl Pts',(-0.0830753959589387,-0.138780911597048,
0.661642860999489));
#18074=CARTESIAN_POINT('Ctrl Pts',(0.0716104924784035,-0.145029652845349,
0.669585029122267));
#18075=CARTESIAN_POINT('Ctrl Pts',(0.160693812980115,-0.0184163326249747,
0.677527197245049));
#18076=CARTESIAN_POINT('Ctrl Pts',(0.102565092089392,0.125068240261613,
0.685469365367828));
#18077=CARTESIAN_POINT('Ctrl Pts',(-0.0495237900674707,0.153977456320057,
0.693411533490608));
#18078=CARTESIAN_POINT('Ctrl Pts',(-0.156243792750268,0.0418275036842162,
0.701353701613389));
#18079=CARTESIAN_POINT('Ctrl Pts',(-0.119828429739121,-0.108640739429086,
0.709295869736167));
#18080=CARTESIAN_POINT('Ctrl Pts',(0.0263620853553792,-0.159582904138124,
0.717238037858949));
#18081=CARTESIAN_POINT('Ctrl Pts',(0.148402221984423,-0.0643307340819919,
0.725180205981728));
#18082=CARTESIAN_POINT('Ctrl Pts',(0.134490677336207,0.0898549973406614,
0.733122374104509));
#18083=CARTESIAN_POINT('Ctrl Pts',(-0.00262814450422035,0.161724320044658,
0.741064542227287));
#18084=CARTESIAN_POINT('Ctrl Pts',(-0.137339315979238,0.0854375510170853,
0.749006710350069));
#18085=CARTESIAN_POINT('Ctrl Pts',(-0.146233564613262,-0.0691187920752458,
0.756948878472847));
#18086=CARTESIAN_POINT('Ctrl Pts',(-0.0211628449166461,-0.160355220783347,
0.764891046595629));
#18087=CARTESIAN_POINT('Ctrl Pts',(0.12329521486528,-0.104689793336152,
0.772833214718408));
#18088=CARTESIAN_POINT('Ctrl Pts',(0.154802191231926,0.0468822399980663,
0.780775382841188));
#18089=CARTESIAN_POINT('Ctrl Pts',(0.0444944569967772,0.155505325098544,
0.788717550963968));
#18090=CARTESIAN_POINT('Ctrl Pts',(-0.106574770936664,0.121669556739719,
0.796659719086747));
#18091=CARTESIAN_POINT('Ctrl Pts',(-0.160010559849905,-0.0236280251811701,
0.804601887209529));
#18092=CARTESIAN_POINT('Ctrl Pts',(-0.0668602374312443,-0.147279908636853,
0.812544055332307));
#18093=CARTESIAN_POINT('Ctrl Pts',(0.0875409312876049,-0.13600826514128,
0.820486223455089));
#18094=CARTESIAN_POINT('Ctrl Pts',(0.161745613525436,-0.000139078116330951,
0.828428391577867));
#18095=CARTESIAN_POINT('Ctrl Pts',(0.0877746970157421,0.135857518751215,
0.836370559700649));
#18096=CARTESIAN_POINT('Ctrl Pts',(-0.0666068593976089,0.147394671269449,
0.844312727823428));
#18097=CARTESIAN_POINT('Ctrl Pts',(-0.159969689820096,0.0239031624749592,
0.852254895946208));
#18098=CARTESIAN_POINT('Ctrl Pts',(-0.106783850056725,-0.121486098811777,
0.860197064068988));
#18099=CARTESIAN_POINT('Ctrl Pts',(0.0442269666803361,-0.155581612845794,
0.868139232191768));
#18100=CARTESIAN_POINT('Ctrl Pts',(0.154721338329289,-0.0471483860066884,
0.876081400314548));
#18101=CARTESIAN_POINT('Ctrl Pts',(0.123475068941597,0.104477606152275,
0.884023568437328));
#18102=CARTESIAN_POINT('Ctrl Pts',(-0.0208870486723946,0.160391377683462,
0.891965736560109));
#18103=CARTESIAN_POINT('Ctrl Pts',(-0.146114483894434,0.0693701696243073,
0.899907904682887));
#18104=CARTESIAN_POINT('Ctrl Pts',(-0.137486040957907,-0.0852012404790134,
0.907850072805669));
#18105=CARTESIAN_POINT('Ctrl Pts',(-0.00290626002629624,-0.161719561247554,
0.915792240928448));
#18106=CARTESIAN_POINT('Ctrl Pts',(0.134335953660838,-0.0900861498315643,
0.923734409051229));
#18107=CARTESIAN_POINT('Ctrl Pts',(0.148512632937768,0.0640754297319473,
0.931676577174007));
#18108=CARTESIAN_POINT('Ctrl Pts',(0.0266364831612253,0.159537332941991,
0.939618745296788));
#18109=CARTESIAN_POINT('Ctrl Pts',(-0.119641421660886,0.10884664928423,
0.947560913419568));
#18110=CARTESIAN_POINT('Ctrl Pts',(-0.156315493011378,-0.0415587473590326,
0.955503081542348));
#18111=CARTESIAN_POINT('Ctrl Pts',(-0.0497885138626987,-0.153892061929087,
0.963445249665127));
#18112=CARTESIAN_POINT('Ctrl Pts',(0.102349858952582,-0.125244437839883,
0.971387417787908));
#18113=CARTESIAN_POINT('Ctrl Pts',(0.160725246166783,0.018139958160622,
0.979329585910688));
#18114=CARTESIAN_POINT('Ctrl Pts',(0.0718597959603077,0.14490628889729,
0.987271754033468));
#18115=CARTESIAN_POINT('Ctrl Pts',(-0.0828366097831417,0.138923572215364,
0.995213922156248));
#18116=CARTESIAN_POINT('Ctrl Pts',(-0.161646170836971,0.00567259122332548,
1.00315609027903));
#18117=CARTESIAN_POINT('Ctrl Pts',(-0.0923712328620446,-0.132775066096718,
1.01109825840181));
#18118=CARTESIAN_POINT('Ctrl Pts',(0.0615252440718216,-0.149587122371362,
1.01904042652459));
#18119=CARTESIAN_POINT('Ctrl Pts',(0.159058276707423,-0.0293620068848675,
1.02698259464737));
#18120=CARTESIAN_POINT('Ctrl Pts',(0.1108775872014,0.117761723381742,1.03492476277015));
#18121=CARTESIAN_POINT('Ctrl Pts',(-0.0388783630684312,0.157003616909169,
1.04286693089293));
#18122=CARTESIAN_POINT('Ctrl Pts',(-0.153017738641585,0.0524140677533946,
1.05080909901571));
#18123=CARTESIAN_POINT('Ctrl Pts',(-0.126977145509477,-0.10019215216626,
1.05875126713849));
#18124=CARTESIAN_POINT('Ctrl Pts',(0.0153875577671049,-0.161012067570745,
1.06669343526127));
#18125=CARTESIAN_POINT('Ctrl Pts',(0.143655677305146,-0.0743283876822416,
1.07463560338405));
#18126=CARTESIAN_POINT('Ctrl Pts',(0.140320438123209,0.080447731368589,
1.08257777150683));
#18127=CARTESIAN_POINT('Ctrl Pts',(0.00843726195408678,0.161525463776335,
1.09051993962961));
#18128=CARTESIAN_POINT('Ctrl Pts',(-0.131175312957834,0.094629277223576,
1.09846210775239));
#18129=CARTESIAN_POINT('Ctrl Pts',(-0.150617825048456,-0.0589570489009974,
1.10640427587517));
#18130=CARTESIAN_POINT('Ctrl Pts',(-0.0320789358376135,-0.158532661344495,
1.11434644399795));
#18131=CARTESIAN_POINT('Ctrl Pts',(0.115847554194776,-0.112876069317329,
1.12228861212073));
#18132=CARTESIAN_POINT('Ctrl Pts',(0.157645783113317,0.0361865984037055,
1.13023078024351));
#18133=CARTESIAN_POINT('Ctrl Pts',(0.0550242791334153,0.152098624396442,
1.13817294836629));
#18134=CARTESIAN_POINT('Ctrl Pts',(-0.0980051173916675,0.128672684756662,
1.14611511648907));
#18135=CARTESIAN_POINT('Ctrl Pts',(-0.161251757937727,-0.0126306531673768,
1.15405728461185));
#18136=CARTESIAN_POINT('Ctrl Pts',(-0.0767752221903169,-0.142363015193798,
1.16199945273463));
#18137=CARTESIAN_POINT('Ctrl Pts',(0.0780353045016797,-0.141676229794458,
1.16994162085741));
#18138=CARTESIAN_POINT('Ctrl Pts',(0.161357475398708,-0.0111994629512984,
1.17788378898019));
#18139=CARTESIAN_POINT('Ctrl Pts',(0.0968596219472387,0.129537162519796,
1.18582595710297));
#18140=CARTESIAN_POINT('Ctrl Pts',(-0.0563715959749383,0.151604439264423,
1.19376812522575));
#18141=CARTESIAN_POINT('Ctrl Pts',(-0.157960640709981,0.0347864747270306,
1.20171029334853));
#18142=CARTESIAN_POINT('Ctrl Pts',(-0.114841510641486,-0.113899474410655,
1.20965246147131));
#18143=CARTESIAN_POINT('Ctrl Pts',(0.03348424129126,-0.158241803650584,
1.21759462959409));
#18144=CARTESIAN_POINT('Ctrl Pts',(0.151134988234409,-0.0576183839484237,
1.22553679771687));
#18145=CARTESIAN_POINT('Ctrl Pts',(0.130330559267559,0.0957893948119858,
1.23347896583965));
#18146=CARTESIAN_POINT('Ctrl Pts',(-0.0098700513554357,0.16144424710618,
1.24142113396243));
#18147=CARTESIAN_POINT('Ctrl Pts',(-0.141028680947982,0.0791995832534545,
1.24936330208521));
#18148=CARTESIAN_POINT('Ctrl Pts',(-0.142990550365238,-0.0756000353418,
1.25730547020799));
#18149=CARTESIAN_POINT('Ctrl Pts',(-0.013958385670676,-0.161142254877177,
1.26524763833077));
#18150=CARTESIAN_POINT('Ctrl Pts',(0.127861094297897,-0.0990616141723472,
1.27318980645355));
#18151=CARTESIAN_POINT('Ctrl Pts',(0.152546676219863,0.0537696421008814,
1.28113197457633));
#18152=CARTESIAN_POINT('Ctrl Pts',(0.0374838310097642,0.157342382244044,
1.28907414269911));
#18153=CARTESIAN_POINT('Ctrl Pts',(-0.111918054267102,0.116773335855419,
1.29701631082189));
#18154=CARTESIAN_POINT('Ctrl Pts',(-0.158791504053787,-0.0307720827589687,
1.30495847894467));
#18155=CARTESIAN_POINT('Ctrl Pts',(-0.060195622861772,-0.150127112226926,
1.31290064706745));
#18156=CARTESIAN_POINT('Ctrl Pts',(0.0935456330135535,-0.131950283756556,
1.32084281519023));
#18157=CARTESIAN_POINT('Ctrl Pts',(0.161589478720268,0.00710656041347678,
1.32878498331301));
#18158=CARTESIAN_POINT('Ctrl Pts',(0.0816007612396376,0.139653065139265,
1.33672715143579));
#18159=CARTESIAN_POINT('Ctrl Pts',(-0.0731426367739486,0.144263015132499,
1.34466931955857));
#18160=CARTESIAN_POINT('Ctrl Pts',(-0.160879865135934,0.0167132224867059,
1.35261148768135));
#18161=CARTESIAN_POINT('Ctrl Pts',(-0.101234609479067,-0.126147598829082,
1.36055365580413));
#18162=CARTESIAN_POINT('Ctrl Pts',(0.051151949184981,-0.153444260252591,
1.36849582392691));
#18163=CARTESIAN_POINT('Ctrl Pts',(0.15667806641111,-0.0401702148435725,
1.37643799204969));
#18164=CARTESIAN_POINT('Ctrl Pts',(0.118670980449659,0.10990387323047,1.38438016017247));
#18165=CARTESIAN_POINT('Ctrl Pts',(-0.0280509185434417,0.159294724422008,
1.39232232829525));
#18166=CARTESIAN_POINT('Ctrl Pts',(-0.149075287902345,0.0627552395607943,
1.40026449641803));
#18167=CARTESIAN_POINT('Ctrl Pts',(-0.133531390736797,-0.0912744851582948,
1.40820666454081));
#18168=CARTESIAN_POINT('Ctrl Pts',(0.00434100186018791,-0.161687417152987,
1.41614883266359));
#18169=CARTESIAN_POINT('Ctrl Pts',(0.138236546518021,-0.0839780402106489,
1.42409100078637));
#18170=CARTESIAN_POINT('Ctrl Pts',(0.145493297031458,0.07066380330362,1.43203316890915));
#18171=CARTESIAN_POINT('Ctrl Pts',(0.0194630807988606,0.160570430100525,
1.43997533703193));
#18172=CARTESIAN_POINT('Ctrl Pts',(-0.124397014000637,0.103377882332206,
1.44791750515471));
#18173=CARTESIAN_POINT('Ctrl Pts',(-0.15429723939393,-0.0485191136187331,
1.45585967327749));
#18174=CARTESIAN_POINT('Ctrl Pts',(-0.042844249846,-0.155968210152522,1.46380184140027));
#18175=CARTESIAN_POINT('Ctrl Pts',(0.107856400646442,-0.120533276677448,
1.47174400952305));
#18176=CARTESIAN_POINT('Ctrl Pts',(0.159753444358638,0.0253203827049868,
1.47968617764583));
#18177=CARTESIAN_POINT('Ctrl Pts',(0.0652924466007548,0.147982030257331,
1.48762834576861));
#18178=CARTESIAN_POINT('Ctrl Pts',(-0.0889689487809616,0.13506922671723,
1.49557051389139));
#18179=CARTESIAN_POINT('Ctrl Pts',(-0.161752593421533,-0.00156622680492735,
1.50351268201417));
#18180=CARTESIAN_POINT('Ctrl Pts',(-0.086303059730943,-0.136794666273195,
1.51145485013695));
#18181=CARTESIAN_POINT('Ctrl Pts',(0.0681115549116652,-0.14665217563879,
1.51939701825973));
#18182=CARTESIAN_POINT('Ctrl Pts',(0.160315645894948,-0.02226314405755,
1.52733918638251));
#18183=CARTESIAN_POINT('Ctrl Pts',(0.105284883301553,0.122726172858702,
1.53528135450529));
#18184=CARTESIAN_POINT('Ctrl Pts',(0.00484533846358528,0.144116573583224,
1.54057613325381));
#18185=CARTESIAN_POINT('Ctrl Pts',(-0.0388047044047284,0.131206995015745,
1.54322352262807));
#18186=CARTESIAN_POINT('Ctrl Pts',(-0.0634007094575145,0.131904027763688,
-3.88578058618805E-16));
#18187=CARTESIAN_POINT('Ctrl Pts',(-0.107282641710421,0.110811831533068,
0.00264738937425961));
#18188=CARTESIAN_POINT('Ctrl Pts',(-0.171581760589518,0.0217576868851663,
0.0079421681227796));
#18189=CARTESIAN_POINT('Ctrl Pts',(-0.111156590520044,-0.1327225175337,
0.0158843362455596));
#18190=CARTESIAN_POINT('Ctrl Pts',(0.0512451567233008,-0.165187689797298,
0.0238265043683396));
#18191=CARTESIAN_POINT('Ctrl Pts',(0.16662620135312,-0.0465387668729445,
0.0317686724911196));
#18192=CARTESIAN_POINT('Ctrl Pts',(0.129399745666171,0.114856349193662,
0.0397108406138996));
#18193=CARTESIAN_POINT('Ctrl Pts',(-0.026390801400978,0.170972456562021,
0.0476530087366796));
#18194=CARTESIAN_POINT('Ctrl Pts',(-0.157993800025737,0.070491178324729,
0.0555951768594596));
#18195=CARTESIAN_POINT('Ctrl Pts',(-0.144863967768493,-0.0945835600760224,
0.0635373449822396));
#18196=CARTESIAN_POINT('Ctrl Pts',(0.000979154756195248,-0.17300145605975,
0.0714795131050195));
#18197=CARTESIAN_POINT('Ctrl Pts',(0.145923683802689,-0.0929367665856833,
0.0794216812277997));
#18198=CARTESIAN_POINT('Ctrl Pts',(0.157187963117837,0.0722699302633024,
0.0873638493505794));
#18199=CARTESIAN_POINT('Ctrl Pts',(0.0244514793930555,0.171268692120756,
0.0953060174733598));
#18200=CARTESIAN_POINT('Ctrl Pts',(-0.130684839550095,0.113368397534175,
0.103248185596139));
#18201=CARTESIAN_POINT('Ctrl Pts',(-0.166100541844429,-0.0483893439312075,
0.11119035371892));
#18202=CARTESIAN_POINT('Ctrl Pts',(-0.0493510193195793,-0.165817291858885,
0.119132521841699));
#18203=CARTESIAN_POINT('Ctrl Pts',(0.112609073040783,-0.131339661914923,
0.12707468996448));
#18204=CARTESIAN_POINT('Ctrl Pts',(0.17140770357293,0.0234586422209967,
0.135016858087259));
#18205=CARTESIAN_POINT('Ctrl Pts',(0.0731792588499177,0.156766393306209,
0.14295902621004));
#18206=CARTESIAN_POINT('Ctrl Pts',(-0.0920889000195865,0.146460037003638,
0.150901194332819));
#18207=CARTESIAN_POINT('Ctrl Pts',(-0.172994168426659,0.00198123296575728,
0.1588433624556));
#18208=CARTESIAN_POINT('Ctrl Pts',(-0.0954190048152776,-0.144312580095855,
0.16678553057838));
#18209=CARTESIAN_POINT('Ctrl Pts',(0.0695697692503139,-0.158401246055831,
0.17472769870116));
#18210=CARTESIAN_POINT('Ctrl Pts',(0.170825487889685,-0.0273780963649298,
0.18266986682394));
#18211=CARTESIAN_POINT('Ctrl Pts',(0.115587509852263,0.128726201683253,
0.19061203494672));
#18212=CARTESIAN_POINT('Ctrl Pts',(-0.0455405018601966,0.16690407474553,
0.198554203069499));
#18213=CARTESIAN_POINT('Ctrl Pts',(-0.164948735370872,0.0521806684752238,
0.20649637119228));
#18214=CARTESIAN_POINT('Ctrl Pts',(-0.133246981425072,-0.110345590758605,
0.214438539315059));
#18215=CARTESIAN_POINT('Ctrl Pts',(0.0205226964731592,-0.171783952668295,
0.22238070743784));
#18216=CARTESIAN_POINT('Ctrl Pts',(0.155491476033395,-0.0758505658746651,
0.230322875560619));
#18217=CARTESIAN_POINT('Ctrl Pts',(0.148014089296488,0.0895697316726553,
0.2382650436834));
#18218=CARTESIAN_POINT('Ctrl Pts',(0.00494059070111224,0.172934953166096,
0.24620721180618));
#18219=CARTESIAN_POINT('Ctrl Pts',(-0.142658996543838,0.0978739912732451,
0.25414937992896));
#18220=CARTESIAN_POINT('Ctrl Pts',(-0.159568287038446,-0.0668496016012732,
0.262091548051739));
#18221=CARTESIAN_POINT('Ctrl Pts',(-0.0302966335331915,-0.170332091689456,
0.27003371617452));
#18222=CARTESIAN_POINT('Ctrl Pts',(0.126729848780061,-0.11777288690896,
0.2779758842973));
#18223=CARTESIAN_POINT('Ctrl Pts',(0.167658770158652,0.0426783815482623,
0.28591805242008));
#18224=CARTESIAN_POINT('Ctrl Pts',(0.0549950338320791,0.164031867990689,
0.293860220542859));
#18225=CARTESIAN_POINT('Ctrl Pts',(-0.108049803339193,0.135115311719503,
0.30180238866564));
#18226=CARTESIAN_POINT('Ctrl Pts',(-0.1721099202737,-0.0175807510100837,
0.309744556788419));
#18227=CARTESIAN_POINT('Ctrl Pts',(-0.0784996687135917,-0.154171039675278,
0.3176867249112));
#18228=CARTESIAN_POINT('Ctrl Pts',(0.087024343965547,-0.14952481740522,
0.325628893033979));
#18229=CARTESIAN_POINT('Ctrl Pts',(0.172825117221703,-0.00789850112384905,
0.33357106115676));
#18230=CARTESIAN_POINT('Ctrl Pts',(0.100300328103893,0.140963653630822,
0.341513229279539));
#18231=CARTESIAN_POINT('Ctrl Pts',(-0.0641098658012952,0.160688619913292,
0.349455397402319));
#18232=CARTESIAN_POINT('Ctrl Pts',(-0.16978883637574,0.033206302186043,
0.357397565525099));
#18233=CARTESIAN_POINT('Ctrl Pts',(-0.119923789760104,-0.124696399756661,
0.36533973364788));
#18234=CARTESIAN_POINT('Ctrl Pts',(0.0398037685148125,-0.168364388974385,
0.373281901770659));
#18235=CARTESIAN_POINT('Ctrl Pts',(0.163066985633654,-0.0577933011607096,
0.38122406989344));
#18236=CARTESIAN_POINT('Ctrl Pts',(0.136944091404129,0.10572238784759,0.38916623801622));
#18237=CARTESIAN_POINT('Ctrl Pts',(-0.0146336593526265,0.172385508313924,
0.397108406138999));
#18238=CARTESIAN_POINT('Ctrl Pts',(-0.152805474769431,0.0811257933285562,
0.40505057426178));
#18239=CARTESIAN_POINT('Ctrl Pts',(-0.150991776994562,-0.0844534827151793,
0.412992742384559));
#18240=CARTESIAN_POINT('Ctrl Pts',(-0.0108540995180527,-0.172664692355881,
0.42093491050734));
#18241=CARTESIAN_POINT('Ctrl Pts',(0.139227048201004,-0.102697305280782,
0.428877078630119));
#18242=CARTESIAN_POINT('Ctrl Pts',(0.16176191642983,0.0613513639265466,
0.4368192467529));
#18243=CARTESIAN_POINT('Ctrl Pts',(0.0361062507758455,0.169195880912067,
0.444761414875679));
#18244=CARTESIAN_POINT('Ctrl Pts',(-0.12262644992489,0.12203958882886,0.45270358299846));
#18245=CARTESIAN_POINT('Ctrl Pts',(-0.169020724600573,-0.0369175042249048,
0.460645751121239));
#18246=CARTESIAN_POINT('Ctrl Pts',(-0.0605746513833496,-0.162054370729346,
0.468587919244019));
#18247=CARTESIAN_POINT('Ctrl Pts',(0.103364025571403,-0.138732785167649,
0.4765300873668));
#18248=CARTESIAN_POINT('Ctrl Pts',(0.172610636112938,0.0116822841681558,
0.484472255489579));
#18249=CARTESIAN_POINT('Ctrl Pts',(0.083728171010617,0.151395181039277,
0.49241442361236));
#18250=CARTESIAN_POINT('Ctrl Pts',(-0.081857900459256,0.152414538660527,
0.500356591735139));
#18251=CARTESIAN_POINT('Ctrl Pts',(-0.172453725526818,0.0138065207282529,
0.50829875985792));
#18252=CARTESIAN_POINT('Ctrl Pts',(-0.105064221167447,-0.137449688588867,
0.516240927980699));
#18253=CARTESIAN_POINT('Ctrl Pts',(0.0585749034388466,-0.162787862415564,
0.52418309610348));
#18254=CARTESIAN_POINT('Ctrl Pts',(0.168553398866689,-0.0389956304370821,
0.532125264226259));
#18255=CARTESIAN_POINT('Ctrl Pts',(0.124119664784058,0.120520605195094,
0.54006743234904));
#18256=CARTESIAN_POINT('Ctrl Pts',(-0.0340204335384149,0.16962758491636,
0.548009600471819));
#18257=CARTESIAN_POINT('Ctrl Pts',(-0.160994319687769,0.0633382703503284,
0.5559517685946));
#18258=CARTESIAN_POINT('Ctrl Pts',(-0.14048086942825,-0.100975406844349,
0.563893936717379));
#18259=CARTESIAN_POINT('Ctrl Pts',(0.00872748937560605,-0.172785237771916,
0.57183610484016));
#18260=CARTESIAN_POINT('Ctrl Pts',(0.149940571302356,-0.0863060399984934,
0.579778272962939));
#18261=CARTESIAN_POINT('Ctrl Pts',(0.153792685935992,0.0792383569699183,
0.58772044108572));
#18262=CARTESIAN_POINT('Ctrl Pts',(0.0167549005293281,0.17219227848818,
0.595662609208499));
#18263=CARTESIAN_POINT('Ctrl Pts',(-0.135632095058532,0.107400382926376,
0.60360477733128));
#18264=CARTESIAN_POINT('Ctrl Pts',(-0.163766157558233,-0.0557812970565469,
0.611546945454059));
#18265=CARTESIAN_POINT('Ctrl Pts',(-0.0418735953979919,-0.167861578305293,
0.61948911357684));
#18266=CARTESIAN_POINT('Ctrl Pts',(0.118379481984711,-0.126163408751231,
0.627431281699619));
#18267=CARTESIAN_POINT('Ctrl Pts',(0.17018479228316,0.0311134044783985,
0.6353734498224));
#18268=CARTESIAN_POINT('Ctrl Pts',(0.0660833491022344,0.159887142804326,
0.643315617945179));
#18269=CARTESIAN_POINT('Ctrl Pts',(-0.0985572308567358,0.142187832491218,
0.651257786067961));
#18270=CARTESIAN_POINT('Ctrl Pts',(-0.172909262181909,-0.00577013989488307,
0.659199954190738));
#18271=CARTESIAN_POINT('Ctrl Pts',(-0.0888586457050277,-0.148442071348278,
0.667142122313521));
#18272=CARTESIAN_POINT('Ctrl Pts',(0.0765956190331784,-0.155125815413241,
0.675084290436298));
#18273=CARTESIAN_POINT('Ctrl Pts',(0.171880427770071,-0.0196983758791502,
0.683026458559081));
#18274=CARTESIAN_POINT('Ctrl Pts',(0.109705106722326,0.133774799651286,
0.690968626681858));
#18275=CARTESIAN_POINT('Ctrl Pts',(-0.0529713625168984,0.164696515493808,
0.698910794804641));
#18276=CARTESIAN_POINT('Ctrl Pts',(-0.167120621735807,0.0447393032280997,
0.706852962927418));
#18277=CARTESIAN_POINT('Ctrl Pts',(-0.12817022249092,-0.116203707037801,
0.7147951310502));
#18278=CARTESIAN_POINT('Ctrl Pts',(0.0281972679828983,-0.17069218359667,
0.722737299172979));
#18279=CARTESIAN_POINT('Ctrl Pts',(0.158733164168978,-0.0688090841067,0.73067946729576));
#18280=CARTESIAN_POINT('Ctrl Pts',(0.14385317469873,0.0961102054508026,
0.738621635418538));
#18281=CARTESIAN_POINT('Ctrl Pts',(-0.00281110139369983,0.172982673038814,
0.746563803541321));
#18282=CARTESIAN_POINT('Ctrl Pts',(-0.146900119814081,0.0913852409380608,
0.754505971664098));
#18283=CARTESIAN_POINT('Ctrl Pts',(-0.156413536862055,-0.0739304602244656,
0.762448139786881));
#18284=CARTESIAN_POINT('Ctrl Pts',(-0.0226360851712103,-0.171518264656626,
0.770390307909658));
#18285=CARTESIAN_POINT('Ctrl Pts',(0.131878346029848,-0.111977717922496,
0.778332476032441));
#18286=CARTESIAN_POINT('Ctrl Pts',(0.165578663890314,0.0501459223366878,
0.786274644155218));
#18287=CARTESIAN_POINT('Ctrl Pts',(0.047591915084802,0.166330746049129,
0.794216812278001));
#18288=CARTESIAN_POINT('Ctrl Pts',(-0.113993917241593,0.130139518573781,
0.802158980400778));
#18289=CARTESIAN_POINT('Ctrl Pts',(-0.171149610334614,-0.0252728776558711,
0.81010114852356));
#18290=CARTESIAN_POINT('Ctrl Pts',(-0.0715146774936035,-0.157532721571376,
0.818043316646339));
#18291=CARTESIAN_POINT('Ctrl Pts',(0.0936350469135118,-0.14547640857611,
0.825985484769119));
#18292=CARTESIAN_POINT('Ctrl Pts',(0.173005448853992,-0.000148759965830227,
0.8339276528919));
#18293=CARTESIAN_POINT('Ctrl Pts',(0.0938850861191564,0.145315168055841,
0.841869821014678));
#18294=CARTESIAN_POINT('Ctrl Pts',(-0.0712436606821878,0.157655473343934,
0.849811989137461));
#18295=CARTESIAN_POINT('Ctrl Pts',(-0.171105895159299,0.0255671684868261,
0.857754157260238));
#18296=CARTESIAN_POINT('Ctrl Pts',(-0.114217551294,-0.129943289319231,0.86569632538302));
#18297=CARTESIAN_POINT('Ctrl Pts',(0.0473058035714782,-0.166412344527548,
0.873638493505798));
#18298=CARTESIAN_POINT('Ctrl Pts',(0.16549218245563,-0.0504305959589149,
0.88158066162858));
#18299=CARTESIAN_POINT('Ctrl Pts',(0.132070720552549,0.111750759440056,
0.889522829751358));
#18300=CARTESIAN_POINT('Ctrl Pts',(-0.022341089517305,0.171556938600217,
0.89746499787414));
#18301=CARTESIAN_POINT('Ctrl Pts',(-0.156286166401977,0.074199337288632,
0.905407165996919));
#18302=CARTESIAN_POINT('Ctrl Pts',(-0.147057058974526,-0.0911324797668838,
0.913349334119699));
#18303=CARTESIAN_POINT('Ctrl Pts',(-0.00310857778072832,-0.172977582960567,
0.92129150224248));
#18304=CARTESIAN_POINT('Ctrl Pts',(0.143687680016546,-0.0963574495000853,
0.929233670365259));
#18305=CARTESIAN_POINT('Ctrl Pts',(0.158851261322436,0.0685360068793772,
0.93717583848804));
#18306=CARTESIAN_POINT('Ctrl Pts',(0.0284907678468484,0.170643439985825,
0.945118006610819));
#18307=CARTESIAN_POINT('Ctrl Pts',(-0.127970195944242,0.116423951198588,
0.9530601747336));
#18308=CARTESIAN_POINT('Ctrl Pts',(-0.167197313372666,-0.0444518375735043,
0.961002342856378));
#18309=CARTESIAN_POINT('Ctrl Pts',(-0.0532545149190986,-0.164605176417482,
0.96894451097916));
#18310=CARTESIAN_POINT('Ctrl Pts',(0.10947489024455,-0.133963263130763,
0.976886679101939));
#18311=CARTESIAN_POINT('Ctrl Pts',(0.1719140491614,0.0194027617526574,0.984828847224719));
#18312=CARTESIAN_POINT('Ctrl Pts',(0.0768622776450996,0.154993863549195,
0.992771015347499));
#18313=CARTESIAN_POINT('Ctrl Pts',(-0.088603236555915,0.148594663210074,
1.00071318347028));
#18314=CARTESIAN_POINT('Ctrl Pts',(-0.172899083515371,0.00606748566075909,
1.00865535159306));
#18315=CARTESIAN_POINT('Ctrl Pts',(-0.0988016073770141,-0.142018132090297,
1.01659751971584));
#18316=CARTESIAN_POINT('Ctrl Pts',(0.0658082913934689,-0.160000550769587,
1.02453968783862));
#18317=CARTESIAN_POINT('Ctrl Pts',(0.170131034504888,-0.0314060274628177,
1.0324818559614));
#18318=CARTESIAN_POINT('Ctrl Pts',(0.118596271784576,0.125959643463681,
1.04042402408418));
#18319=CARTESIAN_POINT('Ctrl Pts',(-0.0415848597483297,0.167933340651612,
1.04836619220696));
#18320=CARTESIAN_POINT('Ctrl Pts',(-0.163669987576804,0.0560628453550813,
1.05630836032974));
#18321=CARTESIAN_POINT('Ctrl Pts',(-0.135816592328243,-0.107166975841641,
1.06425052845252));
#18322=CARTESIAN_POINT('Ctrl Pts',(0.0164587544616562,-0.172220837485682,
1.0721926965753));
#18323=CARTESIAN_POINT('Ctrl Pts',(0.153656191292587,-0.0795027190739688,
1.08013486469808));
#18324=CARTESIAN_POINT('Ctrl Pts',(0.150088771199207,0.0860480576341552,
1.08807703282086));
#18325=CARTESIAN_POINT('Ctrl Pts',(0.00902461748204118,0.172769973496559,
1.09601920094364));
#18326=CARTESIAN_POINT('Ctrl Pts',(-0.140307012982855,0.101216844302358,
1.10396136906642));
#18327=CARTESIAN_POINT('Ctrl Pts',(-0.161103005268346,-0.0630613126743013,
1.1119035371892));
#18328=CARTESIAN_POINT('Ctrl Pts',(-0.0343120939874615,-0.1695688287065,
1.11984570531198));
#18329=CARTESIAN_POINT('Ctrl Pts',(0.123912220401285,-0.120733877175888,
1.12778787343476));
#18330=CARTESIAN_POINT('Ctrl Pts',(0.168620210916381,0.0387057093103061,
1.13573004155754));
#18331=CARTESIAN_POINT('Ctrl Pts',(0.0588547652196237,0.162686889679659,
1.14367220968032));
#18332=CARTESIAN_POINT('Ctrl Pts',(-0.104827691798069,0.137630165643247,
1.1516143778031));
#18333=CARTESIAN_POINT('Ctrl Pts',(-0.172477213770776,-0.0135099294065116,
1.15955654592588));
#18334=CARTESIAN_POINT('Ctrl Pts',(-0.0821198886720452,-0.152273541192125,
1.16749871404866));
#18335=CARTESIAN_POINT('Ctrl Pts',(0.083467690946984,-0.15153894559049,
1.17544088217144));
#18336=CARTESIAN_POINT('Ctrl Pts',(0.172590290696882,-0.0119791076405788,
1.18338305029422));
#18337=CARTESIAN_POINT('Ctrl Pts',(0.103602453294194,0.13855482356859,1.191325218417));
#18338=CARTESIAN_POINT('Ctrl Pts',(-0.0602958748103966,0.162158302111078,
1.19926738653978));
#18339=CARTESIAN_POINT('Ctrl Pts',(-0.168956987158091,0.0372081167644847,
1.20720955466256));
#18340=CARTESIAN_POINT('Ctrl Pts',(-0.122836141658186,-0.121828526073448,
1.21515172278534));
#18341=CARTESIAN_POINT('Ctrl Pts',(0.0358152290369173,-0.169257723108079,
1.22309389090812));
#18342=CARTESIAN_POINT('Ctrl Pts',(0.161656170495932,-0.0616294572691503,
1.2310360590309));
#18343=CARTESIAN_POINT('Ctrl Pts',(0.13940345221127,0.102457722863032,1.23897822715368));
#18344=CARTESIAN_POINT('Ctrl Pts',(-0.0105571497596809,0.172683102970871,
1.24692039527646));
#18345=CARTESIAN_POINT('Ctrl Pts',(-0.150846317973597,0.0847130203482025,
1.25486256339924));
#18346=CARTESIAN_POINT('Ctrl Pts',(-0.152944761892581,-0.0808628918127005,
1.26280473152202));
#18347=CARTESIAN_POINT('Ctrl Pts',(-0.0149300913057054,-0.172360087712588,
1.2707468996448));
#18348=CARTESIAN_POINT('Ctrl Pts',(0.136762076743997,-0.105957736043287,
1.27868906776758));
#18349=CARTESIAN_POINT('Ctrl Pts',(0.163166132393764,0.0575127872937276,
1.28663123589036));
#18350=CARTESIAN_POINT('Ctrl Pts',(0.0400932480780463,0.168295688956082,
1.29457340401314));
#18351=CARTESIAN_POINT('Ctrl Pts',(-0.119709170414695,0.124902449862528,
1.30251557213592));
#18352=CARTESIAN_POINT('Ctrl Pts',(-0.169845690614082,-0.0329142650230248,
1.3104577402587));
#18353=CARTESIAN_POINT('Ctrl Pts',(-0.0643861093061943,-0.160578131733314,
1.31839990838148));
#18354=CARTESIAN_POINT('Ctrl Pts',(0.100057762773863,-0.141135932963798,
1.32634207650426));
#18355=CARTESIAN_POINT('Ctrl Pts',(0.172838444806952,0.00760127985757451,
1.33428424462704));
#18356=CARTESIAN_POINT('Ctrl Pts',(0.0872813550697656,0.149374939398002,
1.34222641274982));
#18357=CARTESIAN_POINT('Ctrl Pts',(-0.0782344227434143,0.154305808621531,
1.3501685808726));
#18358=CARTESIAN_POINT('Ctrl Pts',(-0.172079431848303,0.0178767046294837,
1.35811074899538));
#18359=CARTESIAN_POINT('Ctrl Pts',(-0.108282003268856,-0.134929297194493,
1.36605291711816));
#18360=CARTESIAN_POINT('Ctrl Pts',(0.0547128650701426,-0.164126201264144,
1.37399508524094));
#18361=CARTESIAN_POINT('Ctrl Pts',(0.167585127127835,-0.0429666431014547,
1.38193725336372));
#18362=CARTESIAN_POINT('Ctrl Pts',(0.126932197981417,0.117554773230619,
1.3898794214865));
#18363=CARTESIAN_POINT('Ctrl Pts',(-0.0300036684000219,0.170383942402052,
1.39782158960928));
#18364=CARTESIAN_POINT('Ctrl Pts',(-0.159453085214751,0.0671239123677834,
1.40576375773206));
#18365=CARTESIAN_POINT('Ctrl Pts',(-0.142827107870127,-0.0976285101620078,
1.41370592585484));
#18366=CARTESIAN_POINT('Ctrl Pts',(0.00464319840846943,-0.172943201171859,
1.42164809397762));
#18367=CARTESIAN_POINT('Ctrl Pts',(0.147859810582222,-0.0898241270588577,
1.4295902621004));
#18368=CARTESIAN_POINT('Ctrl Pts',(0.155621735944117,0.0755830265922534,
1.43753243022318));
#18369=CARTESIAN_POINT('Ctrl Pts',(0.0208179928734729,0.171748455656582,
1.44547459834596));
#18370=CARTESIAN_POINT('Ctrl Pts',(-0.133056846329205,0.11057447892796,
1.45341676646874));
#18371=CARTESIAN_POINT('Ctrl Pts',(-0.165038560097216,-0.0518967460486161,
1.46135893459152));
#18372=CARTESIAN_POINT('Ctrl Pts',(-0.0458268296361176,-0.166825854601292,
1.4693011027143));
#18373=CARTESIAN_POINT('Ctrl Pts',(0.115364766925686,-0.128924136976022,
1.47724327083708));
#18374=CARTESIAN_POINT('Ctrl Pts',(0.170874595884426,0.0270830477535184,
1.48518543895986));
#18375=CARTESIAN_POINT('Ctrl Pts',(0.0698377457337486,0.158283721017069,
1.49312760708264));
#18376=CARTESIAN_POINT('Ctrl Pts',(-0.0951624750893037,0.144471999488883,
1.50106977520542));
#18377=CARTESIAN_POINT('Ctrl Pts',(-0.173012914651864,-0.00167525885548286,
1.5090119433282));
#18378=CARTESIAN_POINT('Ctrl Pts',(-0.092311001583214,-0.14631755460685,
1.51695411145098));
#18379=CARTESIAN_POINT('Ctrl Pts',(0.072853104778531,-0.156861289272697,
1.52489627957376));
#18380=CARTESIAN_POINT('Ctrl Pts',(0.171475934783304,-0.0238129810547936,
1.53283844769654));
#18381=CARTESIAN_POINT('Ctrl Pts',(0.11261423476106,0.131269690464983,1.54078061581932));
#18382=CARTESIAN_POINT('Ctrl Pts',(0.00518264413773371,0.154149172621267,
1.54607539456784));
#18383=CARTESIAN_POINT('Ctrl Pts',(-0.0415060733757155,0.140340900570467,
1.5487227839421));
#18384=CARTESIAN_POINT('Ctrl Pts',(-0.146248097568756,-0.000123763188177425,
1.45893449541571));
#18385=CARTESIAN_POINT('Ctrl Pts',(-0.146367493381718,-0.0150081347743067,
1.45974264180765));
#18386=CARTESIAN_POINT('Ctrl Pts',(-0.144277648885518,-0.0298597803798721,
1.46055078819958));
#18387=CARTESIAN_POINT('Ctrl Pts',(-0.139839652725699,-0.043973059977961,
1.46135893459152));
#18388=CARTESIAN_POINT('Ctrl Pts',(-0.125301316610186,-0.0902064488995044,
1.46400632396578));
#18389=CARTESIAN_POINT('Ctrl Pts',(-0.08556407312315,-0.1285161517504,1.46665371334004));
#18390=CARTESIAN_POINT('Ctrl Pts',(-0.0388301852859989,-0.141354050238301,
1.4693011027143));
#18391=CARTESIAN_POINT('Ctrl Pts',(0.00790370255115092,-0.154191948726202,
1.47194849208856));
#18392=CARTESIAN_POINT('Ctrl Pts',(0.0616342347384179,-0.141558042851112,
1.47459588146282));
#18393=CARTESIAN_POINT('Ctrl Pts',(0.0977511389918415,-0.109239892458645,
1.47724327083708));
#18394=CARTESIAN_POINT('Ctrl Pts',(0.133868043245265,-0.0769217420661769,
1.47989066021134));
#18395=CARTESIAN_POINT('Ctrl Pts',(0.152371319564846,-0.024919347156331,
1.4825380495856));
#18396=CARTESIAN_POINT('Ctrl Pts',(0.144783482699524,0.0229486291758506,
1.48518543895986));
#18397=CARTESIAN_POINT('Ctrl Pts',(0.137195645834202,0.0708166055080336,
1.48783282833412));
#18398=CARTESIAN_POINT('Ctrl Pts',(0.103516695783975,0.114550163262552,
1.49048021770838));
#18399=CARTESIAN_POINT('Ctrl Pts',(0.0591771839550196,0.13411498855178,
1.49312760708264));
#18400=CARTESIAN_POINT('Ctrl Pts',(0.014837672126065,0.153679813841007,
1.4957749964569));
#18401=CARTESIAN_POINT('Ctrl Pts',(-0.0401624014816186,0.149075906664945,
1.49842238583116));
#18402=CARTESIAN_POINT('Ctrl Pts',(-0.0806375115458872,0.122416076686187,
1.50106977520542));
#18403=CARTESIAN_POINT('Ctrl Pts',(-0.0937869288003098,0.113754921033589,
1.50192985013695));
#18404=CARTESIAN_POINT('Ctrl Pts',(-0.105403311347291,0.102765876910903,
1.50278992506847));
#18405=CARTESIAN_POINT('Ctrl Pts',(-0.115078604842433,0.0902138214954038,
1.50365));
#18406=CARTESIAN_POINT('Ctrl Pts',(-0.0686146973663081,-0.0959584553529135,
1.07336015076065E-17));
#18407=CARTESIAN_POINT('Ctrl Pts',(-0.0712979561985307,-0.0944995001033786,
9.02613639135873E-18));
#18408=CARTESIAN_POINT('Ctrl Pts',(-0.0739152333025289,-0.0929325179580126,
1.64107321374712E-17));
#18409=CARTESIAN_POINT('Ctrl Pts',(-0.0764591723283171,-0.0912589988675934,
1.6154612370034E-17));
#18410=CARTESIAN_POINT('Ctrl Pts',(-0.0824897891353913,-0.0872917841461184,
1.52077426268717E-17));
#18411=CARTESIAN_POINT('Ctrl Pts',(-0.0881090519769445,-0.0827275518978924,
1.30971627060498E-17));
#18412=CARTESIAN_POINT('Ctrl Pts',(-0.0932912133381108,-0.0776621329443405,
1.43114686768087E-17));
#18413=CARTESIAN_POINT('Ctrl Pts',(-0.0960634919631888,-0.074952307504085,
1.49610807310118E-17));
#18414=CARTESIAN_POINT('Ctrl Pts',(-0.0987043519497191,-0.0721043812799658,
1.74993329480528E-17));
#18415=CARTESIAN_POINT('Ctrl Pts',(-0.101206237074718,-0.0691378820326018,
9.97465998686664E-18));
#18416=CARTESIAN_POINT('Ctrl Pts',(-0.105823426721714,-0.0636632543305198,
-3.91200561030858E-18));
#18417=CARTESIAN_POINT('Ctrl Pts',(-0.109972666997065,-0.0577811896139199,
2.24798207762934E-18));
#18418=CARTESIAN_POINT('Ctrl Pts',(-0.113625452403263,-0.0515741981665521,
9.54097911787244E-18));
#18419=CARTESIAN_POINT('Ctrl Pts',(-0.115386295340069,-0.0485820878086944,
1.30566037435822E-17));
#18420=CARTESIAN_POINT('Ctrl Pts',(-0.117027309103105,-0.0455212415157476,
-2.79521757168051E-18));
#18421=CARTESIAN_POINT('Ctrl Pts',(-0.118543833519887,-0.0424058589801268,
-3.46944695195361E-18));
#18422=CARTESIAN_POINT('Ctrl Pts',(-0.122700941917732,-0.0338659484069709,
-5.31764971597768E-18));
#18423=CARTESIAN_POINT('Ctrl Pts',(-0.125931492798984,-0.0249085743588085,
-1.15219401683824E-18));
#18424=CARTESIAN_POINT('Ctrl Pts',(-0.128167520083254,-0.0157105262534848,
9.54097911787244E-18));
#18425=CARTESIAN_POINT('Ctrl Pts',(-0.128992166906242,-0.0123182862745252,
1.3484621181291E-17));
#18426=CARTESIAN_POINT('Ctrl Pts',(-0.129681150280034,-0.00889298553317688,
1.10989611676181E-17));
#18427=CARTESIAN_POINT('Ctrl Pts',(-0.130229483957028,-0.00544263935519351,
9.54097911787244E-18));
#18428=CARTESIAN_POINT('Ctrl Pts',(-0.130761899349706,-0.00209245771889707,
8.02822573502553E-18));
#18429=CARTESIAN_POINT('Ctrl Pts',(-0.131160261982709,0.00127366115726457,
1.11791151702242E-17));
#18430=CARTESIAN_POINT('Ctrl Pts',(-0.131420990891747,0.00464012593483382,
8.67361737988404E-18));
#18431=CARTESIAN_POINT('Ctrl Pts',(-0.131728666658755,0.00861275649723166,
5.71697955546795E-18));
#18432=CARTESIAN_POINT('Ctrl Pts',(-0.131845259942619,0.0125891451047215,
-9.26473565962443E-18));
#18433=CARTESIAN_POINT('Ctrl Pts',(-0.131765781147177,0.0165567997877194,
-1.04083408558608E-17));
#18434=CARTESIAN_POINT('Ctrl Pts',(-0.131635692412819,0.0230509492424239,
-1.21888544026837E-17));
#18435=CARTESIAN_POINT('Ctrl Pts',(-0.13098103789945,0.0295216962360144,
-2.67049856555875E-17));
#18436=CARTESIAN_POINT('Ctrl Pts',(-0.129839098367345,0.0359278479980343,
-3.46944695195361E-17));
#18437=CARTESIAN_POINT('Ctrl Pts',(-0.129254890951344,0.0392051855997028,
-3.87818275556788E-17));
#18438=CARTESIAN_POINT('Ctrl Pts',(-0.128542951403208,0.0424656461998481,
-3.10678831811161E-17));
#18439=CARTESIAN_POINT('Ctrl Pts',(-0.1277070993652,0.0457037274559979,
-3.29597460435593E-17));
#18440=CARTESIAN_POINT('Ctrl Pts',(-0.126886363095037,0.0488832504000222,
-3.48173959609792E-17));
#18441=CARTESIAN_POINT('Ctrl Pts',(-0.125948031872817,0.0520333657183593,
-3.53366201082739E-17));
#18442=CARTESIAN_POINT('Ctrl Pts',(-0.124899042599898,0.0551436241923499,
-3.46944695195361E-17));
#18443=CARTESIAN_POINT('Ctrl Pts',(-0.122234979928128,0.0630425834229368,
-3.30636335736642E-17));
#18444=CARTESIAN_POINT('Ctrl Pts',(-0.118856305871375,0.070695441500891,
-2.1366080483524E-17));
#18445=CARTESIAN_POINT('Ctrl Pts',(-0.114834854776346,0.078019637496205,
-1.73472347597681E-17));
#18446=CARTESIAN_POINT('Ctrl Pts',(-0.11215901866562,0.0828930893082948,
-1.46731322388254E-17));
#18447=CARTESIAN_POINT('Ctrl Pts',(-0.109198005187061,0.0876211033078822,
8.28606628989234E-18));
#18448=CARTESIAN_POINT('Ctrl Pts',(-0.105966883726074,0.0921780034666525,
8.67361737988404E-18));
#18449=CARTESIAN_POINT('Ctrl Pts',(-0.104137243112614,0.094758373688769,
8.89307035390601E-18));
#18450=CARTESIAN_POINT('Ctrl Pts',(-0.102221042121924,0.0972831505018574,
-2.31209379389524E-17));
#18451=CARTESIAN_POINT('Ctrl Pts',(-0.100229777791505,0.0997373632832089,
-2.08166817117217E-17));
#18452=CARTESIAN_POINT('Ctrl Pts',(-0.0937202782075859,0.107760254486057,
-1.32840027382311E-17));
#18453=CARTESIAN_POINT('Ctrl Pts',(-0.0863914655699752,0.115060936709644,
5.4842312373535E-18));
#18454=CARTESIAN_POINT('Ctrl Pts',(-0.0783508402622743,0.121487309774744,
1.38777878078145E-17));
#18455=CARTESIAN_POINT('Ctrl Pts',(-0.073610711791116,0.125275800441382,
1.8825977152717E-17));
#18456=CARTESIAN_POINT('Ctrl Pts',(-0.068622257850438,0.128760167547443,
-9.09579695168528E-18));
#18457=CARTESIAN_POINT('Ctrl Pts',(-0.0634007094575209,0.131904027763685,
-6.93889390390723E-18));
#18458=CARTESIAN_POINT('Origin',(0.,0.,0.));
#18459=CARTESIAN_POINT('Origin',(-0.0721687836487033,-0.125,-0.3));
#18460=CARTESIAN_POINT('',(-0.0721687836487033,-0.125,-0.3));
#18461=CARTESIAN_POINT('',(0.0721687836487032,-0.125,-0.3));
#18462=CARTESIAN_POINT('',(-0.0360843918243517,-0.125,-0.3));
#18463=CARTESIAN_POINT('',(-0.0721687836487033,-0.125,-0.15));
#18464=CARTESIAN_POINT('',(-0.0721687836487033,-0.125,-0.3));
#18465=CARTESIAN_POINT('',(0.0721687836487032,-0.125,-0.15));
#18466=CARTESIAN_POINT('',(-0.0721687836487033,-0.125,-0.15));
#18467=CARTESIAN_POINT('',(0.0721687836487032,-0.125,-0.3));
#18468=CARTESIAN_POINT('Origin',(-0.144337567297406,1.76762539787485E-17,
-0.3));
#18469=CARTESIAN_POINT('',(-0.144337567297406,1.76762539787485E-17,-0.3));
#18470=CARTESIAN_POINT('',(-0.126295371385231,-0.03125,-0.3));
#18471=CARTESIAN_POINT('',(-0.144337567297406,2.77555756156289E-17,-0.15));
#18472=CARTESIAN_POINT('',(-0.144337567297406,1.76762539787485E-17,-0.3));
#18473=CARTESIAN_POINT('',(-0.144337567297406,1.76762539787485E-17,-0.15));
#18474=CARTESIAN_POINT('Origin',(-0.0721687836487032,0.125,-0.3));
#18475=CARTESIAN_POINT('',(-0.0721687836487032,0.125,-0.3));
#18476=CARTESIAN_POINT('',(-0.090210979560879,0.09375,-0.3));
#18477=CARTESIAN_POINT('',(-0.0721687836487032,0.125,-0.15));
#18478=CARTESIAN_POINT('',(-0.0721687836487032,0.125,-0.3));
#18479=CARTESIAN_POINT('',(-0.0721687836487032,0.125,-0.15));
#18480=CARTESIAN_POINT('Origin',(0.0721687836487032,0.125,-0.3));
#18481=CARTESIAN_POINT('',(0.0721687836487032,0.125,-0.3));
#18482=CARTESIAN_POINT('',(0.0360843918243516,0.125,-0.3));
#18483=CARTESIAN_POINT('',(0.0721687836487032,0.125,-0.15));
#18484=CARTESIAN_POINT('',(0.0721687836487032,0.125,-0.3));
#18485=CARTESIAN_POINT('',(0.0721687836487032,0.125,-0.15));
#18486=CARTESIAN_POINT('Origin',(0.144337567297406,0.,-0.3));
#18487=CARTESIAN_POINT('',(0.144337567297406,0.,-0.3));
#18488=CARTESIAN_POINT('',(0.126295371385231,0.03125,-0.3));
#18489=CARTESIAN_POINT('',(0.144337567297406,0.,-0.15));
#18490=CARTESIAN_POINT('',(0.144337567297406,0.,-0.3));
#18491=CARTESIAN_POINT('',(0.144337567297406,0.,-0.15));
#18492=CARTESIAN_POINT('Origin',(0.0721687836487032,-0.125,-0.3));
#18493=CARTESIAN_POINT('',(0.0902109795608791,-0.09375,-0.3));
#18494=CARTESIAN_POINT('',(0.0721687836487032,-0.125,-0.15));
#18495=CARTESIAN_POINT('Origin',(0.,0.,-0.15));
#18496=CARTESIAN_POINT('Origin',(0.,0.,0.));
#18497=CARTESIAN_POINT('',(-0.275,-3.36777869765522E-17,0.));
#18498=CARTESIAN_POINT('Origin',(0.,0.,0.));
#18499=CARTESIAN_POINT('Origin',(0.,0.,-0.3));
#18500=CARTESIAN_POINT('',(-0.275,-3.36777869765522E-17,-0.3));
#18501=CARTESIAN_POINT('',(-0.275,-3.36777869765522E-17,-0.3));
#18502=CARTESIAN_POINT('Origin',(0.,0.,-0.3));
#18503=CARTESIAN_POINT('Origin',(0.,0.,-0.3));
#18504=CARTESIAN_POINT('Origin',(0.,0.,1.6));
#19455=UNCERTAINTY_MEASURE_WITH_UNIT(LENGTH_MEASURE(0.001),#19472,
'DISTANCE_ACCURACY_VALUE',
'Maximum model space distance between geometric entities at asserted c
onnectivities');
#19458=UNCERTAINTY_MEASURE_WITH_UNIT(LENGTH_MEASURE(0.001),#19472,
'DISTANCE_ACCURACY_VALUE',
'Maximum model space distance between geometric entities at asserted c
onnectivities');
#19468=(
GEOMETRIC_REPRESENTATION_CONTEXT(3)
GLOBAL_UNCERTAINTY_ASSIGNED_CONTEXT((#19455))
GLOBAL_UNIT_ASSIGNED_CONTEXT((#19472,#19474,#19475))
REPRESENTATION_CONTEXT('','3D')
);
#19471=(
GEOMETRIC_REPRESENTATION_CONTEXT(3)
GLOBAL_UNCERTAINTY_ASSIGNED_CONTEXT((#19458))
GLOBAL_UNIT_ASSIGNED_CONTEXT((#19472,#19474,#19475))
REPRESENTATION_CONTEXT('','3D')
);
#19472=(
LENGTH_UNIT()
NAMED_UNIT(*)
SI_UNIT(.CENTI.,.METRE.)
);
#19474=(
NAMED_UNIT(*)
PLANE_ANGLE_UNIT()
SI_UNIT($,.RADIAN.)
);
#19475=(
NAMED_UNIT(*)
SI_UNIT($,.STERADIAN.)
SOLID_ANGLE_UNIT()
);
#19485=SHAPE_DEFINITION_REPRESENTATION(#19497,#19525);
#19497=PRODUCT_DEFINITION_SHAPE('',$,#19538);
#19525=SHAPE_REPRESENTATION('',(#7686),#19468);
#19528=PRODUCT_DEFINITION_CONTEXT('part definition',#19566,'design');
#19538=PRODUCT_DEFINITION('2026-11-10-01-30-02-397',
'Socket head cap screw M3x16',#19550,#19528);
#19550=PRODUCT_DEFINITION_FORMATION('',$,#19577);
#19566=APPLICATION_CONTEXT(
'Core Data for Automotive Mechanical Design Process');
#19567=PRODUCT_CONTEXT('part definition',#19566,'mechanical');
#19577=PRODUCT('2026-11-10-01-30-02-397','Socket head cap screw M3x16',
$,(#19567));
#19583=PRESENTATION_STYLE_ASSIGNMENT((#19591));
#19591=SURFACE_STYLE_USAGE(.BOTH.,#19599);
#19599=SURFACE_SIDE_STYLE('',(#19607));
#19607=SURFACE_STYLE_FILL_AREA(#19615);
#19615=FILL_AREA_STYLE('Dark gray',(#19623));
#19623=FILL_AREA_STYLE_COLOUR('Dark gray',#19631);
#19631=COLOUR_RGB('Dark gray',0.250980392156863,0.282352941176471,0.32156862745098);
ENDSEC;
END-ISO-10303-21;
